ISO-10303-21;
HEADER;
FILE_DESCRIPTION (('STEP AP214'),
    '1' );
FILE_NAME ('Main Body.step',
    '2026-10-07T18:46:32',
    ( '' ),
    ( '' ),
    'SwSTEP 2.0',
    'SolidWorks 2020',
    '' );
FILE_SCHEMA (( 'AUTOMOTIVE_DESIGN' ));
ENDSEC;

DATA;
#1=DIRECTION ( 'NONE',  ( -1.000000000000000000, 0.000000000000000000, 0.000000000000000000 ) ) ;
#4=CARTESIAN_POINT ( 'NONE',  ( -15.21174975910704852, -52.39333383871510108, 13.50000000000000000 ) ) ;
#9=CARTESIAN_POINT ( 'NONE',  ( -3.127054932750481964, 33.43424481021354921, 68.00000000000000000 ) ) ;
#11=CIRCLE ( 'NONE', #13928, 0.6999999999999992895 ) ;
#14=CARTESIAN_POINT ( 'NONE',  ( 23.02398829872513986, 5.683640910026983128, 42.50000000000000000 ) ) ;
#15=EDGE_CURVE ( 'NONE', #14785, #7135, #6042, .T. ) ;
#17=VERTEX_POINT ( 'NONE', #7499 ) ;
#18=VERTEX_POINT ( 'NONE', #14070 ) ;
#19=CARTESIAN_POINT ( 'NONE',  ( 3.127054932750481964, -32.61873716947361856, 68.00000000000000000 ) ) ;
#28=CARTESIAN_POINT ( 'NONE',  ( 0.000000000000000000, -51.61873716947361856, 68.50000000000000000 ) ) ;
#29=DIRECTION ( 'NONE',  ( 0.000000000000000000, 0.000000000000000000, 1.000000000000000000 ) ) ;
#33=CARTESIAN_POINT ( 'NONE',  ( 14.66174975910705314, -51.84675762924568687, 13.49999999999999822 ) ) ;
#34=EDGE_CURVE ( 'NONE', #6576, #7257, #22097, .T. ) ;
#36=CARTESIAN_POINT ( 'NONE',  ( 29.37540678000427619, 6.000000000000000000, 7.200000000000000178 ) ) ;
#40=CARTESIAN_POINT ( 'NONE',  ( 0.000000000000000000, -5.299999999999999822, 7.500000000000000000 ) ) ;
#41=CARTESIAN_POINT ( 'NONE',  ( 25.37540678000427263, 67.24634676501045760, 13.19999999999999929 ) ) ;
#43=AXIS2_PLACEMENT_3D ( 'NONE', #3141, #11622, #1672 ) ;
#48=DIRECTION ( 'NONE',  ( -1.000000000000000000, 0.000000000000000000, 0.000000000000000000 ) ) ;
#49=EDGE_CURVE ( 'NONE', #170, #808, #17062, .T. ) ;
#50=AXIS2_PLACEMENT_3D ( 'NONE', #10111, #15028, #13337 ) ;
#51=CARTESIAN_POINT ( 'NONE',  ( 15.95292532278785913, 32.11873716947361856, 42.50000000000000711 ) ) ;
#54=CARTESIAN_POINT ( 'NONE',  ( 25.37540678000427263, -67.24634676501045760, 13.19999999999999929 ) ) ;
#55=FACE_OUTER_BOUND ( 'NONE', #4259, .T. ) ;
#57=CARTESIAN_POINT ( 'NONE',  ( 25.37540678000427263, 63.74634676501045050, 7.200000000000000178 ) ) ;
#59=EDGE_LOOP ( 'NONE', ( #5538, #18267, #7700, #20296 ) ) ;
#62=EDGE_CURVE ( 'NONE', #14667, #2179, #18422, .T. ) ;
#63=ORIENTED_EDGE ( 'NONE', *, *, #4716, .F. ) ;
#64=CARTESIAN_POINT ( 'NONE',  ( -30.37540678000427619, 0.000000000000000000, 7.500000000000000000 ) ) ;
#66=EDGE_CURVE ( 'NONE', #4678, #19429, #10289, .T. ) ;
#67=DIRECTION ( 'NONE',  ( -1.000000000000000000, 0.000000000000000000, 0.000000000000000000 ) ) ;
#68=ORIENTED_EDGE ( 'NONE', *, *, #21177, .T. ) ;
#72=DIRECTION ( 'NONE',  ( 0.000000000000000000, 0.000000000000000000, -1.000000000000000000 ) ) ;
#74=AXIS2_PLACEMENT_3D ( 'NONE', #22093, #6650, #20627 ) ;
#76=VECTOR ( 'NONE', #22096, 1000.000000000000000 ) ;
#78=ORIENTED_EDGE ( 'NONE', *, *, #20383, .T. ) ;
#79=CARTESIAN_POINT ( 'NONE',  ( 15.95292532278785913, 34.11873716947361856, 109.6002446535588319 ) ) ;
#80=ADVANCED_FACE ( 'NONE', ( #2894 ), #13173, .F. ) ;
#87=CARTESIAN_POINT ( 'NONE',  ( 23.02398829872513986, 3.264788445950721929, 13.78841001078599504 ) ) ;
#88=LINE ( 'NONE', #10714, #11380 ) ;
#89=CIRCLE ( 'NONE', #20092, 3.800000000000004707 ) ;
#93=ORIENTED_EDGE ( 'NONE', *, *, #21253, .F. ) ;
#95=ADVANCED_FACE ( 'NONE', ( #9936 ), #19786, .F. ) ;
#96=EDGE_CURVE ( 'NONE', #20277, #16343, #4681, .T. ) ;
#99=CARTESIAN_POINT ( 'NONE',  ( 15.95292532278785913, -50.11873716947361856, 13.79999999999999893 ) ) ;
#100=EDGE_CURVE ( 'NONE', #8484, #21526, #21584, .T. ) ;
#101=LINE ( 'NONE', #6945, #13482 ) ;
#102=ORIENTED_EDGE ( 'NONE', *, *, #10991, .T. ) ;
#104=VERTEX_POINT ( 'NONE', #1089 ) ;
#106=ORIENTED_EDGE ( 'NONE', *, *, #2093, .F. ) ;
#107=LINE ( 'NONE', #18791, #3053 ) ;
#109=CARTESIAN_POINT ( 'NONE',  ( -17.92752199202934094, 38.74634676501045760, 13.79999999999999893 ) ) ;
#111=DIRECTION ( 'NONE',  ( 0.000000000000000000, 0.000000000000000000, 1.000000000000000000 ) ) ;
#112=CARTESIAN_POINT ( 'NONE',  ( 29.13662752439705272, -5.000000000000000000, 3.799999999999999822 ) ) ;
#118=ORIENTED_EDGE ( 'NONE', *, *, #14708, .F. ) ;
#121=ORIENTED_EDGE ( 'NONE', *, *, #13941, .T. ) ;
#124=VERTEX_POINT ( 'NONE', #8038 ) ;
#125=EDGE_LOOP ( 'NONE', ( #20790, #19352, #641, #8535 ) ) ;
#126=EDGE_CURVE ( 'NONE', #6172, #3604, #6011, .T. ) ;
#127=FACE_OUTER_BOUND ( 'NONE', #20029, .T. ) ;
#128=LINE ( 'NONE', #15349, #12033 ) ;
#129=ADVANCED_FACE ( 'NONE', ( #19899 ), #11490, .T. ) ;
#130=LINE ( 'NONE', #11767, #7823 ) ;
#133=DIRECTION ( 'NONE',  ( 0.000000000000000000, 0.000000000000000000, 1.000000000000000000 ) ) ;
#134=CARTESIAN_POINT ( 'NONE',  ( -30.37540678000427619, -63.74634676501045050, 3.799999999999999822 ) ) ;
#135=LINE ( 'NONE', #17252, #1789 ) ;
#136=DIRECTION ( 'NONE',  ( 1.000000000000000000, 0.000000000000000000, 0.000000000000000000 ) ) ;
#139=CARTESIAN_POINT ( 'NONE',  ( 29.13662752439705272, 5.299999999999999822, 7.500000000000000000 ) ) ;
#142=EDGE_LOOP ( 'NONE', ( #9212, #19592, #9345, #5042 ) ) ;
#143=EDGE_CURVE ( 'NONE', #15755, #12023, #9721, .T. ) ;
#145=ORIENTED_EDGE ( 'NONE', *, *, #17677, .T. ) ;
#147=CIRCLE ( 'NONE', #15855, 1.000000000000000888 ) ;
#148=CARTESIAN_POINT ( 'NONE',  ( 4.127054932750481520, 33.43424481021354921, 13.50000000000000000 ) ) ;
#149=EDGE_CURVE ( 'NONE', #13948, #20015, #21002, .T. ) ;
#151=FACE_OUTER_BOUND ( 'NONE', #855, .T. ) ;
#153=CARTESIAN_POINT ( 'NONE',  ( 27.37540678000427974, -5.683640910026986681, 13.50000000000000000 ) ) ;
#154=DIRECTION ( 'NONE',  ( -1.000000000000000000, 0.000000000000000000, -0.000000000000000000 ) ) ;
#158=DIRECTION ( 'NONE',  ( 1.000000000000000000, 0.000000000000000000, 0.000000000000000000 ) ) ;
#161=ORIENTED_EDGE ( 'NONE', *, *, #17115, .T. ) ;
#162=CIRCLE ( 'NONE', #17316, 2.500000000000002220 ) ;
#163=ORIENTED_EDGE ( 'NONE', *, *, #4099, .F. ) ;
#165=EDGE_CURVE ( 'NONE', #17, #1178, #11385, .T. ) ;
#167=ORIENTED_EDGE ( 'NONE', *, *, #3663, .F. ) ;
#168=CARTESIAN_POINT ( 'NONE',  ( -27.37540678000427619, 7.754037881813018962E-15, 42.50000000000000000 ) ) ;
#169=EDGE_CURVE ( 'NONE', #2258, #13733, #12053, .T. ) ;
#170=VERTEX_POINT ( 'NONE', #9480 ) ;
#175=CARTESIAN_POINT ( 'NONE',  ( 30.37540678000427619, 63.74634676501045050, 3.799999999999999822 ) ) ;
#176=AXIS2_PLACEMENT_3D ( 'NONE', #3775, #19006, #19330 ) ;
#178=ORIENTED_EDGE ( 'NONE', *, *, #14383, .T. ) ;
#179=CARTESIAN_POINT ( 'NONE',  ( 23.02398829872513986, 3.528912754968628551, 13.50000000000000178 ) ) ;
#182=FACE_OUTER_BOUND ( 'NONE', #18592, .T. ) ;
#186=VECTOR ( 'NONE', #8638, 1000.000000000000000 ) ;
#188=ADVANCED_FACE ( 'NONE', ( #6511 ), #8182, .T. ) ;
#191=EDGE_LOOP ( 'NONE', ( #16439, #11802, #15937, #11017 ) ) ;
#193=VECTOR ( 'NONE', #20461, 1000.000000000000000 ) ;
#194=EDGE_LOOP ( 'NONE', ( #10664, #7894, #6707, #20696 ) ) ;
#195=EDGE_CURVE ( 'NONE', #11031, #19749, #18677, .T. ) ;
#197=DIRECTION ( 'NONE',  ( 1.000000000000000000, 0.000000000000000000, 0.000000000000000000 ) ) ;
#198=EDGE_CURVE ( 'NONE', #14667, #21935, #6366, .T. ) ;
#199=VECTOR ( 'NONE', #1261, 1000.000000000000000 ) ;
#207=VECTOR ( 'NONE', #21201, 1000.000000000000000 ) ;
#212=FACE_OUTER_BOUND ( 'NONE', #3377, .T. ) ;
#213=DIRECTION ( 'NONE',  ( -1.000000000000000000, 0.000000000000000000, 0.000000000000000000 ) ) ;
#214=AXIS2_PLACEMENT_3D ( 'NONE', #8138, #16842, #6580 ) ;
#215=DIRECTION ( 'NONE',  ( 0.000000000000000000, 0.000000000000000000, -1.000000000000000000 ) ) ;
#219=DIRECTION ( 'NONE',  ( 0.000000000000000000, 0.000000000000000000, -1.000000000000000000 ) ) ;
#220=EDGE_LOOP ( 'NONE', ( #1787, #8382, #3209, #12139 ) ) ;
#221=VECTOR ( 'NONE', #7639, 1000.000000000000000 ) ;
#222=CARTESIAN_POINT ( 'NONE',  ( 23.02398829872514341, -2.157133568460918305, 13.19999999999998685 ) ) ;
#223=ORIENTED_EDGE ( 'NONE', *, *, #5319, .F. ) ;
#224=EDGE_CURVE ( 'NONE', #11867, #21299, #18788, .T. ) ;
#225=VERTEX_POINT ( 'NONE', #16772 ) ;
#227=CYLINDRICAL_SURFACE ( 'NONE', #2701, 0.2999999999999999334 ) ;
#229=FACE_OUTER_BOUND ( 'NONE', #21241, .T. ) ;
#230=CIRCLE ( 'NONE', #5974, 0.2500000000000002220 ) ;
#233=CARTESIAN_POINT ( 'NONE',  ( -25.37540678000427263, 63.74634676501045050, 7.500000000000000000 ) ) ;
#238=CARTESIAN_POINT ( 'NONE',  ( 23.05541308335691042, -2.330322924046650535, 13.28711303755810214 ) ) ;
#239=DIRECTION ( 'NONE',  ( -1.000000000000000000, -0.000000000000000000, -0.000000000000000000 ) ) ;
#242=ORIENTED_EDGE ( 'NONE', *, *, #2603, .F. ) ;
#246=CARTESIAN_POINT ( 'NONE',  ( -9.141460742840918030, 32.61873716947361856, 68.00000000000000000 ) ) ;
#247=EDGE_CURVE ( 'NONE', #13036, #14518, #16350, .T. ) ;
#250=EDGE_CURVE ( 'NONE', #1621, #2258, #12761, .T. ) ;
#251=VECTOR ( 'NONE', #6061, 1000.000000000000000 ) ;
#252=VERTEX_POINT ( 'NONE', #14865 ) ;
#254=AXIS2_PLACEMENT_3D ( 'NONE', #1378, #3292, #10118 ) ;
#256=DIRECTION ( 'NONE',  ( 0.000000000000000000, 0.000000000000000000, 1.000000000000000000 ) ) ;
#257=LINE ( 'NONE', #20968, #15223 ) ;
#260=DIRECTION ( 'NONE',  ( 0.000000000000000000, 1.000000000000000000, 0.000000000000000000 ) ) ;
#261=DIRECTION ( 'NONE',  ( 0.000000000000000000, 0.000000000000000000, 1.000000000000000000 ) ) ;
#262=CARTESIAN_POINT ( 'NONE',  ( -29.50000000000002132, 2.473451120191013430, 0.2999999999999947153 ) ) ;
#265=VECTOR ( 'NONE', #8153, 1000.000000000000000 ) ;
#266=CIRCLE ( 'NONE', #7796, 0.5000000000000004441 ) ;
#267=CARTESIAN_POINT ( 'NONE',  ( 8.641460742840918030, -33.93424481021354921, 68.50000000000000000 ) ) ;
#270=AXIS2_PLACEMENT_3D ( 'NONE', #2660, #4352, #7834 ) ;
#275=EDGE_LOOP ( 'NONE', ( #21466, #6868, #2704, #15839 ) ) ;
#276=CARTESIAN_POINT ( 'NONE',  ( -30.37540678000427619, 63.74634676501045050, 7.200000000000000178 ) ) ;
#279=DIRECTION ( 'NONE',  ( 0.000000000000000000, 0.000000000000000000, -1.000000000000000000 ) ) ;
#281=FACE_OUTER_BOUND ( 'NONE', #19070, .T. ) ;
#282=ORIENTED_EDGE ( 'NONE', *, *, #19222, .F. ) ;
#285=VECTOR ( 'NONE', #15351, 1000.000000000000000 ) ;
#287=CARTESIAN_POINT ( 'NONE',  ( -25.37540678000427263, 67.24634676501045760, 13.19999999999999929 ) ) ;
#290=DIRECTION ( 'NONE',  ( -0.000000000000000000, -1.000000000000000000, -0.000000000000000000 ) ) ;
#291=AXIS2_PLACEMENT_3D ( 'NONE', #3039, #1688, #20501 ) ;
#293=ORIENTED_EDGE ( 'NONE', *, *, #21149, .F. ) ;
#294=CARTESIAN_POINT ( 'NONE',  ( 23.02398829872513986, 2.191402100636968608, 13.32997043993373154 ) ) ;
#297=DIRECTION ( 'NONE',  ( -0.000000000000000000, 0.000000000000000000, 1.000000000000000000 ) ) ;
#298=PLANE ( 'NONE',  #15665 ) ;
#300=ADVANCED_FACE ( 'NONE', ( #11737 ), #986, .T. ) ;
#301=ORIENTED_EDGE ( 'NONE', *, *, #4018, .F. ) ;
#303=CARTESIAN_POINT ( 'NONE',  ( 27.67540678000428045, 7.839012376739720627E-15, 13.79999999999999893 ) ) ;
#304=TOROIDAL_SURFACE ( 'NONE', #8184, 5.300000000000004263, 0.2999999999999999889 ) ;
#307=EDGE_CURVE ( 'NONE', #20337, #8429, #10176, .T. ) ;
#308=EDGE_CURVE ( 'NONE', #12411, #15111, #14209, .T. ) ;
#309=DIRECTION ( 'NONE',  ( -1.000000000000000000, -0.000000000000000000, -0.000000000000000000 ) ) ;
#310=AXIS2_PLACEMENT_3D ( 'NONE', #370, #14021, #12447 ) ;
#315=DIRECTION ( 'NONE',  ( 1.000000000000000000, 0.000000000000000000, 0.000000000000000000 ) ) ;
#316=DIRECTION ( 'NONE',  ( 0.000000000000000000, 1.000000000000000000, 0.000000000000000000 ) ) ;
#320=AXIS2_PLACEMENT_3D ( 'NONE', #10464, #1935, #8778 ) ;
#321=FACE_OUTER_BOUND ( 'NONE', #6015, .T. ) ;
#322=ORIENTED_EDGE ( 'NONE', *, *, #5171, .T. ) ;
#323=CARTESIAN_POINT ( 'NONE',  ( -17.92752199202933738, 38.74634676501045760, 13.62426406871192874 ) ) ;
#325=CYLINDRICAL_SURFACE ( 'NONE', #22147, 0.2999999999999999334 ) ;
#326=CARTESIAN_POINT ( 'NONE',  ( 0.000000000000000000, 51.61873716947361856, 14.00000000000000000 ) ) ;
#327=ORIENTED_EDGE ( 'NONE', *, *, #5171, .F. ) ;
#328=EDGE_CURVE ( 'NONE', #620, #12977, #10161, .T. ) ;
#330=CARTESIAN_POINT ( 'NONE',  ( -14.66895121610833463, 51.92349730072803027, 13.50000000000000000 ) ) ;
#332=EDGE_LOOP ( 'NONE', ( #15947, #21417, #21604, #10884 ) ) ;
#333=ORIENTED_EDGE ( 'NONE', *, *, #12972, .T. ) ;
#334=DIRECTION ( 'NONE',  ( 0.000000000000000000, 0.000000000000000000, 1.000000000000000000 ) ) ;
#335=ADVANCED_FACE ( 'NONE', ( #13732 ), #17952, .T. ) ;
#337=ORIENTED_EDGE ( 'NONE', *, *, #19898, .F. ) ;
#339=TOROIDAL_SURFACE ( 'NONE', #15345, 1.500000000000000000, 0.5000000000000000000 ) ;
#340=CARTESIAN_POINT ( 'NONE',  ( 23.02398829872513986, -2.501891433835003564, 13.57888791970315445 ) ) ;
#345=EDGE_CURVE ( 'NONE', #6305, #10550, #10954, .T. ) ;
#347=DIRECTION ( 'NONE',  ( 0.000000000000000000, 0.000000000000000000, 1.000000000000000000 ) ) ;
#352=LINE ( 'NONE', #21076, #2928 ) ;
#357=EDGE_LOOP ( 'NONE', ( #11362, #10177, #13871 ) ) ;
#358=ORIENTED_EDGE ( 'NONE', *, *, #14725, .T. ) ;
#359=CYLINDRICAL_SURFACE ( 'NONE', #18503, 0.2999999999999999334 ) ;
#360=EDGE_CURVE ( 'NONE', #21866, #13036, #8625, .T. ) ;
#361=LINE ( 'NONE', #5531, #13170 ) ;
#362=EDGE_LOOP ( 'NONE', ( #19566, #18335, #18750, #10632, #13457, #9597 ) ) ;
#363=ORIENTED_EDGE ( 'NONE', *, *, #6744, .T. ) ;
#365=CIRCLE ( 'NONE', #11086, 0.2500000000000002220 ) ;
#370=CARTESIAN_POINT ( 'NONE',  ( 0.000000000000000000, -67.24634676501045760, 13.50000000000000000 ) ) ;
#371=EDGE_CURVE ( 'NONE', #1033, #17036, #14160, .T. ) ;
#372=DIRECTION ( 'NONE',  ( 1.000000000000000000, 0.000000000000000000, 0.000000000000000000 ) ) ;
#373=CARTESIAN_POINT ( 'NONE',  ( -18.22752199202934520, 50.11873716947361856, 13.79999999999999716 ) ) ;
#376=ORIENTED_EDGE ( 'NONE', *, *, #12243, .F. ) ;
#378=AXIS2_PLACEMENT_3D ( 'NONE', #16998, #14999, #20380 ) ;
#380=CARTESIAN_POINT ( 'NONE',  ( 9.641460742840918030, 32.93424481021354921, 68.00000000000000000 ) ) ;
#382=EDGE_LOOP ( 'NONE', ( #7646, #514, #20961, #15975, #3152, #9896 ) ) ;
#383=ORIENTED_EDGE ( 'NONE', *, *, #4666, .T. ) ;
#384=CARTESIAN_POINT ( 'NONE',  ( 27.77120804565216261, -2.094189496455383548, 0.2207451490129595517 ) ) ;
#385=CARTESIAN_POINT ( 'NONE',  ( 3.627054932750481964, 32.61873716947361856, 42.50000000000000000 ) ) ;
#386=EDGE_CURVE ( 'NONE', #4334, #5485, #19645, .T. ) ;
#387=DIRECTION ( 'NONE',  ( 1.000000000000000000, 0.000000000000000000, 0.000000000000000000 ) ) ;
#388=DIRECTION ( 'NONE',  ( 0.000000000000000000, 0.000000000000000000, -1.000000000000000000 ) ) ;
#389=CIRCLE ( 'NONE', #16102, 1.999999999999991340 ) ;
#391=CYLINDRICAL_SURFACE ( 'NONE', #20736, 1.999999999999991340 ) ;
#393=DIRECTION ( 'NONE',  ( 1.000000000000000000, 0.000000000000000000, 0.000000000000000000 ) ) ;
#394=CIRCLE ( 'NONE', #4286, 0.6999999999999992895 ) ;
#396=CARTESIAN_POINT ( 'NONE',  ( -14.96174975910705207, 42.31054587065082728, 68.25000000000000000 ) ) ;
#397=FACE_OUTER_BOUND ( 'NONE', #15118, .T. ) ;
#399=CARTESIAN_POINT ( 'NONE',  ( -15.95292532278785913, 52.39333383871510108, 13.50000000000000000 ) ) ;
#401=EDGE_CURVE ( 'NONE', #12977, #16033, #17843, .T. ) ;
#402=AXIS2_PLACEMENT_3D ( 'NONE', #9005, #19499, #9104 ) ;
#403=FACE_OUTER_BOUND ( 'NONE', #18761, .T. ) ;
#404=DIRECTION ( 'NONE',  ( -1.000000000000000000, 0.000000000000000000, 0.000000000000000000 ) ) ;
#406=EDGE_CURVE ( 'NONE', #16245, #2755, #5261, .T. ) ;
#408=ORIENTED_EDGE ( 'NONE', *, *, #2837, .F. ) ;
#409=CARTESIAN_POINT ( 'NONE',  ( -14.96174975910705207, -32.10873716947361345, 13.79999999999999893 ) ) ;
#410=VECTOR ( 'NONE', #12305, 1000.000000000000000 ) ;
#414=CARTESIAN_POINT ( 'NONE',  ( -29.13662752439705272, -4.700000000000000178, 3.500000000000000000 ) ) ;
#415=ORIENTED_EDGE ( 'NONE', *, *, #1690, .T. ) ;
#418=CIRCLE ( 'NONE', #10089, 0.5000000000000004441 ) ;
#421=VERTEX_POINT ( 'NONE', #14147 ) ;
#423=CARTESIAN_POINT ( 'NONE',  ( -30.37540678000427619, 6.000000000000000000, 3.799999999999999822 ) ) ;
#424=CARTESIAN_POINT ( 'NONE',  ( -25.37540678000427263, -63.74634676501045050, 7.799999999999999822 ) ) ;
#428=CARTESIAN_POINT ( 'NONE',  ( 29.20000000000002061, 2.848961824869257864, 0.000000000000000000 ) ) ;
#429=DIRECTION ( 'NONE',  ( 0.000000000000000000, 1.000000000000000000, 0.000000000000000000 ) ) ;
#430=DIRECTION ( 'NONE',  ( 1.000000000000000000, 0.000000000000000000, 0.000000000000000000 ) ) ;
#433=CYLINDRICAL_SURFACE ( 'NONE', #8151, 6.500000000000002665 ) ;
#441=ORIENTED_EDGE ( 'NONE', *, *, #14416, .T. ) ;
#442=AXIS2_PLACEMENT_3D ( 'NONE', #12633, #1915, #14875 ) ;
#443=CARTESIAN_POINT ( 'NONE',  ( 23.02398829872514341, -3.052854503364608618, 13.54964687161601056 ) ) ;
#444=VERTEX_POINT ( 'NONE', #17730 ) ;
#446=EDGE_CURVE ( 'NONE', #22135, #12543, #4899, .T. ) ;
#447=DIRECTION ( 'NONE',  ( 0.000000000000000000, 0.000000000000000000, -1.000000000000000000 ) ) ;
#449=CYLINDRICAL_SURFACE ( 'NONE', #22037, 2.500000000000002220 ) ;
#451=DIRECTION ( 'NONE',  ( 1.000000000000000000, 0.000000000000000000, 0.000000000000000000 ) ) ;
#454=CARTESIAN_POINT ( 'NONE',  ( -23.02398829872513986, 2.333487117377073705, 13.47150829744944467 ) ) ;
#455=CARTESIAN_POINT ( 'NONE',  ( -29.20000000000002061, 2.799282752659324025, 0.000000000000000000 ) ) ;
#457=FACE_OUTER_BOUND ( 'NONE', #9813, .T. ) ;
#458=CARTESIAN_POINT ( 'NONE',  ( -14.96174975910694016, -51.80670431852976776, 13.81236938792817348 ) ) ;
#459=ORIENTED_EDGE ( 'NONE', *, *, #7526, .F. ) ;
#470=LINE ( 'NONE', #9099, #3807 ) ;
#472=LINE ( 'NONE', #17497, #11782 ) ;
#473=EDGE_CURVE ( 'NONE', #5001, #15844, #1385, .T. ) ;
#475=DIRECTION ( 'NONE',  ( -2.832483164223434527E-16, -1.000000000000000000, -0.000000000000000000 ) ) ;
#476=DIRECTION ( 'NONE',  ( -0.000000000000000000, 0.000000000000000000, 1.000000000000000000 ) ) ;
#477=DIRECTION ( 'NONE',  ( 0.000000000000000000, 0.000000000000000000, 1.000000000000000000 ) ) ;
#481=DIRECTION ( 'NONE',  ( 1.000000000000000000, 0.000000000000000000, 0.000000000000000000 ) ) ;
#483=VERTEX_POINT ( 'NONE', #9903 ) ;
#484=ORIENTED_EDGE ( 'NONE', *, *, #16147, .T. ) ;
#486=CARTESIAN_POINT ( 'NONE',  ( -15.95292532278785913, -50.11873716947361856, 13.79999999999999893 ) ) ;
#487=EDGE_CURVE ( 'NONE', #17808, #7580, #5613, .T. ) ;
#489=CIRCLE ( 'NONE', #16201, 0.2999999999999999334 ) ;
#493=EDGE_CURVE ( 'NONE', #9687, #4677, #1266, .T. ) ;
#497=VERTEX_POINT ( 'NONE', #9793 ) ;
#498=LINE ( 'NONE', #17731, #18144 ) ;
#500=CARTESIAN_POINT ( 'NONE',  ( 0.000000000000000000, 66.94634676501046044, 13.19999999999999929 ) ) ;
#501=LINE ( 'NONE', #14375, #6304 ) ;
#502=EDGE_LOOP ( 'NONE', ( #20106, #3281, #5812, #15625 ) ) ;
#504=EDGE_CURVE ( 'NONE', #14858, #20195, #8459, .T. ) ;
#505=CARTESIAN_POINT ( 'NONE',  ( 15.95292532278785913, 32.61873716947361856, 68.50000000000000000 ) ) ;
#506=CYLINDRICAL_SURFACE ( 'NONE', #10149, 1.000000000000000888 ) ;
#507=ORIENTED_EDGE ( 'NONE', *, *, #21987, .T. ) ;
#508=DIRECTION ( 'NONE',  ( -1.000000000000000000, 0.000000000000000000, 0.000000000000000000 ) ) ;
#510=ORIENTED_EDGE ( 'NONE', *, *, #2837, .T. ) ;
#512=CARTESIAN_POINT ( 'NONE',  ( -29.37540678000427619, 5.000000000000000000, 7.500000000000000000 ) ) ;
#514=ORIENTED_EDGE ( 'NONE', *, *, #7199, .T. ) ;
#516=EDGE_LOOP ( 'NONE', ( #2065, #11314, #11936, #11078 ) ) ;
#517=EDGE_CURVE ( 'NONE', #5434, #19294, #22048, .T. ) ;
#519=ORIENTED_EDGE ( 'NONE', *, *, #1419, .T. ) ;
#521=VECTOR ( 'NONE', #11856, 1000.000000000000000 ) ;
#522=STYLED_ITEM ( 'NONE', ( #4431 ), #6179 ) ;
#523=EDGE_LOOP ( 'NONE', ( #14955, #10482, #2541, #6131 ) ) ;
#526=DIRECTION ( 'NONE',  ( 1.000000000000000000, 0.000000000000000000, 0.000000000000000000 ) ) ;
#527=ORIENTED_EDGE ( 'NONE', *, *, #6447, .T. ) ;
#528=CARTESIAN_POINT ( 'NONE',  ( 15.95292532278785913, 50.11873716947361856, 13.79999999999999893 ) ) ;
#530=CARTESIAN_POINT ( 'NONE',  ( -15.95292532278785913, -50.11873716947361856, 13.87499999999999822 ) ) ;
#536=ORIENTED_EDGE ( 'NONE', *, *, #2118, .T. ) ;
#539=B_SPLINE_CURVE_WITH_KNOTS ( 'NONE', 3,
 ( #19419, #21120, #4092, #10588, #15827, #20784, #10909, #10708 ),
 .UNSPECIFIED., .F., .F.,
 ( 4, 2, 2, 4 ),
 ( -3.470042892451968281E-06, 0.0002769752510348927397, 0.0004171978979985645165, 0.0005574205449622362391 ),
 .UNSPECIFIED. ) ;
#551=AXIS2_PLACEMENT_3D ( 'NONE', #18040, #2721, #16137 ) ;
#553=AXIS2_PLACEMENT_3D ( 'NONE', #13252, #944, #14600 ) ;
#554=ORIENTED_EDGE ( 'NONE', *, *, #18237, .T. ) ;
#556=CYLINDRICAL_SURFACE ( 'NONE', #14490, 0.5000000000000004441 ) ;
#557=DIRECTION ( 'NONE',  ( 1.000000000000000000, 0.000000000000000000, 0.000000000000000000 ) ) ;
#558=DIRECTION ( 'NONE',  ( 0.000000000000000000, 0.000000000000000000, 1.000000000000000000 ) ) ;
#559=CARTESIAN_POINT ( 'NONE',  ( -25.37540678000427263, 66.94634676501046044, 13.19999999999999929 ) ) ;
#562=DIRECTION ( 'NONE',  ( 1.000000000000000000, 0.000000000000000000, 0.000000000000000000 ) ) ;
#563=DIRECTION ( 'NONE',  ( 1.000000000000000000, 0.000000000000000000, 0.000000000000000000 ) ) ;
#565=VECTOR ( 'NONE', #5582, 1000.000000000000000 ) ;
#567=VECTOR ( 'NONE', #12317, 1000.000000000000000 ) ;
#568=EDGE_LOOP ( 'NONE', ( #14082, #870, #8986, #11798 ) ) ;
#569=LINE ( 'NONE', #7425, #20682 ) ;
#570=EDGE_CURVE ( 'NONE', #6397, #9425, #13802, .T. ) ;
#574=ORIENTED_EDGE ( 'NONE', *, *, #17986, .F. ) ;
#575=AXIS2_PLACEMENT_3D ( 'NONE', #5688, #15432, #10907 ) ;
#578=AXIS2_PLACEMENT_3D ( 'NONE', #18424, #18545, #13175 ) ;
#580=B_SPLINE_CURVE_WITH_KNOTS ( 'NONE', 3,
 ( #18832, #1823, #2030, #3723, #8551, #15360, #33, #7097 ),
 .UNSPECIFIED., .F., .F.,
 ( 4, 2, 2, 4 ),
 ( 0.000000000000000000, 0.0004639257417130339422, 0.0006958886125695525667, 0.0009278514834260711370 ),
 .UNSPECIFIED. ) ;
#581=LINE ( 'NONE', #9211, #6671 ) ;
#582=CIRCLE ( 'NONE', #10948, 1.000000000000000888 ) ;
#585=CARTESIAN_POINT ( 'NONE',  ( -24.13662752439704917, 0.000000000000000000, 7.200000000000000178 ) ) ;
#586=EDGE_CURVE ( 'NONE', #8695, #13748, #1302, .T. ) ;
#589=CARTESIAN_POINT ( 'NONE',  ( -26.63662752439704917, -3.061616997868386099E-16, 0.3000000000000016542 ) ) ;
#590=DIRECTION ( 'NONE',  ( 0.000000000000000000, -1.000000000000000000, 0.000000000000000000 ) ) ;
#591=ORIENTED_EDGE ( 'NONE', *, *, #17666, .T. ) ;
#592=DIRECTION ( 'NONE',  ( 2.832483164223434527E-16, 1.000000000000000000, -0.000000000000000000 ) ) ;
#593=VECTOR ( 'NONE', #8543, 1000.000000000000000 ) ;
#594=DIRECTION ( 'NONE',  ( 0.000000000000000000, -1.000000000000000000, 0.000000000000000000 ) ) ;
#597=AXIS2_PLACEMENT_3D ( 'NONE', #9978, #8302, #13745 ) ;
#598=EDGE_LOOP ( 'NONE', ( #10735, #2509, #14989, #19917 ) ) ;
#599=ORIENTED_EDGE ( 'NONE', *, *, #18143, .F. ) ;
#600=DIRECTION ( 'NONE',  ( 0.000000000000000000, 0.000000000000000000, -1.000000000000000000 ) ) ;
#602=DIRECTION ( 'NONE',  ( 0.000000000000000000, 0.000000000000000000, -1.000000000000000000 ) ) ;
#606=EDGE_CURVE ( 'NONE', #8611, #22039, #230, .T. ) ;
#610=ORIENTED_EDGE ( 'NONE', *, *, #14343, .T. ) ;
#611=CARTESIAN_POINT ( 'NONE',  ( 0.000000000000000000, 32.61873716947361856, 68.00000000000000000 ) ) ;
#613=ORIENTED_EDGE ( 'NONE', *, *, #21858, .F. ) ;
#614=LINE ( 'NONE', #9243, #11724 ) ;
#617=AXIS2_PLACEMENT_3D ( 'NONE', #8740, #3596, #15537 ) ;
#618=CARTESIAN_POINT ( 'NONE',  ( 23.02398829872514696, 2.191346223869591991, 13.32987162994455232 ) ) ;
#620=VERTEX_POINT ( 'NONE', #10019 ) ;
#621=CARTESIAN_POINT ( 'NONE',  ( -18.22752199202934520, -50.11873716947361856, 13.50000000000000000 ) ) ;
#622=DIRECTION ( 'NONE',  ( 0.000000000000000000, 0.000000000000000000, 1.000000000000000000 ) ) ;
#624=AXIS2_PLACEMENT_3D ( 'NONE', #6692, #5459, #388 ) ;
#625=DIRECTION ( 'NONE',  ( -0.000000000000000000, 1.000000000000000000, -0.000000000000000000 ) ) ;
#626=DIRECTION ( 'NONE',  ( 0.000000000000000000, 0.000000000000000000, -1.000000000000000000 ) ) ;
#628=CIRCLE ( 'NONE', #254, 0.4999999999999995559 ) ;
#630=VERTEX_POINT ( 'NONE', #21990 ) ;
#631=DIRECTION ( 'NONE',  ( 0.000000000000000000, 0.000000000000000000, -1.000000000000000000 ) ) ;
#635=DIRECTION ( 'NONE',  ( 0.000000000000000000, 0.000000000000000000, 1.000000000000000000 ) ) ;
#637=EDGE_CURVE ( 'NONE', #19547, #1107, #20309, .T. ) ;
#638=AXIS2_PLACEMENT_3D ( 'NONE', #14469, #4417, #16496 ) ;
#639=ORIENTED_EDGE ( 'NONE', *, *, #308, .T. ) ;
#640=EDGE_CURVE ( 'NONE', #10963, #16873, #16824, .T. ) ;
#641=ORIENTED_EDGE ( 'NONE', *, *, #21556, .F. ) ;
#647=CARTESIAN_POINT ( 'NONE',  ( 4.127054932750481520, -33.93424481021354921, 68.00000000000000000 ) ) ;
#649=CARTESIAN_POINT ( 'NONE',  ( 0.000000000000000000, 38.74634676501045760, 42.50000000000000000 ) ) ;
#651=AXIS2_PLACEMENT_3D ( 'NONE', #13561, #15460, #1364 ) ;
#654=EDGE_CURVE ( 'NONE', #20195, #15586, #1602, .T. ) ;
#655=CARTESIAN_POINT ( 'NONE',  ( -29.13662752439705272, 0.000000000000000000, 7.500000000000000000 ) ) ;
#658=LINE ( 'NONE', #8737, #3312 ) ;
#660=CIRCLE ( 'NONE', #16380, 0.2999999999999999334 ) ;
#663=ORIENTED_EDGE ( 'NONE', *, *, #13368, .F. ) ;
#664=EDGE_LOOP ( 'NONE', ( #2962, #17686, #15766, #12256 ) ) ;
#665=ORIENTED_EDGE ( 'NONE', *, *, #14831, .T. ) ;
#666=DIRECTION ( 'NONE',  ( 1.000000000000000000, 0.000000000000000000, -0.000000000000000000 ) ) ;
#667=ADVANCED_FACE ( 'NONE', ( #6666 ), #8444, .T. ) ;
#669=EDGE_LOOP ( 'NONE', ( #7518, #13127, #6320, #178 ) ) ;
#670=CIRCLE ( 'NONE', #3550, 0.5000000000000004441 ) ;
#672=ORIENTED_EDGE ( 'NONE', *, *, #21439, .F. ) ;
#678=FACE_OUTER_BOUND ( 'NONE', #14910, .T. ) ;
#679=CARTESIAN_POINT ( 'NONE',  ( 23.32398829872514057, 7.118794219358020148E-15, 13.79999999999999893 ) ) ;
#680=EDGE_CURVE ( 'NONE', #13756, #9842, #19639, .T. ) ;
#681=CARTESIAN_POINT ( 'NONE',  ( -23.02398829872514341, 2.681487294389183429, 13.50129116665769757 ) ) ;
#682=DIRECTION ( 'NONE',  ( 0.000000000000000000, -0.000000000000000000, 1.000000000000000000 ) ) ;
#684=DIRECTION ( 'NONE',  ( -0.000000000000000000, -1.000000000000000000, -0.000000000000000000 ) ) ;
#690=ORIENTED_EDGE ( 'NONE', *, *, #5227, .F. ) ;
#691=ORIENTED_EDGE ( 'NONE', *, *, #15476, .T. ) ;
#694=DIRECTION ( 'NONE',  ( 0.000000000000000000, 0.000000000000000000, -1.000000000000000000 ) ) ;
#695=TOROIDAL_SURFACE ( 'NONE', #9998, 4.051418481279135619, 0.2999999999999999889 ) ;
#696=VECTOR ( 'NONE', #15399, 1000.000000000000000 ) ;
#699=CARTESIAN_POINT ( 'NONE',  ( 3.627054932750481964, 32.93424481021354921, 68.50000000000000000 ) ) ;
#700=EDGE_CURVE ( 'NONE', #630, #4674, #21089, .T. ) ;
#702=CARTESIAN_POINT ( 'NONE',  ( 18.22752199202934520, -50.11873716947361856, 13.79999999999999716 ) ) ;
#703=CARTESIAN_POINT ( 'NONE',  ( -29.37540678000427619, -4.700000000000000178, 3.500000000000000000 ) ) ;
#704=CARTESIAN_POINT ( 'NONE',  ( 15.95292532278785913, -52.11873716947361856, 13.99999999999999822 ) ) ;
#705=CARTESIAN_POINT ( 'NONE',  ( -23.02398829872513630, 2.192334671524719170, 13.33121981694520741 ) ) ;
#706=VERTEX_POINT ( 'NONE', #18916 ) ;
#707=CARTESIAN_POINT ( 'NONE',  ( -25.37540678000427263, 63.74634676501045050, 7.200000000000000178 ) ) ;
#711=ORIENTED_EDGE ( 'NONE', *, *, #13546, .F. ) ;
#712=VERTEX_POINT ( 'NONE', #3588 ) ;
#716=ORIENTED_EDGE ( 'NONE', *, *, #14040, .T. ) ;
#717=VECTOR ( 'NONE', #8892, 1000.000000000000000 ) ;
#719=ADVANCED_FACE ( 'NONE', ( #14628 ), #754, .T. ) ;
#723=DIRECTION ( 'NONE',  ( 0.000000000000000000, 0.000000000000000000, 1.000000000000000000 ) ) ;
#724=DIRECTION ( 'NONE',  ( -0.000000000000000000, -0.000000000000000000, -1.000000000000000000 ) ) ;
#725=CARTESIAN_POINT ( 'NONE',  ( 29.37540678000427619, 4.700000000000000178, 3.799999999999999822 ) ) ;
#726=CARTESIAN_POINT ( 'NONE',  ( 23.02398829872513986, 7.027230193580998154E-15, 42.50000000000000000 ) ) ;
#732=AXIS2_PLACEMENT_3D ( 'NONE', #11982, #10438, #13447 ) ;
#734=CYLINDRICAL_SURFACE ( 'NONE', #12273, 0.5000000000000004441 ) ;
#737=FILL_AREA_STYLE_COLOUR ( '', #2686 ) ;
#744=LINE ( 'NONE', #9713, #19223 ) ;
#745=DIRECTION ( 'NONE',  ( -0.000000000000000000, -1.000000000000000000, -0.000000000000000000 ) ) ;
#749=CIRCLE ( 'NONE', #378, 0.2500000000000002220 ) ;
#751=CARTESIAN_POINT ( 'NONE',  ( -18.22752199202934520, 50.11873716947361856, 13.79999999999999716 ) ) ;
#752=AXIS2_PLACEMENT_3D ( 'NONE', #5771, #14246, #10791 ) ;
#753=AXIS2_PLACEMENT_3D ( 'NONE', #12913, #9578, #1063 ) ;
#754=PLANE ( 'NONE',  #8215 ) ;
#755=CARTESIAN_POINT ( 'NONE',  ( -23.02398829872513986, 2.157133568460765538, 13.19999999999999929 ) ) ;
#761=DIRECTION ( 'NONE',  ( -1.000000000000000000, 0.000000000000000000, 0.000000000000000000 ) ) ;
#762=DIRECTION ( 'NONE',  ( 0.000000000000000000, 0.000000000000000000, 1.000000000000000000 ) ) ;
#763=EDGE_LOOP ( 'NONE', ( #11586, #167, #21202, #9598 ) ) ;
#765=EDGE_CURVE ( 'NONE', #16245, #21932, #11058, .T. ) ;
#767=CARTESIAN_POINT ( 'NONE',  ( -25.37540678000429040, -36.74634676501047181, 42.50000000000000000 ) ) ;
#769=FACE_OUTER_BOUND ( 'NONE', #17919, .T. ) ;
#770=ORIENTED_EDGE ( 'NONE', *, *, #13810, .F. ) ;
#772=ORIENTED_EDGE ( 'NONE', *, *, #10656, .F. ) ;
#777=CIRCLE ( 'NONE', #15079, 0.2999999999999999334 ) ;
#778=AXIS2_PLACEMENT_3D ( 'NONE', #8553, #15361, #136 ) ;
#780=VECTOR ( 'NONE', #12733, 1000.000000000000000 ) ;
#787=DIRECTION ( 'NONE',  ( 1.000000000000000000, 0.000000000000000000, 0.000000000000000000 ) ) ;
#788=DIRECTION ( 'NONE',  ( 0.000000000000000000, 0.000000000000000000, 1.000000000000000000 ) ) ;
#790=ADVANCED_FACE ( 'NONE', ( #7940 ), #18215, .T. ) ;
#792=DIRECTION ( 'NONE',  ( 1.000000000000000000, 0.000000000000000000, 0.000000000000000000 ) ) ;
#795=FACE_OUTER_BOUND ( 'NONE', #2508, .T. ) ;
#796=DIRECTION ( 'NONE',  ( 0.000000000000000000, -0.000000000000000000, -1.000000000000000000 ) ) ;
#797=PLANE ( 'NONE',  #6379 ) ;
#801=AXIS2_PLACEMENT_3D ( 'NONE', #4744, #14793, #5982 ) ;
#805=EDGE_CURVE ( 'NONE', #11236, #19185, #21443, .T. ) ;
#806=FACE_OUTER_BOUND ( 'NONE', #2034, .T. ) ;
#808=VERTEX_POINT ( 'NONE', #9483 ) ;
#809=FACE_BOUND ( 'NONE', #18279, .T. ) ;
#811=CARTESIAN_POINT ( 'NONE',  ( -28.57540678000427548, 6.776800961815481195, 13.50000000000000000 ) ) ;
#817=CARTESIAN_POINT ( 'NONE',  ( -15.95292532278785913, 50.11873716947361856, 13.79999999999999893 ) ) ;
#821=DIRECTION ( 'NONE',  ( -1.000000000000000000, -0.000000000000000000, -0.000000000000000000 ) ) ;
#827=CARTESIAN_POINT ( 'NONE',  ( -29.37540678000427619, -5.000000000000000000, 7.500000000000000000 ) ) ;
#828=DIRECTION ( 'NONE',  ( -0.000000000000000000, -1.000000000000000000, -0.000000000000000000 ) ) ;
#829=CARTESIAN_POINT ( 'NONE',  ( 23.02398829872513630, -2.333754220862764406, 13.47170153661532943 ) ) ;
#830=DIRECTION ( 'NONE',  ( 0.000000000000000000, 0.000000000000000000, 1.000000000000000000 ) ) ;
#834=LINE ( 'NONE', #19652, #7743 ) ;
#839=ORIENTED_EDGE ( 'NONE', *, *, #12806, .T. ) ;
#840=CYLINDRICAL_SURFACE ( 'NONE', #19835, 0.3000000000000003775 ) ;
#841=LINE ( 'NONE', #21347, #8216 ) ;
#842=EDGE_CURVE ( 'NONE', #17942, #4860, #4449, .T. ) ;
#844=DIRECTION ( 'NONE',  ( 1.000000000000000000, 0.000000000000000000, 0.000000000000000000 ) ) ;
#845=AXIS2_PLACEMENT_3D ( 'NONE', #11623, #22060, #18688 ) ;
#850=FACE_OUTER_BOUND ( 'NONE', #16602, .T. ) ;
#851=PLANE ( 'NONE',  #1729 ) ;
#852=VERTEX_POINT ( 'NONE', #19905 ) ;
#855=EDGE_LOOP ( 'NONE', ( #21772, #772, #17828, #9443 ) ) ;
#860=DIRECTION ( 'NONE',  ( 0.000000000000000000, 0.000000000000000000, 1.000000000000000000 ) ) ;
#866=DIRECTION ( 'NONE',  ( 0.000000000000000000, 1.000000000000000000, -0.000000000000000000 ) ) ;
#867=CARTESIAN_POINT ( 'NONE',  ( 9.641460742840918030, -33.43424481021354921, 68.00000000000000000 ) ) ;
#868=DIRECTION ( 'NONE',  ( 0.000000000000000000, 0.000000000000000000, 1.000000000000000000 ) ) ;
#870=ORIENTED_EDGE ( 'NONE', *, *, #9475, .T. ) ;
#877=VERTEX_POINT ( 'NONE', #21812 ) ;
#881=ORIENTED_EDGE ( 'NONE', *, *, #7498, .T. ) ;
#883=ORIENTED_EDGE ( 'NONE', *, *, #16397, .F. ) ;
#884=DIRECTION ( 'NONE',  ( 0.000000000000000000, 0.000000000000000000, -1.000000000000000000 ) ) ;
#885=DIRECTION ( 'NONE',  ( -1.000000000000000000, 0.000000000000000000, 0.000000000000000000 ) ) ;
#887=AXIS2_PLACEMENT_3D ( 'NONE', #9917, #13697, #8245 ) ;
#890=ADVANCED_FACE ( 'NONE', ( #16862 ), #6705, .F. ) ;
#894=DIRECTION ( 'NONE',  ( 0.000000000000000000, -0.000000000000000000, -1.000000000000000000 ) ) ;
#895=EDGE_LOOP ( 'NONE', ( #14862, #3669, #14526, #19387 ) ) ;
#901=ORIENTED_EDGE ( 'NONE', *, *, #20856, .F. ) ;
#903=VECTOR ( 'NONE', #12659, 1000.000000000000000 ) ;
#913=EDGE_LOOP ( 'NONE', ( #10029, #20388, #14591, #2616 ) ) ;
#915=DIRECTION ( 'NONE',  ( -0.000000000000000000, -0.000000000000000000, -1.000000000000000000 ) ) ;
#916=CARTESIAN_POINT ( 'NONE',  ( -32.20000000000001705, 71.00000000000001421, 3.200000000000000178 ) ) ;
#917=DIRECTION ( 'NONE',  ( 1.000000000000000000, 0.000000000000000000, 0.000000000000000000 ) ) ;
#919=AXIS2_PLACEMENT_3D ( 'NONE', #9639, #7857, #7963 ) ;
#922=ORIENTED_EDGE ( 'NONE', *, *, #21017, .F. ) ;
#925=EDGE_CURVE ( 'NONE', #14127, #8942, #8229, .T. ) ;
#926=ORIENTED_EDGE ( 'NONE', *, *, #4496, .T. ) ;
#927=ORIENTED_EDGE ( 'NONE', *, *, #17536, .T. ) ;
#928=ORIENTED_EDGE ( 'NONE', *, *, #2538, .T. ) ;
#929=DIRECTION ( 'NONE',  ( 1.000000000000000000, 0.000000000000000000, 0.000000000000000000 ) ) ;
#930=CARTESIAN_POINT ( 'NONE',  ( -17.93704824106378837, -50.11873716947361856, 13.87500000000000000 ) ) ;
#932=TOROIDAL_SURFACE ( 'NONE', #14503, 2.274596669241483848, 0.2999999999999999889 ) ;
#933=AXIS2_PLACEMENT_3D ( 'NONE', #13488, #20112, #16949 ) ;
#939=AXIS2_PLACEMENT_3D ( 'NONE', #1566, #15007, #8402 ) ;
#941=CARTESIAN_POINT ( 'NONE',  ( -17.95292532278785913, 50.11873716947361856, 13.49999999999999822 ) ) ;
#942=LINE ( 'NONE', #11873, #13771 ) ;
#944=DIRECTION ( 'NONE',  ( 1.000000000000000000, 0.000000000000000000, 0.000000000000000000 ) ) ;
#945=ORIENTED_EDGE ( 'NONE', *, *, #18650, .T. ) ;
#946=CARTESIAN_POINT ( 'NONE',  ( 3.627054932750481964, -32.61873716947361856, 68.00000000000000000 ) ) ;
#947=DIRECTION ( 'NONE',  ( 0.000000000000000000, -1.000000000000000000, 0.000000000000000000 ) ) ;
#948=DIRECTION ( 'NONE',  ( -1.000000000000000000, 2.832483164223434527E-16, 0.000000000000000000 ) ) ;
#950=EDGE_LOOP ( 'NONE', ( #13983, #7847, #11178, #17308 ) ) ;
#953=CIRCLE ( 'NONE', #17045, 5.000000000000000888 ) ;
#954=LINE ( 'NONE', #14608, #1961 ) ;
#955=DIRECTION ( 'NONE',  ( 1.000000000000000000, 0.000000000000000000, 0.000000000000000000 ) ) ;
#957=ORIENTED_EDGE ( 'NONE', *, *, #11169, .F. ) ;
#960=EDGE_CURVE ( 'NONE', #17392, #1107, #13582, .T. ) ;
#961=VERTEX_POINT ( 'NONE', #3224 ) ;
#963=ORIENTED_EDGE ( 'NONE', *, *, #19556, .F. ) ;
#964=CARTESIAN_POINT ( 'NONE',  ( 15.95292532278785913, -52.10286008774954780, 13.87499999999999822 ) ) ;
#965=DIRECTION ( 'NONE',  ( -0.000000000000000000, -0.000000000000000000, 1.000000000000000000 ) ) ;
#970=VECTOR ( 'NONE', #17319, 1000.000000000000000 ) ;
#971=CARTESIAN_POINT ( 'NONE',  ( -23.02398829872514341, -2.157133865694323305, 13.26854876702554442 ) ) ;
#973=EDGE_CURVE ( 'NONE', #13238, #14227, #9667, .T. ) ;
#975=AXIS2_PLACEMENT_3D ( 'NONE', #21550, #21655, #6109 ) ;
#976=CARTESIAN_POINT ( 'NONE',  ( 18.22752199202934520, -38.74634676501045760, 13.79999999999999893 ) ) ;
#977=AXIS2_PLACEMENT_3D ( 'NONE', #2763, #16516, #13034 ) ;
#979=CARTESIAN_POINT ( 'NONE',  ( 14.96174975910707161, 51.61873716947361856, 68.25000000000000000 ) ) ;
#980=CARTESIAN_POINT ( 'NONE',  ( 28.87540678000427619, 0.000000000000000000, 13.50000000000000000 ) ) ;
#985=LINE ( 'NONE', #21375, #8673 ) ;
#986=TOROIDAL_SURFACE ( 'NONE', #13498, 0.2500000000000000000, 0.2500000000000000000 ) ;
#987=VECTOR ( 'NONE', #3190, 1000.000000000000000 ) ;
#989=LINE ( 'NONE', #8052, #6411 ) ;
#995=AXIS2_PLACEMENT_3D ( 'NONE', #2080, #19097, #10385 ) ;
#996=EDGE_CURVE ( 'NONE', #16076, #18467, #11, .T. ) ;
#997=LINE ( 'NONE', #2581, #18287 ) ;
#998=EDGE_LOOP ( 'NONE', ( #15546, #16742, #6475, #118 ) ) ;
#999=CARTESIAN_POINT ( 'NONE',  ( -29.13662752439705272, 0.000000000000000000, 0.3000000000000016542 ) ) ;
#1002=DIRECTION ( 'NONE',  ( 0.000000000000000000, 0.000000000000000000, 1.000000000000000000 ) ) ;
#1003=DIRECTION ( 'NONE',  ( 0.000000000000000000, 0.000000000000000000, 1.000000000000000000 ) ) ;
#1005=CIRCLE ( 'NONE', #16373, 0.3000000000000004885 ) ;
#1007=CARTESIAN_POINT ( 'NONE',  ( 23.08502376492392116, 2.484776121502525026, 13.35369709827396001 ) ) ;
#1008=AXIS2_PLACEMENT_3D ( 'NONE', #17665, #7398, #9176 ) ;
#1017=ORIENTED_EDGE ( 'NONE', *, *, #8325, .F. ) ;
#1019=VECTOR ( 'NONE', #14846, 1000.000000000000000 ) ;
#1020=CARTESIAN_POINT ( 'NONE',  ( -25.37540678000426908, 36.74634676501047181, 42.50000000000000000 ) ) ;
#1025=CIRCLE ( 'NONE', #7842, 0.2999999999999999334 ) ;
#1026=VERTEX_POINT ( 'NONE', #11494 ) ;
#1027=EDGE_LOOP ( 'NONE', ( #17597, #18505, #3215, #1779 ) ) ;
#1028=AXIS2_PLACEMENT_3D ( 'NONE', #17974, #11251, #18205 ) ;
#1030=ORIENTED_EDGE ( 'NONE', *, *, #6924, .T. ) ;
#1032=DIRECTION ( 'NONE',  ( 0.000000000000000000, 0.000000000000000000, -1.000000000000000000 ) ) ;
#1033=VERTEX_POINT ( 'NONE', #8808 ) ;
#1037=CARTESIAN_POINT ( 'NONE',  ( 0.000000000000000000, -32.11873716947361856, 109.6002446535588319 ) ) ;
#1038=CIRCLE ( 'NONE', #19641, 0.2999999999999999334 ) ;
#1039=EDGE_CURVE ( 'NONE', #20933, #14982, #10815, .T. ) ;
#1040=CARTESIAN_POINT ( 'NONE',  ( 14.98586301832698808, 51.95135570414442583, 13.85537332152988554 ) ) ;
#1042=CARTESIAN_POINT ( 'NONE',  ( -23.02398829872514341, 2.502141052783100061, 13.57900107139873747 ) ) ;
#1047=VERTEX_POINT ( 'NONE', #175 ) ;
#1048=ORIENTED_EDGE ( 'NONE', *, *, #3785, .F. ) ;
#1053=TOROIDAL_SURFACE ( 'NONE', #13353, 0.7000000000000000666, 0.2999999999999999889 ) ;
#1054=CARTESIAN_POINT ( 'NONE',  ( 9.141460742840918030, -33.43424481021354921, 42.50000000000000000 ) ) ;
#1059=DIRECTION ( 'NONE',  ( 1.000000000000000000, 0.000000000000000000, 0.000000000000000000 ) ) ;
#1061=DIRECTION ( 'NONE',  ( 1.000000000000000000, 0.000000000000000000, 0.000000000000000000 ) ) ;
#1063=DIRECTION ( 'NONE',  ( -1.000000000000000000, 0.000000000000000000, 0.000000000000000000 ) ) ;
#1066=DIRECTION ( 'NONE',  ( 1.000000000000000000, 0.000000000000000000, 0.000000000000000000 ) ) ;
#1067=FACE_OUTER_BOUND ( 'NONE', #16797, .T. ) ;
#1071=CYLINDRICAL_SURFACE ( 'NONE', #15191, 0.2999999999999999889 ) ;
#1075=ORIENTED_EDGE ( 'NONE', *, *, #195, .F. ) ;
#1076=AXIS2_PLACEMENT_3D ( 'NONE', #15904, #2049, #5659 ) ;
#1077=CARTESIAN_POINT ( 'NONE',  ( 28.87540678000427619, 6.494748934539263274, 13.19999999999999929 ) ) ;
#1078=CARTESIAN_POINT ( 'NONE',  ( 29.37540678000427619, 5.299999999999999822, 7.200000000000000178 ) ) ;
#1079=EDGE_LOOP ( 'NONE', ( #1272, #8804, #3579, #12493, #1570 ) ) ;
#1080=ORIENTED_EDGE ( 'NONE', *, *, #7728, .F. ) ;
#1082=CARTESIAN_POINT ( 'NONE',  ( 0.000000000000000000, 68.70000000000001705, 0.000000000000000000 ) ) ;
#1088=ADVANCED_FACE ( 'NONE', ( #10487 ), #2301, .T. ) ;
#1089=CARTESIAN_POINT ( 'NONE',  ( -29.17540678000427690, 6.499884319688664647, 7.500000000000000000 ) ) ;
#1090=FACE_OUTER_BOUND ( 'NONE', #20472, .T. ) ;
#1092=CARTESIAN_POINT ( 'NONE',  ( -4.127054932750482408, -33.43424481021354921, 42.50000000000000000 ) ) ;
#1098=DIRECTION ( 'NONE',  ( 1.000000000000000000, 0.000000000000000000, -0.000000000000000000 ) ) ;
#1102=CYLINDRICAL_SURFACE ( 'NONE', #5106, 1.999999999999991340 ) ;
#1103=ORIENTED_EDGE ( 'NONE', *, *, #1983, .T. ) ;
#1105=LINE ( 'NONE', #14981, #13124 ) ;
#1107=VERTEX_POINT ( 'NONE', #17194 ) ;
#1108=EDGE_CURVE ( 'NONE', #18032, #16813, #15430, .T. ) ;
#1109=ORIENTED_EDGE ( 'NONE', *, *, #20925, .T. ) ;
#1110=LINE ( 'NONE', #19462, #5275 ) ;
#1115=AXIS2_PLACEMENT_3D ( 'NONE', #14128, #5670, #14252 ) ;
#1116=DIRECTION ( 'NONE',  ( -0.000000000000000000, -0.000000000000000000, 1.000000000000000000 ) ) ;
#1117=CARTESIAN_POINT ( 'NONE',  ( -29.17540678000427690, 0.000000000000000000, 7.799999999999999822 ) ) ;
#1119=DIRECTION ( 'NONE',  ( 0.000000000000000000, 0.000000000000000000, 1.000000000000000000 ) ) ;
#1121=CARTESIAN_POINT ( 'NONE',  ( 17.45292532278785913, 34.11873716947361856, 68.50000000000000000 ) ) ;
#1124=EDGE_CURVE ( 'NONE', #19800, #11695, #15727, .T. ) ;
#1130=ORIENTED_EDGE ( 'NONE', *, *, #2625, .F. ) ;
#1132=DIRECTION ( 'NONE',  ( -1.000000000000000000, 0.000000000000000000, 0.000000000000000000 ) ) ;
#1133=ORIENTED_EDGE ( 'NONE', *, *, #9281, .F. ) ;
#1134=ORIENTED_EDGE ( 'NONE', *, *, #14013, .F. ) ;
#1136=EDGE_CURVE ( 'NONE', #20345, #10550, #18886, .T. ) ;
#1137=EDGE_LOOP ( 'NONE', ( #8614, #20350, #9374, #13119, #17297, #5583, #19057, #13369, #18610, #9638, #5260, #1739, #4437, #4162, #14733, #9061, #11584, #10946, #4991, #16370, #21549, #21887, #415, #16787 ) ) ;
#1140=CARTESIAN_POINT ( 'NONE',  ( -14.66895125224955976, -51.92349729544097414, 13.50000000000000000 ) ) ;
#1141=VECTOR ( 'NONE', #6596, 1000.000000000000000 ) ;
#1142=DIRECTION ( 'NONE',  ( 0.000000000000000000, 0.000000000000000000, 1.000000000000000000 ) ) ;
#1144=CARTESIAN_POINT ( 'NONE',  ( 32.50000000000002132, 72.00000000000001421, 1.800000000000000044 ) ) ;
#1145=DIRECTION ( 'NONE',  ( 0.000000000000000000, 0.000000000000000000, 1.000000000000000000 ) ) ;
#1146=DIRECTION ( 'NONE',  ( 0.000000000000000000, -1.000000000000000000, 0.000000000000000000 ) ) ;
#1147=EDGE_CURVE ( 'NONE', #2755, #12023, #21164, .T. ) ;
#1148=VERTEX_POINT ( 'NONE', #12247 ) ;
#1150=VERTEX_POINT ( 'NONE', #15830 ) ;
#1151=ORIENTED_EDGE ( 'NONE', *, *, #13368, .T. ) ;
#1152=VERTEX_POINT ( 'NONE', #19098 ) ;
#1153=DIRECTION ( 'NONE',  ( -0.000000000000000000, -0.000000000000000000, -1.000000000000000000 ) ) ;
#1154=CARTESIAN_POINT ( 'NONE',  ( 27.37540678000427619, 10.94079601157914539, 13.79999999999999893 ) ) ;
#1156=DIRECTION ( 'NONE',  ( 1.000000000000000000, 0.000000000000000000, 0.000000000000000000 ) ) ;
#1157=ADVANCED_FACE ( 'NONE', ( #20892 ), #3766, .T. ) ;
#1158=EDGE_CURVE ( 'NONE', #22102, #16814, #5693, .T. ) ;
#1162=EDGE_CURVE ( 'NONE', #18311, #2722, #418, .T. ) ;
#1163=CARTESIAN_POINT ( 'NONE',  ( -15.21174975910705207, 51.86873716947361856, 14.00000000000000000 ) ) ;
#1165=VERTEX_POINT ( 'NONE', #14599 ) ;
#1168=CARTESIAN_POINT ( 'NONE',  ( -15.05282292896043295, 52.05812657117055409, 13.87232935072191786 ) ) ;
#1170=VERTEX_POINT ( 'NONE', #17956 ) ;
#1171=DIRECTION ( 'NONE',  ( 1.000000000000000000, 0.000000000000000000, 0.000000000000000000 ) ) ;
#1175=FACE_OUTER_BOUND ( 'NONE', #21833, .T. ) ;
#1178=VERTEX_POINT ( 'NONE', #7909 ) ;
#1179=ORIENTED_EDGE ( 'NONE', *, *, #2808, .T. ) ;
#1180=CARTESIAN_POINT ( 'NONE',  ( -15.12826760881917387, 51.99271056040087302, 13.49999999999999822 ) ) ;
#1183=LINE ( 'NONE', #12697, #18158 ) ;
#1185=EDGE_LOOP ( 'NONE', ( #14887, #223, #21649, #15891, #11578, #7138, #9352, #4309, #18651, #11198, #21910, #11567, #14634, #6720, #9249, #18703, #5681, #4978, #21522, #20267, #20160, #10856, #11371, #7817 ) ) ;
#1187=ADVANCED_FACE ( 'NONE', ( #2416 ), #21122, .F. ) ;
#1194=CARTESIAN_POINT ( 'NONE',  ( -15.95292532278785913, -50.11873716947361856, 13.79999999999999893 ) ) ;
#1196=DIRECTION ( 'NONE',  ( -1.000000000000000000, -0.000000000000000000, -0.000000000000000000 ) ) ;
#1197=DIRECTION ( 'NONE',  ( 1.000000000000000000, -0.000000000000000000, 0.000000000000000000 ) ) ;
#1199=CARTESIAN_POINT ( 'NONE',  ( 23.04273156199908357, 2.261510999192738680, 13.50000000000000000 ) ) ;
#1202=AXIS2_PLACEMENT_3D ( 'NONE', #20688, #17852, #5899 ) ;
#1204=EDGE_CURVE ( 'NONE', #19855, #10005, #21882, .T. ) ;
#1206=ORIENTED_EDGE ( 'NONE', *, *, #16364, .T. ) ;
#1207=DIRECTION ( 'NONE',  ( -1.000000000000000000, 0.000000000000000000, 0.000000000000000000 ) ) ;
#1211=CARTESIAN_POINT ( 'NONE',  ( 3.127054932750481964, -32.61873716947361856, 68.00000000000000000 ) ) ;
#1212=ORIENTED_EDGE ( 'NONE', *, *, #1930, .T. ) ;
#1214=DIRECTION ( 'NONE',  ( 0.000000000000000000, 0.000000000000000000, 1.000000000000000000 ) ) ;
#1215=CARTESIAN_POINT ( 'NONE',  ( 23.18291235612340628, 2.947575143997193337, 13.45754841673216973 ) ) ;
#1217=CYLINDRICAL_SURFACE ( 'NONE', #4984, 0.2999999999999999334 ) ;
#1223=EDGE_CURVE ( 'NONE', #21686, #13159, #1495, .T. ) ;
#1224=ORIENTED_EDGE ( 'NONE', *, *, #17536, .F. ) ;
#1226=ORIENTED_EDGE ( 'NONE', *, *, #2404, .F. ) ;
#1227=DIRECTION ( 'NONE',  ( 0.000000000000000000, 0.000000000000000000, -1.000000000000000000 ) ) ;
#1230=CYLINDRICAL_SURFACE ( 'NONE', #15654, 1.000000000000000888 ) ;
#1231=ORIENTED_EDGE ( 'NONE', *, *, #21219, .T. ) ;
#1232=EDGE_LOOP ( 'NONE', ( #17781, #13374, #17762, #19889 ) ) ;
#1233=DIRECTION ( 'NONE',  ( 0.000000000000000000, 0.000000000000000000, -1.000000000000000000 ) ) ;
#1235=UNCERTAINTY_MEASURE_WITH_UNIT (LENGTH_MEASURE( 1.000000000000000082E-05 ), #13754, 'distance_accuracy_value', 'NONE');
#1236=ORIENTED_EDGE ( 'NONE', *, *, #17216, .T. ) ;
#1237=DIRECTION ( 'NONE',  ( 0.000000000000000000, 0.000000000000000000, 1.000000000000000000 ) ) ;
#1239=VERTEX_POINT ( 'NONE', #21334 ) ;
#1240=ORIENTED_EDGE ( 'NONE', *, *, #195, .T. ) ;
#1241=CARTESIAN_POINT ( 'NONE',  ( 15.00289696508457915, -51.98500081155935248, 13.86091301037357226 ) ) ;
#1243=CARTESIAN_POINT ( 'NONE',  ( 9.641460742840918030, 32.61873716947361856, 68.00000000000000000 ) ) ;
#1244=ORIENTED_EDGE ( 'NONE', *, *, #4424, .F. ) ;
#1245=DIRECTION ( 'NONE',  ( 1.000000000000000000, 0.000000000000000000, 0.000000000000000000 ) ) ;
#1248=CARTESIAN_POINT ( 'NONE',  ( -29.01849620351543280, 6.499161877189502334, 7.532606289305298297 ) ) ;
#1250=ADVANCED_FACE ( 'NONE', ( #9350 ), #4209, .F. ) ;
#1253=VECTOR ( 'NONE', #14129, 1000.000000000000000 ) ;
#1256=AXIS2_PLACEMENT_3D ( 'NONE', #14931, #16393, #4420 ) ;
#1257=ORIENTED_EDGE ( 'NONE', *, *, #16855, .T. ) ;
#1258=DIRECTION ( 'NONE',  ( 0.000000000000000000, 0.000000000000000000, 1.000000000000000000 ) ) ;
#1259=FACE_OUTER_BOUND ( 'NONE', #20406, .T. ) ;
#1261=DIRECTION ( 'NONE',  ( -0.000000000000000000, -1.000000000000000000, -0.000000000000000000 ) ) ;
#1262=EDGE_LOOP ( 'NONE', ( #12377, #121, #4226, #1320 ) ) ;
#1263=DIRECTION ( 'NONE',  ( 0.000000000000000000, 0.000000000000000000, 1.000000000000000000 ) ) ;
#1264=VECTOR ( 'NONE', #3007, 1000.000000000000000 ) ;
#1266=LINE ( 'NONE', #11350, #12361 ) ;
#1269=CIRCLE ( 'NONE', #3432, 2.500000000000002220 ) ;
#1272=ORIENTED_EDGE ( 'NONE', *, *, #5763, .F. ) ;
#1274=CARTESIAN_POINT ( 'NONE',  ( 9.641460742840918030, -32.61873716947361856, 68.50000000000000000 ) ) ;
#1278=CARTESIAN_POINT ( 'NONE',  ( -29.13662752439705272, 4.700000000000000178, 3.799999999999999822 ) ) ;
#1279=CARTESIAN_POINT ( 'NONE',  ( -29.50000000000002132, 2.473451120191013430, -150.0833101980363722 ) ) ;
#1280=ADVANCED_FACE ( 'NONE', ( #21453 ), #6124, .T. ) ;
#1281=EDGE_CURVE ( 'NONE', #16343, #19005, #21564, .T. ) ;
#1282=ORIENTED_EDGE ( 'NONE', *, *, #19556, .T. ) ;
#1283=CARTESIAN_POINT ( 'NONE',  ( -30.67540678000428045, -6.000000000000000000, 3.500000000000000000 ) ) ;
#1284=EDGE_CURVE ( 'NONE', #17663, #13966, #8905, .T. ) ;
#1287=AXIS2_PLACEMENT_3D ( 'NONE', #13763, #5302, #10764 ) ;
#1289=AXIS2_PLACEMENT_3D ( 'NONE', #14870, #21727, #16657 ) ;
#1291=DIRECTION ( 'NONE',  ( 0.000000000000000000, 1.000000000000000000, 0.000000000000000000 ) ) ;
#1292=EDGE_CURVE ( 'NONE', #20277, #1170, #19360, .T. ) ;
#1295=VECTOR ( 'NONE', #11323, 1000.000000000000000 ) ;
#1296=ORIENTED_EDGE ( 'NONE', *, *, #11231, .T. ) ;
#1297=DIRECTION ( 'NONE',  ( 1.000000000000000000, 0.000000000000000000, 0.000000000000000000 ) ) ;
#1299=CARTESIAN_POINT ( 'NONE',  ( 9.641460742840918030, 32.11873716947361856, 109.6002446535588319 ) ) ;
#1300=CARTESIAN_POINT ( 'NONE',  ( -23.02398829872513986, -2.877181859310994128, 13.71509684061244450 ) ) ;
#1301=CARTESIAN_POINT ( 'NONE',  ( -17.45292532278785913, 0.000000000000000000, 68.00000000000000000 ) ) ;
#1302=CIRCLE ( 'NONE', #16664, 1.500000000000001332 ) ;
#1304=AXIS2_PLACEMENT_3D ( 'NONE', #3872, #10571, #7334 ) ;
#1306=VECTOR ( 'NONE', #14026, 1000.000000000000000 ) ;
#1312=FACE_OUTER_BOUND ( 'NONE', #16989, .T. ) ;
#1313=ADVANCED_FACE ( 'NONE', ( #22086 ), #3381, .T. ) ;
#1317=CARTESIAN_POINT ( 'NONE',  ( -27.67540678000428045, 7.839012376739720627E-15, 13.79999999999999893 ) ) ;
#1319=CARTESIAN_POINT ( 'NONE',  ( 28.87540678000427619, -6.494748934539263274, 13.19999999999999929 ) ) ;
#1320=ORIENTED_EDGE ( 'NONE', *, *, #4061, .T. ) ;
#1322=AXIS2_PLACEMENT_3D ( 'NONE', #21500, #17998, #7849 ) ;
#1325=CARTESIAN_POINT ( 'NONE',  ( 29.20000000000002061, -2.799282752659324025, 0.000000000000000000 ) ) ;
#1326=AXIS2_PLACEMENT_3D ( 'NONE', #15402, #6923, #5230 ) ;
#1327=VERTEX_POINT ( 'NONE', #17558 ) ;
#1330=CARTESIAN_POINT ( 'NONE',  ( 29.13662752439705272, 5.000000000000000000, 7.500000000000000000 ) ) ;
#1333=FACE_OUTER_BOUND ( 'NONE', #9515, .T. ) ;
#1335=AXIS2_PLACEMENT_3D ( 'NONE', #21037, #19346, #15749 ) ;
#1337=CARTESIAN_POINT ( 'NONE',  ( 23.21374285137841298, 3.085791193308921265, 13.47995019114138415 ) ) ;
#1339=DIRECTION ( 'NONE',  ( 0.000000000000000000, 1.000000000000000000, -0.000000000000000000 ) ) ;
#1342=CARTESIAN_POINT ( 'NONE',  ( 14.66174975910705847, 51.76873716947361714, 13.80000000000000071 ) ) ;
#1344=EDGE_CURVE ( 'NONE', #8084, #10729, #15644, .T. ) ;
#1346=DIRECTION ( 'NONE',  ( 0.000000000000000000, 0.000000000000000000, 1.000000000000000000 ) ) ;
#1347=ORIENTED_EDGE ( 'NONE', *, *, #20274, .T. ) ;
#1349=CARTESIAN_POINT ( 'NONE',  ( 4.127054932750481520, 32.93424481021354921, 68.00000000000000000 ) ) ;
#1350=VERTEX_POINT ( 'NONE', #19125 ) ;
#1357=VERTEX_POINT ( 'NONE', #14302 ) ;
#1358=ORIENTED_EDGE ( 'NONE', *, *, #2520, .T. ) ;
#1360=AXIS2_PLACEMENT_3D ( 'NONE', #12287, #19259, #334 ) ;
#1361=ORIENTED_EDGE ( 'NONE', *, *, #9673, .F. ) ;
#1364=DIRECTION ( 'NONE',  ( 0.000000000000000000, 0.000000000000000000, -1.000000000000000000 ) ) ;
#1365=ADVANCED_FACE ( 'NONE', ( #321 ), #10838, .T. ) ;
#1369=CARTESIAN_POINT ( 'NONE',  ( -23.02398829872513986, 3.395586890286275139, 13.79999998301280328 ) ) ;
#1372=CARTESIAN_POINT ( 'NONE',  ( 25.37540678000427263, 67.54634676501045476, 7.500000000000000000 ) ) ;
#1373=FACE_OUTER_BOUND ( 'NONE', #21577, .T. ) ;
#1375=ORIENTED_EDGE ( 'NONE', *, *, #15709, .F. ) ;
#1376=ORIENTED_EDGE ( 'NONE', *, *, #8385, .F. ) ;
#1378=CARTESIAN_POINT ( 'NONE',  ( 4.127054932750481520, -32.93424481021354921, 42.50000000000000000 ) ) ;
#1383=ORIENTED_EDGE ( 'NONE', *, *, #17832, .T. ) ;
#1384=DIRECTION ( 'NONE',  ( -0.000000000000000000, -0.000000000000000000, -1.000000000000000000 ) ) ;
#1385=LINE ( 'NONE', #2966, #21696 ) ;
#1387=ADVANCED_FACE ( 'NONE', ( #9278 ), #2115, .F. ) ;
#1390=LINE ( 'NONE', #3303, #21690 ) ;
#1391=ORIENTED_EDGE ( 'NONE', *, *, #8160, .T. ) ;
#1392=DIRECTION ( 'NONE',  ( -1.000000000000000000, -0.000000000000000000, 2.388292521039847891E-16 ) ) ;
#1393=DIRECTION ( 'NONE',  ( 0.000000000000000000, 0.000000000000000000, 1.000000000000000000 ) ) ;
#1395=EDGE_LOOP ( 'NONE', ( #10162, #19516, #12645, #8970 ) ) ;
#1400=LINE ( 'NONE', #13265, #15573 ) ;
#1401=VERTEX_POINT ( 'NONE', #5385 ) ;
#1402=ORIENTED_EDGE ( 'NONE', *, *, #5701, .F. ) ;
#1403=ORIENTED_EDGE ( 'NONE', *, *, #10168, .F. ) ;
#1405=EDGE_CURVE ( 'NONE', #13059, #10497, #3111, .T. ) ;
#1406=CARTESIAN_POINT ( 'NONE',  ( 25.37540678000427263, 69.04634676501045476, 3.500000000000000000 ) ) ;
#1408=AXIS2_PLACEMENT_3D ( 'NONE', #17856, #6239, #16165 ) ;
#1409=TOROIDAL_SURFACE ( 'NONE', #13907, 5.299999999999999822, 0.2999999999999999889 ) ;
#1416=EDGE_CURVE ( 'NONE', #4773, #1863, #19197, .T. ) ;
#1417=DIRECTION ( 'NONE',  ( 1.000000000000000000, 8.881784197001254296E-16, 0.000000000000000000 ) ) ;
#1418=CARTESIAN_POINT ( 'NONE',  ( 29.13662752439705272, 5.000000000000000000, 7.200000000000000178 ) ) ;
#1419=EDGE_CURVE ( 'NONE', #19294, #9791, #4572, .T. ) ;
#1421=DIRECTION ( 'NONE',  ( -0.000000000000000000, -0.000000000000000000, -1.000000000000000000 ) ) ;
#1422=CARTESIAN_POINT ( 'NONE',  ( 25.37540678000427263, 63.74634676501045050, 7.799999999999999822 ) ) ;
#1425=AXIS2_PLACEMENT_3D ( 'NONE', #20226, #4902, #18546 ) ;
#1429=CARTESIAN_POINT ( 'NONE',  ( -8.641460742840918030, 32.93424481021354921, 68.00000000000000000 ) ) ;
#1430=ORIENTED_EDGE ( 'NONE', *, *, #360, .F. ) ;
#1431=CARTESIAN_POINT ( 'NONE',  ( 14.66174975910705847, 0.000000000000000000, 13.50000000000000000 ) ) ;
#1433=ORIENTED_EDGE ( 'NONE', *, *, #13453, .T. ) ;
#1434=DIRECTION ( 'NONE',  ( -1.000000000000000000, -0.000000000000000000, -0.000000000000000000 ) ) ;
#1438=ORIENTED_EDGE ( 'NONE', *, *, #3254, .T. ) ;
#1439=CARTESIAN_POINT ( 'NONE',  ( -29.13662752439705272, 0.000000000000000000, 7.200000000000000178 ) ) ;
#1440=VECTOR ( 'NONE', #12854, 1000.000000000000000 ) ;
#1442=EDGE_CURVE ( 'NONE', #6809, #18032, #16429, .T. ) ;
#1443=DIRECTION ( 'NONE',  ( 1.000000000000000000, 0.000000000000000000, 0.000000000000000000 ) ) ;
#1445=EDGE_CURVE ( 'NONE', #7686, #22008, #13837, .T. ) ;
#1448=DIRECTION ( 'NONE',  ( 0.000000000000000000, 0.000000000000000000, -1.000000000000000000 ) ) ;
#1449=CARTESIAN_POINT ( 'NONE',  ( 25.37540678000427263, -63.74634676501045050, 13.50000000000000000 ) ) ;
#1453=CARTESIAN_POINT ( 'NONE',  ( -14.90262738048940960, -52.32122554936407255, 13.50000000000000000 ) ) ;
#1455=VERTEX_POINT ( 'NONE', #6264 ) ;
#1456=EDGE_CURVE ( 'NONE', #11318, #1170, #16296, .T. ) ;
#1458=VERTEX_POINT ( 'NONE', #979 ) ;
#1459=CARTESIAN_POINT ( 'NONE',  ( -15.95292532278785913, -32.11873716947361856, 109.6002446535588319 ) ) ;
#1462=DIRECTION ( 'NONE',  ( -0.000000000000000000, -0.000000000000000000, -1.000000000000000000 ) ) ;
#1466=ORIENTED_EDGE ( 'NONE', *, *, #22110, .F. ) ;
#1467=TOROIDAL_SURFACE ( 'NONE', #1115, 1.300000000000000044, 0.2999999999999999889 ) ;
#1468=SURFACE_STYLE_USAGE ( .BOTH. , #3490 ) ;
#1469=ORIENTED_EDGE ( 'NONE', *, *, #3727, .F. ) ;
#1471=AXIS2_PLACEMENT_3D ( 'NONE', #5011, #10148, #16962 ) ;
#1472=EDGE_LOOP ( 'NONE', ( #11225, #14748 ) ) ;
#1473=EDGE_CURVE ( 'NONE', #16854, #225, #12713, .T. ) ;
#1476=DIRECTION ( 'NONE',  ( -1.000000000000000000, 0.000000000000000000, 0.000000000000000000 ) ) ;
#1477=DIRECTION ( 'NONE',  ( 0.000000000000000000, 0.000000000000000000, 1.000000000000000000 ) ) ;
#1480=VECTOR ( 'NONE', #16480, 1000.000000000000000 ) ;
#1481=DIRECTION ( 'NONE',  ( 1.000000000000000000, 0.000000000000000000, 0.000000000000000000 ) ) ;
#1482=AXIS2_PLACEMENT_3D ( 'NONE', #20081, #19847, #12997 ) ;
#1485=CARTESIAN_POINT ( 'NONE',  ( 28.57540678000427548, -63.74634676501045050, 13.50000000000000000 ) ) ;
#1492=ORIENTED_EDGE ( 'NONE', *, *, #3274, .F. ) ;
#1494=EDGE_CURVE ( 'NONE', #8747, #18098, #11392, .T. ) ;
#1495=CIRCLE ( 'NONE', #8997, 0.2999999999999999334 ) ;
#1496=DIRECTION ( 'NONE',  ( 0.000000000000000000, 1.000000000000000000, 0.000000000000000000 ) ) ;
#1497=CIRCLE ( 'NONE', #4366, 5.000000000000004441 ) ;
#1498=AXIS2_PLACEMENT_3D ( 'NONE', #18426, #4450, #21813 ) ;
#1500=DIRECTION ( 'NONE',  ( 1.000000000000000000, 0.000000000000000000, 0.000000000000000000 ) ) ;
#1503=ORIENTED_EDGE ( 'NONE', *, *, #6884, .F. ) ;
#1505=FACE_OUTER_BOUND ( 'NONE', #18436, .T. ) ;
#1506=DIRECTION ( 'NONE',  ( 0.000000000000000000, 0.000000000000000000, -1.000000000000000000 ) ) ;
#1509=EDGE_CURVE ( 'NONE', #16343, #16814, #13466, .T. ) ;
#1510=DIRECTION ( 'NONE',  ( 1.000000000000000000, 0.000000000000000000, 0.000000000000000000 ) ) ;
#1513=VERTEX_POINT ( 'NONE', #21489 ) ;
#1515=ORIENTED_EDGE ( 'NONE', *, *, #20411, .T. ) ;
#1517=ORIENTED_EDGE ( 'NONE', *, *, #9821, .F. ) ;
#1518=FACE_OUTER_BOUND ( 'NONE', #13221, .T. ) ;
#1520=DIRECTION ( 'NONE',  ( 0.000000000000000000, 0.000000000000000000, 1.000000000000000000 ) ) ;
#1521=ORIENTED_EDGE ( 'NONE', *, *, #20493, .F. ) ;
#1524=ORIENTED_EDGE ( 'NONE', *, *, #18572, .F. ) ;
#1525=VERTEX_POINT ( 'NONE', #19910 ) ;
#1526=CARTESIAN_POINT ( 'NONE',  ( -28.87540678000427619, 6.494748934539263274, 13.19999999999999929 ) ) ;
#1528=FACE_OUTER_BOUND ( 'NONE', #18608, .T. ) ;
#1529=CARTESIAN_POINT ( 'NONE',  ( -17.95292532278785913, -38.74634676501045760, 13.99999999999999822 ) ) ;
#1531=LINE ( 'NONE', #18656, #1982 ) ;
#1534=DIRECTION ( 'NONE',  ( 0.000000000000000000, 0.000000000000000000, -1.000000000000000000 ) ) ;
#1535=VERTEX_POINT ( 'NONE', #21704 ) ;
#1536=CARTESIAN_POINT ( 'NONE',  ( -29.13662752439705272, 0.000000000000000000, 7.500000000000000000 ) ) ;
#1537=ORIENTED_EDGE ( 'NONE', *, *, #13957, .T. ) ;
#1539=ADVANCED_FACE ( 'NONE', ( #2559 ), #20026, .T. ) ;
#1541=ORIENTED_EDGE ( 'NONE', *, *, #6935, .T. ) ;
#1542=EDGE_CURVE ( 'NONE', #12877, #4113, #9543, .T. ) ;
#1543=ORIENTED_EDGE ( 'NONE', *, *, #18336, .T. ) ;
#1544=DIRECTION ( 'NONE',  ( -1.000000000000000000, 0.000000000000000000, 0.000000000000000000 ) ) ;
#1551=CARTESIAN_POINT ( 'NONE',  ( 30.37540678000427619, 63.74634676501045050, 7.200000000000000178 ) ) ;
#1552=DIRECTION ( 'NONE',  ( 0.000000000000000000, 0.000000000000000000, 1.000000000000000000 ) ) ;
#1557=DIRECTION ( 'NONE',  ( 0.000000000000000000, -0.000000000000000000, -1.000000000000000000 ) ) ;
#1558=CARTESIAN_POINT ( 'NONE',  ( 3.127054932750481964, -32.61873716947361856, 68.50000000000000000 ) ) ;
#1559=CARTESIAN_POINT ( 'NONE',  ( -25.37540678000427263, 63.74634676501045050, 7.500000000000000000 ) ) ;
#1561=EDGE_CURVE ( 'NONE', #11695, #9706, #12392, .T. ) ;
#1563=EDGE_CURVE ( 'NONE', #15847, #17106, #20130, .T. ) ;
#1565=ORIENTED_EDGE ( 'NONE', *, *, #1936, .F. ) ;
#1566=CARTESIAN_POINT ( 'NONE',  ( -15.21174975910705207, 51.61873716947361856, 14.00000000000000000 ) ) ;
#1570=ORIENTED_EDGE ( 'NONE', *, *, #6982, .T. ) ;
#1571=CIRCLE ( 'NONE', #19809, 1.999999999999991340 ) ;
#1573=CARTESIAN_POINT ( 'NONE',  ( 9.141460742840918030, 32.93424481021354921, 13.50000000000000000 ) ) ;
#1577=VERTEX_POINT ( 'NONE', #6831 ) ;
#1581=CARTESIAN_POINT ( 'NONE',  ( 14.66174954729678248, -51.84624528035402591, 13.50000000000000000 ) ) ;
#1582=DIRECTION ( 'NONE',  ( 0.000000000000000000, -1.000000000000000000, 0.000000000000000000 ) ) ;
#1583=EDGE_LOOP ( 'NONE', ( #4955, #12650, #10583, #13460 ) ) ;
#1585=CARTESIAN_POINT ( 'NONE',  ( -23.02398829872513986, 3.528912754968630328, 13.50000000000000000 ) ) ;
#1587=DIRECTION ( 'NONE',  ( 0.000000000000000000, 0.000000000000000000, 1.000000000000000000 ) ) ;
#1588=CARTESIAN_POINT ( 'NONE',  ( -29.50000000000002132, 0.000000000000000000, 1.500000000000000000 ) ) ;
#1593=CARTESIAN_POINT ( 'NONE',  ( -25.37540678000427263, 66.94634676501046044, 13.50000000000000000 ) ) ;
#1595=DIRECTION ( 'NONE',  ( 1.000000000000000000, 0.000000000000000000, -0.000000000000000000 ) ) ;
#1598=CARTESIAN_POINT ( 'NONE',  ( 14.97552947837228388, -51.92046840034491595, 13.84856038353110463 ) ) ;
#1600=EDGE_LOOP ( 'NONE', ( #527, #18675, #6558, #19357 ) ) ;
#1601=DIRECTION ( 'NONE',  ( 0.000000000000000000, 0.000000000000000000, 1.000000000000000000 ) ) ;
#1602=LINE ( 'NONE', #6997, #7757 ) ;
#1604=DIRECTION ( 'NONE',  ( 0.000000000000000000, 0.000000000000000000, 1.000000000000000000 ) ) ;
#1605=ORIENTED_EDGE ( 'NONE', *, *, #6167, .T. ) ;
#1608=ADVANCED_FACE ( 'NONE', ( #5133 ), #18549, .T. ) ;
#1609=DIRECTION ( 'NONE',  ( 1.000000000000000000, 0.000000000000000000, 0.000000000000000000 ) ) ;
#1611=DIRECTION ( 'NONE',  ( 1.000000000000000000, 0.000000000000000000, 0.000000000000000000 ) ) ;
#1612=CARTESIAN_POINT ( 'NONE',  ( 4.127054932750481520, -32.93424481021354921, 68.00000000000000000 ) ) ;
#1613=ORIENTED_EDGE ( 'NONE', *, *, #17580, .F. ) ;
#1614=FACE_OUTER_BOUND ( 'NONE', #8727, .T. ) ;
#1615=AXIS2_PLACEMENT_3D ( 'NONE', #3649, #19187, #15489 ) ;
#1617=ORIENTED_EDGE ( 'NONE', *, *, #10800, .F. ) ;
#1621=VERTEX_POINT ( 'NONE', #3232 ) ;
#1622=EDGE_LOOP ( 'NONE', ( #3180, #10516, #20398, #12726 ) ) ;
#1623=DIRECTION ( 'NONE',  ( 3.052134192567367925E-16, -1.000000000000000000, 0.000000000000000000 ) ) ;
#1625=CARTESIAN_POINT ( 'NONE',  ( 29.05186365738250842, 0.05288320938007240457, 0.2999999999999947153 ) ) ;
#1626=ORIENTED_EDGE ( 'NONE', *, *, #21936, .F. ) ;
#1627=DIRECTION ( 'NONE',  ( 1.000000000000000000, 0.000000000000000000, -0.000000000000000000 ) ) ;
#1631=AXIS2_PLACEMENT_3D ( 'NONE', #8064, #16210, #18239 ) ;
#1632=AXIS2_PLACEMENT_3D ( 'NONE', #13798, #12228, #15810 ) ;
#1637=DIRECTION ( 'NONE',  ( 1.000000000000000000, 0.000000000000000000, 0.000000000000000000 ) ) ;
#1638=CARTESIAN_POINT ( 'NONE',  ( 17.45292532278785913, -38.74634676501045760, 14.00000000000000000 ) ) ;
#1640=PLANE ( 'NONE',  #17722 ) ;
#1644=CARTESIAN_POINT ( 'NONE',  ( 0.000000000000000000, -68.74634676501045760, 7.500000000000000000 ) ) ;
#1647=VECTOR ( 'NONE', #20575, 1000.000000000000000 ) ;
#1650=FACE_OUTER_BOUND ( 'NONE', #12109, .T. ) ;
#1657=VERTEX_POINT ( 'NONE', #3444 ) ;
#1659=AXIS2_PLACEMENT_3D ( 'NONE', #16500, #16597, #8011 ) ;
#1660=AXIS2_PLACEMENT_3D ( 'NONE', #17749, #10927, #11370 ) ;
#1664=DIRECTION ( 'NONE',  ( 0.000000000000000000, 0.000000000000000000, 1.000000000000000000 ) ) ;
#1667=ADVANCED_FACE ( 'NONE', ( #8813 ), #506, .T. ) ;
#1668=LINE ( 'NONE', #8292, #3144 ) ;
#1669=EDGE_CURVE ( 'NONE', #12996, #1905, #11203, .T. ) ;
#1671=DIRECTION ( 'NONE',  ( -0.000000000000000000, -0.000000000000000000, -1.000000000000000000 ) ) ;
#1672=DIRECTION ( 'NONE',  ( 1.000000000000000000, 0.000000000000000000, 0.000000000000000000 ) ) ;
#1673=CARTESIAN_POINT ( 'NONE',  ( -31.50000000000002132, -71.70000000000001705, 1.500000000000000000 ) ) ;
#1674=AXIS2_PLACEMENT_3D ( 'NONE', #2266, #12548, #1931 ) ;
#1675=CARTESIAN_POINT ( 'NONE',  ( -15.00548668436308830, -51.86811046850819906, 13.49999999999993072 ) ) ;
#1676=CARTESIAN_POINT ( 'NONE',  ( -17.93704824106378837, 0.000000000000000000, 13.87500000000000000 ) ) ;
#1677=VECTOR ( 'NONE', #16986, 1000.000000000000000 ) ;
#1682=LINE ( 'NONE', #8199, #17729 ) ;
#1683=TOROIDAL_SURFACE ( 'NONE', #10279, 4.700000000000000178, 0.2999999999999999889 ) ;
#1687=ORIENTED_EDGE ( 'NONE', *, *, #18273, .T. ) ;
#1688=DIRECTION ( 'NONE',  ( 1.000000000000000000, 0.000000000000000000, 0.000000000000000000 ) ) ;
#1690=EDGE_CURVE ( 'NONE', #17214, #17444, #4426, .T. ) ;
#1694=CIRCLE ( 'NONE', #8845, 0.5000000000000000000 ) ;
#1697=DIRECTION ( 'NONE',  ( 1.000000000000000000, 0.000000000000000000, -0.000000000000000000 ) ) ;
#1699=EDGE_CURVE ( 'NONE', #17937, #16591, #10715, .T. ) ;
#1701=AXIS2_PLACEMENT_3D ( 'NONE', #5084, #17154, #1713 ) ;
#1705=FACE_OUTER_BOUND ( 'NONE', #14578, .T. ) ;
#1708=ORIENTED_EDGE ( 'NONE', *, *, #9949, .F. ) ;
#1710=AXIS2_PLACEMENT_3D ( 'NONE', #19338, #13840, #5484 ) ;
#1711=VERTEX_POINT ( 'NONE', #19218 ) ;
#1712=EDGE_LOOP ( 'NONE', ( #78, #5706, #1361, #4255 ) ) ;
#1713=DIRECTION ( 'NONE',  ( 0.000000000000000000, 0.000000000000000000, 1.000000000000000000 ) ) ;
#1716=ADVANCED_FACE ( 'NONE', ( #12152 ), #12476, .T. ) ;
#1718=AXIS2_PLACEMENT_3D ( 'NONE', #16891, #21941, #6617 ) ;
#1719=CARTESIAN_POINT ( 'NONE',  ( -18.22752199202934520, 0.000000000000000000, 13.79999999999999893 ) ) ;
#1720=CIRCLE ( 'NONE', #7091, 0.5000000000000004441 ) ;
#1724=DIRECTION ( 'NONE',  ( 0.000000000000000000, 0.000000000000000000, 1.000000000000000000 ) ) ;
#1729=AXIS2_PLACEMENT_3D ( 'NONE', #4229, #11047, #21355 ) ;
#1732=CARTESIAN_POINT ( 'NONE',  ( 29.05186365738250842, 0.05288320938007240457, 1.500000000000000000 ) ) ;
#1735=FACE_OUTER_BOUND ( 'NONE', #6534, .T. ) ;
#1738=PLANE ( 'NONE',  #21504 ) ;
#1739=ORIENTED_EDGE ( 'NONE', *, *, #11285, .F. ) ;
#1744=ORIENTED_EDGE ( 'NONE', *, *, #20998, .F. ) ;
#1745=LINE ( 'NONE', #17176, #15044 ) ;
#1746=CARTESIAN_POINT ( 'NONE',  ( -14.66174975910705136, 0.000000000000000000, 13.79999999999999893 ) ) ;
#1747=LINE ( 'NONE', #20208, #20248 ) ;
#1748=VERTEX_POINT ( 'NONE', #14157 ) ;
#1754=EDGE_LOOP ( 'NONE', ( #15471, #21587, #18670, #2197 ) ) ;
#1756=EDGE_CURVE ( 'NONE', #9468, #9603, #17995, .T. ) ;
#1757=AXIS2_PLACEMENT_3D ( 'NONE', #15048, #11901, #14934 ) ;
#1758=ORIENTED_EDGE ( 'NONE', *, *, #5831, .F. ) ;
#1762=CARTESIAN_POINT ( 'NONE',  ( -23.02398829872513986, -3.528912754968629439, 13.50000000000000178 ) ) ;
#1763=CARTESIAN_POINT ( 'NONE',  ( -17.95292532278785913, 0.000000000000000000, 13.99999999999999822 ) ) ;
#1767=CARTESIAN_POINT ( 'NONE',  ( -29.50000000000002132, 0.000000000000000000, -150.0833101980363722 ) ) ;
#1768=EDGE_CURVE ( 'NONE', #1239, #9810, #3359, .T. ) ;
#1769=DIRECTION ( 'NONE',  ( 0.000000000000000000, -1.000000000000000000, 0.000000000000000000 ) ) ;
#1772=ORIENTED_EDGE ( 'NONE', *, *, #2131, .F. ) ;
#1773=CARTESIAN_POINT ( 'NONE',  ( 15.95292532278785913, -52.39333383871510108, 13.50000000000000000 ) ) ;
#1774=AXIS2_PLACEMENT_3D ( 'NONE', #13540, #8735, #8629 ) ;
#1778=DIRECTION ( 'NONE',  ( 1.000000000000000000, 0.000000000000000000, 0.000000000000000000 ) ) ;
#1779=ORIENTED_EDGE ( 'NONE', *, *, #20353, .T. ) ;
#1781=CARTESIAN_POINT ( 'NONE',  ( -29.13662752439705272, 5.000000000000000000, 3.799999999999999822 ) ) ;
#1786=AXIS2_PLACEMENT_3D ( 'NONE', #17650, #3920, #10738 ) ;
#1787=ORIENTED_EDGE ( 'NONE', *, *, #3300, .T. ) ;
#1789=VECTOR ( 'NONE', #8662, 1000.000000000000000 ) ;
#1790=AXIS2_PLACEMENT_3D ( 'NONE', #5118, #16740, #10042 ) ;
#1794=LINE ( 'NONE', #3143, #17287 ) ;
#1795=CARTESIAN_POINT ( 'NONE',  ( -15.12826760881917387, -51.99271056040087302, 13.49999999999999822 ) ) ;
#1797=AXIS2_PLACEMENT_3D ( 'NONE', #6787, #20531, #10233 ) ;
#1798=VERTEX_POINT ( 'NONE', #20897 ) ;
#1801=CIRCLE ( 'NONE', #14297, 0.2999999999999999334 ) ;
#1806=VERTEX_POINT ( 'NONE', #17300 ) ;
#1807=CARTESIAN_POINT ( 'NONE',  ( -25.37540678000427263, 63.74634676501045050, 13.19999999999999929 ) ) ;
#1810=ORIENTED_EDGE ( 'NONE', *, *, #19090, .T. ) ;
#1811=ORIENTED_EDGE ( 'NONE', *, *, #3064, .T. ) ;
#1813=VERTEX_POINT ( 'NONE', #8924 ) ;
#1814=AXIS2_PLACEMENT_3D ( 'NONE', #2978, #4432, #955 ) ;
#1815=CARTESIAN_POINT ( 'NONE',  ( 0.000000000000000000, 67.54634676501045476, 7.799999999999999822 ) ) ;
#1817=DIRECTION ( 'NONE',  ( -1.000000000000000000, -0.000000000000000000, 2.388292521039847891E-16 ) ) ;
#1819=ADVANCED_FACE ( 'NONE', ( #403 ), #13830, .T. ) ;
#1820=DIRECTION ( 'NONE',  ( 0.000000000000000000, 1.000000000000000000, 0.000000000000000000 ) ) ;
#1822=CARTESIAN_POINT ( 'NONE',  ( 23.04273156199906580, -2.261510999192723581, 13.21476795433022211 ) ) ;
#1823=CARTESIAN_POINT ( 'NONE',  ( 15.05486995871382483, -52.39333383871511529, 13.50000000000000178 ) ) ;
#1825=ORIENTED_EDGE ( 'NONE', *, *, #19313, .T. ) ;
#1826=VERTEX_POINT ( 'NONE', #10394 ) ;
#1829=LINE ( 'NONE', #6990, #21766 ) ;
#1831=AXIS2_PLACEMENT_3D ( 'NONE', #8472, #20673, #20455 ) ;
#1833=AXIS2_PLACEMENT_3D ( 'NONE', #13208, #9645, #792 ) ;
#1836=DIRECTION ( 'NONE',  ( -0.000000000000000000, -0.000000000000000000, -1.000000000000000000 ) ) ;
#1837=TOROIDAL_SURFACE ( 'NONE', #2913, 3.200000000000003286, 0.2999999999999999889 ) ;
#1839=AXIS2_PLACEMENT_3D ( 'NONE', #8582, #15587, #15390 ) ;
#1840=CARTESIAN_POINT ( 'NONE',  ( 9.141460742840918030, -33.43424481021354921, 7.321391277662001151 ) ) ;
#1844=EDGE_CURVE ( 'NONE', #6397, #19133, #15377, .T. ) ;
#1845=CARTESIAN_POINT ( 'NONE',  ( -14.96174975910705207, 32.10873716947361345, 13.79999999999999893 ) ) ;
#1846=FACE_OUTER_BOUND ( 'NONE', #14083, .T. ) ;
#1847=CARTESIAN_POINT ( 'NONE',  ( -15.95292532278785913, -52.11873716947361856, 13.99999999999999822 ) ) ;
#1850=DIRECTION ( 'NONE',  ( -0.000000000000000000, -0.000000000000000000, 1.000000000000000000 ) ) ;
#1851=CARTESIAN_POINT ( 'NONE',  ( 31.50000000000002132, -71.00000000000001421, 1.800000000000000044 ) ) ;
#1853=VECTOR ( 'NONE', #12677, 1000.000000000000000 ) ;
#1855=ORIENTED_EDGE ( 'NONE', *, *, #5162, .F. ) ;
#1856=CARTESIAN_POINT ( 'NONE',  ( 0.000000000000000000, 39.04634676501046187, 13.79999999999999893 ) ) ;
#1860=VECTOR ( 'NONE', #2720, 1000.000000000000000 ) ;
#1863=VERTEX_POINT ( 'NONE', #4428 ) ;
#1864=FACE_OUTER_BOUND ( 'NONE', #4723, .T. ) ;
#1865=EDGE_LOOP ( 'NONE', ( #7232, #19228, #17895, #4825 ) ) ;
#1866=DIRECTION ( 'NONE',  ( 1.000000000000000000, 0.000000000000000000, 0.000000000000000000 ) ) ;
#1867=DIRECTION ( 'NONE',  ( 0.000000000000000000, 0.000000000000000000, 1.000000000000000000 ) ) ;
#1871=CARTESIAN_POINT ( 'NONE',  ( 23.02398829872513986, 2.333317872336241994, 13.47139736055077108 ) ) ;
#1872=DIRECTION ( 'NONE',  ( -0.000000000000000000, -1.000000000000000000, 0.000000000000000000 ) ) ;
#1873=ADVANCED_FACE ( 'NONE', ( #19875 ), #19533, .T. ) ;
#1874=AXIS2_PLACEMENT_3D ( 'NONE', #19024, #7168, #20487 ) ;
#1875=DIRECTION ( 'NONE',  ( 1.000000000000000000, 0.000000000000000000, 0.000000000000000000 ) ) ;
#1880=ORIENTED_EDGE ( 'NONE', *, *, #12667, .F. ) ;
#1884=ORIENTED_EDGE ( 'NONE', *, *, #16663, .F. ) ;
#1888=ORIENTED_EDGE ( 'NONE', *, *, #17274, .T. ) ;
#1889=ORIENTED_EDGE ( 'NONE', *, *, #18507, .T. ) ;
#1891=FACE_OUTER_BOUND ( 'NONE', #3418, .T. ) ;
#1893=ADVANCED_FACE ( 'NONE', ( #10920 ), #6592, .F. ) ;
#1896=DIRECTION ( 'NONE',  ( 0.000000000000000000, 0.000000000000000000, 1.000000000000000000 ) ) ;
#1900=CARTESIAN_POINT ( 'NONE',  ( -25.37540678000427263, -69.04634676501045476, 3.799999999999999822 ) ) ;
#1905=VERTEX_POINT ( 'NONE', #12919 ) ;
#1908=CARTESIAN_POINT ( 'NONE',  ( 23.02398829872513986, -2.333487117377077258, 13.47150829744944467 ) ) ;
#1915=DIRECTION ( 'NONE',  ( -0.000000000000000000, 1.000000000000000000, 0.000000000000000000 ) ) ;
#1916=AXIS2_PLACEMENT_3D ( 'NONE', #4378, #11190, #6288 ) ;
#1917=DIRECTION ( 'NONE',  ( -1.000000000000000000, 0.000000000000000000, 0.000000000000000000 ) ) ;
#1919=ADVANCED_FACE ( 'NONE', ( #19765 ), #734, .T. ) ;
#1920=LINE ( 'NONE', #8550, #21267 ) ;
#1923=VERTEX_POINT ( 'NONE', #12808 ) ;
#1925=CARTESIAN_POINT ( 'NONE',  ( 29.50000000000002132, 0.000000000000000000, 0.2999999999999947153 ) ) ;
#1929=DIRECTION ( 'NONE',  ( -1.000000000000000000, 0.000000000000000000, 0.000000000000000000 ) ) ;
#1930=EDGE_CURVE ( 'NONE', #13182, #16858, #10164, .T. ) ;
#1931=DIRECTION ( 'NONE',  ( 1.000000000000000000, 0.000000000000000000, 0.000000000000000000 ) ) ;
#1932=CARTESIAN_POINT ( 'NONE',  ( -27.37540678000428684, -36.74634676501047181, 42.50000000000000000 ) ) ;
#1933=EDGE_LOOP ( 'NONE', ( #3491, #17075, #13880, #12624 ) ) ;
#1935=DIRECTION ( 'NONE',  ( -1.000000000000000000, 0.000000000000000000, 0.000000000000000000 ) ) ;
#1936=EDGE_CURVE ( 'NONE', #21299, #16033, #147, .T. ) ;
#1940=CARTESIAN_POINT ( 'NONE',  ( 14.96174975910707161, -51.61873716947361856, 68.25000000000000000 ) ) ;
#1941=ORIENTED_EDGE ( 'NONE', *, *, #15522, .T. ) ;
#1943=DIRECTION ( 'NONE',  ( 1.000000000000000000, 0.000000000000000000, 0.000000000000000000 ) ) ;
#1944=CARTESIAN_POINT ( 'NONE',  ( -15.21174975910705207, -51.61873716947361856, 14.00000000000000000 ) ) ;
#1946=AXIS2_PLACEMENT_3D ( 'NONE', #14165, #4107, #20902 ) ;
#1950=CARTESIAN_POINT ( 'NONE',  ( 0.000000000000000000, -32.11873716947361856, 109.6002446535588319 ) ) ;
#1951=DIRECTION ( 'NONE',  ( 0.000000000000000000, 0.000000000000000000, 1.000000000000000000 ) ) ;
#1953=CARTESIAN_POINT ( 'NONE',  ( 4.127054932750481520, 32.93424481021354921, 68.50000000000000000 ) ) ;
#1956=CARTESIAN_POINT ( 'NONE',  ( 14.96174975910705918, -51.86873716947361856, 14.00000000000000000 ) ) ;
#1961=VECTOR ( 'NONE', #1171, 1000.000000000000000 ) ;
#1962=CARTESIAN_POINT ( 'NONE',  ( -29.13662752439705272, -5.299999999999999822, 7.500000000000000000 ) ) ;
#1964=CARTESIAN_POINT ( 'NONE',  ( 23.02398829872513986, 2.157133865693446229, 13.26854876702554265 ) ) ;
#1966=ADVANCED_FACE ( 'NONE', ( #6574 ), #5524, .T. ) ;
#1967=EDGE_CURVE ( 'NONE', #14977, #8429, #3018, .T. ) ;
#1968=DIRECTION ( 'NONE',  ( 0.000000000000000000, 0.000000000000000000, -1.000000000000000000 ) ) ;
#1969=DIRECTION ( 'NONE',  ( -1.000000000000000000, 0.000000000000000000, 0.000000000000000000 ) ) ;
#1974=DIRECTION ( 'NONE',  ( 0.000000000000000000, -1.000000000000000000, 0.000000000000000000 ) ) ;
#1979=LINE ( 'NONE', #4112, #6386 ) ;
#1980=AXIS2_PLACEMENT_3D ( 'NONE', #20327, #17069, #4881 ) ;
#1982=VECTOR ( 'NONE', #17195, 1000.000000000000000 ) ;
#1983=EDGE_CURVE ( 'NONE', #6378, #22039, #2291, .T. ) ;
#1984=ORIENTED_EDGE ( 'NONE', *, *, #7152, .T. ) ;
#1987=CARTESIAN_POINT ( 'NONE',  ( 25.37540678000427263, -63.74634676501045050, 13.50000000000000000 ) ) ;
#1989=AXIS2_PLACEMENT_3D ( 'NONE', #5088, #3399, #15371 ) ;
#1990=VECTOR ( 'NONE', #2138, 1000.000000000000000 ) ;
#1991=CARTESIAN_POINT ( 'NONE',  ( 15.21174975910707161, 51.61873716947361856, 68.00000000000000000 ) ) ;
#1992=CARTESIAN_POINT ( 'NONE',  ( -1.836970198721029934E-16, 71.70000000000001705, 3.200000000000000178 ) ) ;
#1995=ORIENTED_EDGE ( 'NONE', *, *, #8002, .F. ) ;
#1996=CARTESIAN_POINT ( 'NONE',  ( 29.33506712743370315, 2.703525840380863521, 0.02198462118690103911 ) ) ;
#1998=AXIS2_PLACEMENT_3D ( 'NONE', #16474, #18152, #2839 ) ;
#2004=CARTESIAN_POINT ( 'NONE',  ( -14.66174954725422630, 51.84669727004962425, 13.50000000000000000 ) ) ;
#2007=ORIENTED_EDGE ( 'NONE', *, *, #15662, .T. ) ;
#2009=EDGE_LOOP ( 'NONE', ( #18116, #12795, #5612, #15564 ) ) ;
#2010=LINE ( 'NONE', #5617, #18169 ) ;
#2015=CARTESIAN_POINT ( 'NONE',  ( 23.18284705826588876, -2.947275247953580202, 13.45749238763921340 ) ) ;
#2016=ORIENTED_EDGE ( 'NONE', *, *, #7943, .T. ) ;
#2017=ORIENTED_EDGE ( 'NONE', *, *, #17977, .F. ) ;
#2019=DIRECTION ( 'NONE',  ( 0.000000000000000000, 1.000000000000000000, 0.000000000000000000 ) ) ;
#2020=DIRECTION ( 'NONE',  ( 0.000000000000000000, -1.000000000000000000, -0.000000000000000000 ) ) ;
#2023=CIRCLE ( 'NONE', #1304, 1.000000000000000000 ) ;
#2027=CARTESIAN_POINT ( 'NONE',  ( -23.02398829872501906, 2.246571036181109982, 13.29719918165967840 ) ) ;
#2030=CARTESIAN_POINT ( 'NONE',  ( 14.90249074642385807, -52.32070855895314310, 13.50000000000000355 ) ) ;
#2031=AXIS2_PLACEMENT_3D ( 'NONE', #17973, #14830, #2886 ) ;
#2034=EDGE_LOOP ( 'NONE', ( #7361, #18472, #3738, #4778 ) ) ;
#2035=LINE ( 'NONE', #20957, #3148 ) ;
#2039=VECTOR ( 'NONE', #3242, 1000.000000000000000 ) ;
#2042=CIRCLE ( 'NONE', #1326, 0.6999999999999992895 ) ;
#2043=EDGE_CURVE ( 'NONE', #8135, #1711, #1571, .T. ) ;
#2046=DIRECTION ( 'NONE',  ( -0.000000000000000000, -0.000000000000000000, -1.000000000000000000 ) ) ;
#2047=DIRECTION ( 'NONE',  ( 0.000000000000000000, 0.000000000000000000, 1.000000000000000000 ) ) ;
#2048=ORIENTED_EDGE ( 'NONE', *, *, #2373, .F. ) ;
#2049=DIRECTION ( 'NONE',  ( 0.000000000000000000, 0.000000000000000000, 1.000000000000000000 ) ) ;
#2053=CARTESIAN_POINT ( 'NONE',  ( -14.66174975910705136, 51.76873716947361714, 13.50000000000000000 ) ) ;
#2054=AXIS2_PLACEMENT_3D ( 'NONE', #751, #11158, #12602 ) ;
#2055=AXIS2_PLACEMENT_3D ( 'NONE', #17648, #2552, #3918 ) ;
#2056=AXIS2_PLACEMENT_3D ( 'NONE', #20807, #12160, #15846 ) ;
#2058=ORIENTED_EDGE ( 'NONE', *, *, #14084, .F. ) ;
#2059=DIRECTION ( 'NONE',  ( 0.000000000000000000, -1.000000000000000000, 0.000000000000000000 ) ) ;
#2061=AXIS2_PLACEMENT_3D ( 'NONE', #7276, #17554, #19124 ) ;
#2064=ORIENTED_EDGE ( 'NONE', *, *, #12333, .F. ) ;
#2065=ORIENTED_EDGE ( 'NONE', *, *, #12737, .T. ) ;
#2067=ORIENTED_EDGE ( 'NONE', *, *, #6555, .F. ) ;
#2071=CARTESIAN_POINT ( 'NONE',  ( -29.50000000000002132, 0.000000000000000000, -150.0833101980363722 ) ) ;
#2073=ADVANCED_FACE ( 'NONE', ( #18739 ), #12989, .T. ) ;
#2074=ORIENTED_EDGE ( 'NONE', *, *, #5013, .T. ) ;
#2076=CIRCLE ( 'NONE', #16717, 6.499999999999999112 ) ;
#2078=VERTEX_POINT ( 'NONE', #15385 ) ;
#2079=DIRECTION ( 'NONE',  ( 1.000000000000000000, 0.000000000000000000, 0.000000000000000000 ) ) ;
#2080=CARTESIAN_POINT ( 'NONE',  ( 15.95292532278785913, -52.39333383871510108, 13.79999999999999893 ) ) ;
#2085=VERTEX_POINT ( 'NONE', #18298 ) ;
#2087=VECTOR ( 'NONE', #14409, 1000.000000000000000 ) ;
#2088=CARTESIAN_POINT ( 'NONE',  ( 8.641460742840918030, -33.43424481021354921, 68.00000000000000000 ) ) ;
#2093=EDGE_CURVE ( 'NONE', #3329, #19467, #5664, .T. ) ;
#2096=DIRECTION ( 'NONE',  ( 1.000000000000000000, 2.832483164223420229E-16, 0.000000000000000000 ) ) ;
#2098=ORIENTED_EDGE ( 'NONE', *, *, #3725, .F. ) ;
#2103=VERTEX_POINT ( 'NONE', #3975 ) ;
#2104=AXIS2_PLACEMENT_3D ( 'NONE', #11045, #19891, #17753 ) ;
#2105=ADVANCED_FACE ( 'NONE', ( #1846 ), #17270, .F. ) ;
#2108=VERTEX_POINT ( 'NONE', #262 ) ;
#2109=ORIENTED_EDGE ( 'NONE', *, *, #20482, .T. ) ;
#2110=DIRECTION ( 'NONE',  ( -0.000000000000000000, -0.000000000000000000, -1.000000000000000000 ) ) ;
#2112=CARTESIAN_POINT ( 'NONE',  ( -8.641460742840918030, -32.93424481021354921, 7.321391277662001151 ) ) ;
#2113=CARTESIAN_POINT ( 'NONE',  ( 29.13662752439705272, -5.299999999999999822, 7.200000000000000178 ) ) ;
#2114=AXIS2_PLACEMENT_3D ( 'NONE', #5387, #12612, #13967 ) ;
#2115=CYLINDRICAL_SURFACE ( 'NONE', #5635, 0.5000000000000000000 ) ;
#2116=ORIENTED_EDGE ( 'NONE', *, *, #16280, .F. ) ;
#2117=CARTESIAN_POINT ( 'NONE',  ( -18.05178606074127501, 38.87061083372239523, 13.49999999999999822 ) ) ;
#2118=EDGE_CURVE ( 'NONE', #21063, #10017, #19447, .T. ) ;
#2121=ORIENTED_EDGE ( 'NONE', *, *, #16881, .F. ) ;
#2123=VECTOR ( 'NONE', #7005, 1000.000000000000000 ) ;
#2129=ORIENTED_EDGE ( 'NONE', *, *, #8000, .F. ) ;
#2131=EDGE_CURVE ( 'NONE', #9554, #10005, #10718, .T. ) ;
#2134=CARTESIAN_POINT ( 'NONE',  ( 32.20000000000001705, 71.00000000000001421, 1.500000000000000000 ) ) ;
#2138=DIRECTION ( 'NONE',  ( -2.832483164223434527E-16, 1.000000000000000000, 0.000000000000000000 ) ) ;
#2139=CARTESIAN_POINT ( 'NONE',  ( 14.66174975910705847, -42.11054587065083155, 13.50000000000000000 ) ) ;
#2144=CARTESIAN_POINT ( 'NONE',  ( -23.02398829872513986, 2.388718329487966585, 13.39778868030486514 ) ) ;
#2145=CARTESIAN_POINT ( 'NONE',  ( 27.37540678000427619, 7.754037881813018962E-15, 42.50000000000000000 ) ) ;
#2146=CARTESIAN_POINT ( 'NONE',  ( 23.32398829872514412, -3.528912754968634768, 13.50000000000000000 ) ) ;
#2148=EDGE_CURVE ( 'NONE', #7257, #15319, #6807, .T. ) ;
#2150=ORIENTED_EDGE ( 'NONE', *, *, #1136, .F. ) ;
#2151=ORIENTED_EDGE ( 'NONE', *, *, #6149, .F. ) ;
#2152=CARTESIAN_POINT ( 'NONE',  ( 27.77120804565220169, -2.094189496455408861, 1.500000000000000666 ) ) ;
#2153=SHAPE_REPRESENTATION_RELATIONSHIP ( 'NONE' , 'NONE' ,  #9407, #7548 ) ;
#2155=ORIENTED_EDGE ( 'NONE', *, *, #20663, .T. ) ;
#2156=ORIENTED_EDGE ( 'NONE', *, *, #100, .T. ) ;
#2157=EDGE_CURVE ( 'NONE', #1357, #13818, #20974, .T. ) ;
#2158=AXIS2_PLACEMENT_3D ( 'NONE', #17896, #9406, #19700 ) ;
#2159=CIRCLE ( 'NONE', #8244, 1.000000000000000888 ) ;
#2161=CARTESIAN_POINT ( 'NONE',  ( 32.50000000000002132, -71.00000000000001421, 1.800000000000000044 ) ) ;
#2163=DIRECTION ( 'NONE',  ( 1.000000000000000000, 0.000000000000000000, 0.000000000000000000 ) ) ;
#2164=PLANE ( 'NONE',  #5351 ) ;
#2166=DIRECTION ( 'NONE',  ( 1.000000000000000000, 0.000000000000000000, 0.000000000000000000 ) ) ;
#2169=CARTESIAN_POINT ( 'NONE',  ( -3.127054932750481964, 32.61873716947361856, 68.50000000000000000 ) ) ;
#2172=CIRCLE ( 'NONE', #2529, 0.2500000000000002220 ) ;
#2173=DIRECTION ( 'NONE',  ( 0.000000000000000000, 0.000000000000000000, 1.000000000000000000 ) ) ;
#2176=ADVANCED_FACE ( 'NONE', ( #20653 ), #8896, .T. ) ;
#2177=EDGE_LOOP ( 'NONE', ( #13663, #12113, #12764, #7426 ) ) ;
#2178=ORIENTED_EDGE ( 'NONE', *, *, #2506, .F. ) ;
#2179=VERTEX_POINT ( 'NONE', #15583 ) ;
#2180=LINE ( 'NONE', #19411, #8851 ) ;
#2181=CARTESIAN_POINT ( 'NONE',  ( -23.02398829872513986, 7.027230193580998154E-15, 42.50000000000000000 ) ) ;
#2182=FACE_OUTER_BOUND ( 'NONE', #14690, .T. ) ;
#2183=ORIENTED_EDGE ( 'NONE', *, *, #4758, .F. ) ;
#2187=AXIS2_PLACEMENT_3D ( 'NONE', #9890, #18039, #18377 ) ;
#2190=CARTESIAN_POINT ( 'NONE',  ( 15.95292532278785913, -50.11873716947361856, 68.00000000000000000 ) ) ;
#2193=AXIS2_PLACEMENT_3D ( 'NONE', #12575, #5565, #20887 ) ;
#2195=DIRECTION ( 'NONE',  ( 0.000000000000000000, 0.000000000000000000, -1.000000000000000000 ) ) ;
#2196=CARTESIAN_POINT ( 'NONE',  ( 25.37540678000427263, -67.24634676501045760, 7.799999999999999822 ) ) ;
#2197=ORIENTED_EDGE ( 'NONE', *, *, #16341, .F. ) ;
#2198=DIRECTION ( 'NONE',  ( -0.000000000000000000, 0.000000000000000000, -1.000000000000000000 ) ) ;
#2199=CARTESIAN_POINT ( 'NONE',  ( -8.641460742840918030, -32.93424481021354921, 68.50000000000000000 ) ) ;
#2202=ORIENTED_EDGE ( 'NONE', *, *, #21718, .F. ) ;
#2203=FACE_OUTER_BOUND ( 'NONE', #16007, .T. ) ;
#2205=EDGE_CURVE ( 'NONE', #13894, #10046, #9649, .T. ) ;
#2208=AXIS2_PLACEMENT_3D ( 'NONE', #7099, #18607, #6653 ) ;
#2211=VERTEX_POINT ( 'NONE', #17380 ) ;
#2212=VERTEX_POINT ( 'NONE', #7225 ) ;
#2213=DIRECTION ( 'NONE',  ( 0.000000000000000000, 0.000000000000000000, -1.000000000000000000 ) ) ;
#2215=EDGE_LOOP ( 'NONE', ( #591, #18324, #11991, #10747 ) ) ;
#2220=AXIS2_PLACEMENT_3D ( 'NONE', #1422, #20020, #4687 ) ;
#2221=CARTESIAN_POINT ( 'NONE',  ( -3.627054932750481964, -33.43424481021354921, 68.00000000000000000 ) ) ;
#2222=DIRECTION ( 'NONE',  ( 0.000000000000000000, 1.000000000000000000, -0.000000000000000000 ) ) ;
#2225=DIRECTION ( 'NONE',  ( 1.000000000000000000, 0.000000000000000000, 0.000000000000000000 ) ) ;
#2226=ADVANCED_FACE ( 'NONE', ( #3861 ), #1053, .T. ) ;
#2227=PLANE ( 'NONE',  #6244 ) ;
#2228=ADVANCED_FACE ( 'NONE', ( #21098 ), #8570, .F. ) ;
#2230=VERTEX_POINT ( 'NONE', #703 ) ;
#2231=CIRCLE ( 'NONE', #20108, 6.499999999999999112 ) ;
#2234=AXIS2_PLACEMENT_3D ( 'NONE', #2307, #15941, #626 ) ;
#2236=DIRECTION ( 'NONE',  ( 1.000000000000000000, 0.000000000000000000, 0.000000000000000000 ) ) ;
#2239=ORIENTED_EDGE ( 'NONE', *, *, #13708, .T. ) ;
#2240=EDGE_CURVE ( 'NONE', #6576, #10531, #21441, .T. ) ;
#2241=CARTESIAN_POINT ( 'NONE',  ( 23.02398829872478814, -2.211005313988728016, 13.25071573983089834 ) ) ;
#2242=VERTEX_POINT ( 'NONE', #21205 ) ;
#2244=FACE_OUTER_BOUND ( 'NONE', #3294, .T. ) ;
#2247=CARTESIAN_POINT ( 'NONE',  ( 25.37540678000427263, -63.74634676501045050, 7.200000000000000178 ) ) ;
#2251=CARTESIAN_POINT ( 'NONE',  ( 28.79994065384636315, 6.566898051583388352, 13.40260211333369256 ) ) ;
#2252=EDGE_CURVE ( 'NONE', #17256, #21160, #15598, .T. ) ;
#2255=FACE_OUTER_BOUND ( 'NONE', #15549, .T. ) ;
#2256=EDGE_CURVE ( 'NONE', #17559, #19811, #777, .T. ) ;
#2257=LINE ( 'NONE', #10544, #16014 ) ;
#2258=VERTEX_POINT ( 'NONE', #5623 ) ;
#2259=ORIENTED_EDGE ( 'NONE', *, *, #22111, .T. ) ;
#2260=CARTESIAN_POINT ( 'NONE',  ( 0.000000000000000000, -5.299999999999999822, 7.200000000000000178 ) ) ;
#2265=ADVANCED_FACE ( 'NONE', ( #5400 ), #16115, .F. ) ;
#2266=CARTESIAN_POINT ( 'NONE',  ( -25.37540678000427263, -63.74634676501045050, 3.799999999999999822 ) ) ;
#2267=( BOUNDED_SURFACE ( )  B_SPLINE_SURFACE ( 3, 2, ( 
 ( #21869, #1585, #11878 ),
 ( #1369, #8321, #8420 ),
 ( #15239, #13568, #8217 ),
 ( #13670, #18829, #6551 ),
 ( #20174, #4842, #11653 ),
 ( #12300, #681, #12424 ),
 ( #14221, #10539, #15677 ),
 ( #454, #2144, #5636 ),
 ( #10866, #17249, #19274 ),
 ( #17680, #2027, #10657 ),
 ( #5413, #10441, #14329 ),
 ( #15556, #20738, #16002 ) ),
 .UNSPECIFIED., .F., .F., .F. ) 
 B_SPLINE_SURFACE_WITH_KNOTS ( ( 4, 2, 2, 2, 2, 4 ),
 ( 3, 3 ),
 ( 0.0006083281319963878804, 0.001004469391314931435, 0.001400610650633475097, 0.001796751909952018760, 0.001994822539611290808, 0.002192893169270562423 ),
 ( 0.000000000000000000, 1.000000000000000000 ),
 .UNSPECIFIED. ) 
 GEOMETRIC_REPRESENTATION_ITEM ( )  RATIONAL_B_SPLINE_SURFACE ( (
 ( 1.000000000000000000, 0.7071067811865475727, 1.000000000000000000),
 ( 1.000000000000000000, 0.7419362082869511710, 1.000000000000000000),
 ( 1.000000000000000000, 0.7734000586050161496, 1.000000000000000000),
 ( 1.000000000000000000, 0.8313348272087629498, 1.000000000000000000),
 ( 1.000000000000000000, 0.8578042680912283391, 1.000000000000000000),
 ( 1.000000000000000000, 0.9064979099737326962, 1.000000000000000000),
 ( 1.000000000000000000, 0.9284078965777999848, 1.000000000000000000),
 ( 1.000000000000000000, 0.9565959158316897915, 1.000000000000000000),
 ( 1.000000000000000000, 0.9652268734598790090, 1.000000000000000000),
 ( 1.000000000000000000, 0.9789818400845240465, 1.000000000000000000),
 ( 1.000000000000000000, 0.9843224408025279537, 1.000000000000000000),
 ( 1.000000000000000000, 0.9842566880020492404, 1.000000000000000000) ) ) 
 REPRESENTATION_ITEM ( '' )  SURFACE ( )  );
#2268=CYLINDRICAL_SURFACE ( 'NONE', #13076, 0.2999999999999999334 ) ;
#2270=DIRECTION ( 'NONE',  ( 0.000000000000000000, 0.000000000000000000, 1.000000000000000000 ) ) ;
#2271=CARTESIAN_POINT ( 'NONE',  ( 23.11743451022278251, 2.646042693280193703, 13.40127653599240531 ) ) ;
#2272=CARTESIAN_POINT ( 'NONE',  ( 15.21174975910707161, -42.31054587065082728, 68.50000000000000000 ) ) ;
#2273=EDGE_CURVE ( 'NONE', #4102, #17715, #4043, .T. ) ;
#2275=DIRECTION ( 'NONE',  ( 0.000000000000000000, 0.000000000000000000, 1.000000000000000000 ) ) ;
#2276=CARTESIAN_POINT ( 'NONE',  ( -29.13662752439705272, -5.000000000000000000, 3.799999999999999822 ) ) ;
#2278=AXIS2_PLACEMENT_3D ( 'NONE', #12252, #625, #12358 ) ;
#2280=CARTESIAN_POINT ( 'NONE',  ( -29.13662752439705272, -5.000000000000000000, 7.500000000000000000 ) ) ;
#2283=ORIENTED_EDGE ( 'NONE', *, *, #8754, .T. ) ;
#2284=ORIENTED_EDGE ( 'NONE', *, *, #20612, .T. ) ;
#2285=CARTESIAN_POINT ( 'NONE',  ( 27.69541703706358504, -2.215671135867736119, 0.03255948639529124972 ) ) ;
#2286=DIRECTION ( 'NONE',  ( -1.000000000000000000, 0.000000000000000000, 0.000000000000000000 ) ) ;
#2287=ORIENTED_EDGE ( 'NONE', *, *, #7882, .F. ) ;
#2288=CIRCLE ( 'NONE', #14788, 0.5000000000000004441 ) ;
#2289=DIRECTION ( 'NONE',  ( 0.000000000000000000, 0.000000000000000000, 1.000000000000000000 ) ) ;
#2291=CIRCLE ( 'NONE', #2645, 0.2500000000000002220 ) ;
#2292=EDGE_LOOP ( 'NONE', ( #19235, #14828, #13607, #6975, #2767, #19204, #20216, #13606, #10636, #16852, #6582, #4263, #3988, #4387, #9907, #16735, #7318, #3557, #13548, #20008, #19285 ) ) ;
#2293=DIRECTION ( 'NONE',  ( -1.000000000000000000, 0.000000000000000000, 0.000000000000000000 ) ) ;
#2295=EDGE_CURVE ( 'NONE', #14227, #852, #5512, .T. ) ;
#2296=VERTEX_POINT ( 'NONE', #7188 ) ;
#2298=EDGE_CURVE ( 'NONE', #1170, #8695, #13984, .T. ) ;
#2299=DIRECTION ( 'NONE',  ( 0.000000000000000000, 0.000000000000000000, 1.000000000000000000 ) ) ;
#2300=B_SPLINE_CURVE_WITH_KNOTS ( 'NONE', 3,
 ( #17616, #384, #3755, #2285, #7457, #7562 ),
 .UNSPECIFIED., .F., .F.,
 ( 4, 2, 4 ),
 ( 3.442662021193151749E-18, 0.0002343895398574032151, 0.0004687790797148030150 ),
 .UNSPECIFIED. ) ;
#2301=CYLINDRICAL_SURFACE ( 'NONE', #13994, 0.2999999999999999334 ) ;
#2306=CARTESIAN_POINT ( 'NONE',  ( -26.37540678000427619, -10.94079601157914716, 42.50000000000000000 ) ) ;
#2307=CARTESIAN_POINT ( 'NONE',  ( 27.67540678000428400, -36.74634676501047181, 13.79999999999999893 ) ) ;
#2312=EDGE_LOOP ( 'NONE', ( #21198, #12646, #9893, #7341 ) ) ;
#2313=DIRECTION ( 'NONE',  ( 0.000000000000000000, 1.000000000000000000, 0.000000000000000000 ) ) ;
#2315=ORIENTED_EDGE ( 'NONE', *, *, #1416, .T. ) ;
#2316=ORIENTED_EDGE ( 'NONE', *, *, #17890, .F. ) ;
#2317=DIRECTION ( 'NONE',  ( -0.000000000000000000, 1.000000000000000000, 0.000000000000000000 ) ) ;
#2318=FACE_OUTER_BOUND ( 'NONE', #11703, .T. ) ;
#2319=VERTEX_POINT ( 'NONE', #17669 ) ;
#2320=VERTEX_POINT ( 'NONE', #2134 ) ;
#2321=AXIS2_PLACEMENT_3D ( 'NONE', #7261, #5053, #19333 ) ;
#2325=DIRECTION ( 'NONE',  ( 1.000000000000000000, 0.000000000000000000, 0.000000000000000000 ) ) ;
#2333=DIRECTION ( 'NONE',  ( 1.000000000000000000, 0.000000000000000000, 0.000000000000000000 ) ) ;
#2335=AXIS2_PLACEMENT_3D ( 'NONE', #1746, #18632, #6681 ) ;
#2336=( GEOMETRIC_REPRESENTATION_CONTEXT ( 3 ) GLOBAL_UNCERTAINTY_ASSIGNED_CONTEXT ( ( #16464 ) ) GLOBAL_UNIT_ASSIGNED_CONTEXT ( ( #4219, #11038, #2638 ) ) REPRESENTATION_CONTEXT ( 'NONE', 'WORKASPACE' ) );
#2342=EDGE_LOOP ( 'NONE', ( #7454, #1231, #691, #11678, #15285, #9026, #12456, #21836, #19722, #10350, #14459, #1855 ) ) ;
#2343=CARTESIAN_POINT ( 'NONE',  ( 17.95292532278785913, 34.11873716947361856, 42.50000000000000711 ) ) ;
#2344=ORIENTED_EDGE ( 'NONE', *, *, #1542, .F. ) ;
#2345=EDGE_LOOP ( 'NONE', ( #2284, #16505, #8213, #19046 ) ) ;
#2347=EDGE_CURVE ( 'NONE', #4007, #19672, #16318, .T. ) ;
#2348=CARTESIAN_POINT ( 'NONE',  ( 23.13130088652697225, -2.712279394122553366, 13.41537141447308379 ) ) ;
#2349=ORIENTED_EDGE ( 'NONE', *, *, #7933, .T. ) ;
#2352=AXIS2_PLACEMENT_3D ( 'NONE', #12890, #4402, #7893 ) ;
#2354=LINE ( 'NONE', #8972, #8802 ) ;
#2355=DIRECTION ( 'NONE',  ( 0.000000000000000000, 0.000000000000000000, 1.000000000000000000 ) ) ;
#2357=DIRECTION ( 'NONE',  ( 0.000000000000000000, 0.000000000000000000, 1.000000000000000000 ) ) ;
#2358=DIRECTION ( 'NONE',  ( 0.000000000000000000, 0.000000000000000000, 1.000000000000000000 ) ) ;
#2359=DIRECTION ( 'NONE',  ( 0.000000000000000000, -1.000000000000000000, 0.000000000000000000 ) ) ;
#2360=CARTESIAN_POINT ( 'NONE',  ( -29.13662752439705272, 0.000000000000000000, 0.3000000000000016542 ) ) ;
#2361=DIRECTION ( 'NONE',  ( -0.000000000000000000, -1.000000000000000000, -0.000000000000000000 ) ) ;
#2363=AXIS2_PLACEMENT_3D ( 'NONE', #21658, #7669, #1156 ) ;
#2365=EDGE_CURVE ( 'NONE', #19005, #20280, #997, .T. ) ;
#2366=EDGE_LOOP ( 'NONE', ( #5505, #10928, #15389, #10607 ) ) ;
#2367=CIRCLE ( 'NONE', #10608, 0.5000000000000004441 ) ;
#2368=CARTESIAN_POINT ( 'NONE',  ( 28.87540678000427619, 6.494748934539263274, 7.799999999999999822 ) ) ;
#2372=EDGE_CURVE ( 'NONE', #7310, #12793, #3657, .T. ) ;
#2373=EDGE_CURVE ( 'NONE', #13948, #18889, #10442, .T. ) ;
#2378=CYLINDRICAL_SURFACE ( 'NONE', #19245, 0.2500000000000002220 ) ;
#2379=DIRECTION ( 'NONE',  ( -0.000000000000000000, -0.000000000000000000, -1.000000000000000000 ) ) ;
#2380=CIRCLE ( 'NONE', #18833, 1.000000000000000888 ) ;
#2381=VERTEX_POINT ( 'NONE', #6066 ) ;
#2383=CARTESIAN_POINT ( 'NONE',  ( 23.32398829872514057, 3.528912754968628551, 13.50000000000000000 ) ) ;
#2385=CARTESIAN_POINT ( 'NONE',  ( 15.00584427753688921, 51.86868465798484351, 13.49999999999999645 ) ) ;
#2386=CARTESIAN_POINT ( 'NONE',  ( -30.67540678000428045, 6.000000000000000000, 3.500000000000000000 ) ) ;
#2392=VECTOR ( 'NONE', #20192, 1000.000000000000000 ) ;
#2393=CARTESIAN_POINT ( 'NONE',  ( 4.127054932750481520, 32.93424481021354921, 7.321391277662001151 ) ) ;
#2394=VERTEX_POINT ( 'NONE', #19698 ) ;
#2395=CIRCLE ( 'NONE', #16685, 2.800000000000003819 ) ;
#2396=CIRCLE ( 'NONE', #15594, 3.500000000000003109 ) ;
#2398=ORIENTED_EDGE ( 'NONE', *, *, #10800, .T. ) ;
#2399=CARTESIAN_POINT ( 'NONE',  ( -29.17540678000427690, -6.499884319688664647, 7.500000000000000000 ) ) ;
#2401=EDGE_LOOP ( 'NONE', ( #5803, #441, #4168, #11659 ) ) ;
#2402=VECTOR ( 'NONE', #19412, 1000.000000000000000 ) ;
#2404=EDGE_CURVE ( 'NONE', #7401, #9771, #16204, .T. ) ;
#2405=EDGE_CURVE ( 'NONE', #17841, #2078, #2914, .T. ) ;
#2406=ORIENTED_EDGE ( 'NONE', *, *, #17159, .F. ) ;
#2408=( BOUNDED_SURFACE ( )  B_SPLINE_SURFACE ( 3, 2, ( 
 ( #13740, #17003, #20600 ),
 ( #16662, #18689, #18349 ),
 ( #15001, #1675, #9974 ),
 ( #8518, #3476, #16784 ),
 ( #15333, #6623, #8298 ),
 ( #1453, #1795, #16897 ),
 ( #15102, #13422, #4936 ),
 ( #4, #8632, #6858 ) ),
 .UNSPECIFIED., .F., .F., .F. ) 
 B_SPLINE_SURFACE_WITH_KNOTS ( ( 4, 2, 2, 4 ),
 ( 3, 3 ),
 ( -1.016439536705160407E-20, 0.0002312589012449743479, 0.0004625178024899486958, 0.0009250356049798973915 ),
 ( 0.000000000000000000, 1.000000000000000000 ),
 .UNSPECIFIED. ) 
 GEOMETRIC_REPRESENTATION_ITEM ( )  RATIONAL_B_SPLINE_SURFACE ( (
 ( 1.000000000000000000, 0.7071067811865475727, 1.000000000000000000),
 ( 1.000000000000000000, 0.6819975405126383894, 1.000000000000000000),
 ( 1.000000000000000000, 0.6638073299468163491, 1.000000000000000000),
 ( 1.000000000000000000, 0.6387680821201728865, 1.000000000000000000),
 ( 1.000000000000000000, 0.6313903660824350395, 1.000000000000000000),
 ( 1.000000000000000000, 0.6152524581541630733, 1.000000000000000000),
 ( 1.000000000000000000, 0.6128152994388438302, 1.000000000000000000),
 ( 1.000000000000000000, 0.6123724356957929160, 1.000000000000000000) ) ) 
 REPRESENTATION_ITEM ( '' )  SURFACE ( )  );
#2409=CARTESIAN_POINT ( 'NONE',  ( 15.21174975910707161, 41.81054587065082728, 68.25000000000000000 ) ) ;
#2412=CARTESIAN_POINT ( 'NONE',  ( 15.95292532278785913, 50.11873716947361856, 13.79999999999999893 ) ) ;
#2413=AXIS2_PLACEMENT_3D ( 'NONE', #9609, #6150, #6371 ) ;
#2416=FACE_OUTER_BOUND ( 'NONE', #13489, .T. ) ;
#2418=ORIENTED_EDGE ( 'NONE', *, *, #4834, .F. ) ;
#2420=CARTESIAN_POINT ( 'NONE',  ( 14.96174975910705918, -51.86873716947361856, 14.00000000000000000 ) ) ;
#2423=DIRECTION ( 'NONE',  ( 1.000000000000000000, 0.000000000000000000, 0.000000000000000000 ) ) ;
#2425=CARTESIAN_POINT ( 'NONE',  ( -23.32398829872514057, 7.118794219358020148E-15, 13.79999999999999893 ) ) ;
#2426=VECTOR ( 'NONE', #9563, 1000.000000000000000 ) ;
#2430=CARTESIAN_POINT ( 'NONE',  ( -23.02398829872513275, -3.002822642624744631, 13.75715867294163353 ) ) ;
#2431=ORIENTED_EDGE ( 'NONE', *, *, #17254, .F. ) ;
#2432=ORIENTED_EDGE ( 'NONE', *, *, #3274, .T. ) ;
#2435=ADVANCED_FACE ( 'NONE', ( #19931 ), #4595, .T. ) ;
#2436=DIRECTION ( 'NONE',  ( 0.000000000000000000, 0.000000000000000000, 1.000000000000000000 ) ) ;
#2439=ORIENTED_EDGE ( 'NONE', *, *, #11128, .T. ) ;
#2441=ORIENTED_EDGE ( 'NONE', *, *, #765, .T. ) ;
#2442=AXIS2_PLACEMENT_3D ( 'NONE', #7208, #19282, #3959 ) ;
#2446=CARTESIAN_POINT ( 'NONE',  ( -29.13662752439705272, 0.000000000000000000, 13.19999999999999929 ) ) ;
#2448=DIRECTION ( 'NONE',  ( -0.000000000000000000, 1.000000000000000000, -0.000000000000000000 ) ) ;
#2449=CARTESIAN_POINT ( 'NONE',  ( -25.37540678000427263, 68.74634676501045760, 3.799999999999999822 ) ) ;
#2452=AXIS2_PLACEMENT_3D ( 'NONE', #4676, #14391, #7929 ) ;
#2453=CARTESIAN_POINT ( 'NONE',  ( 14.66918480534031666, 51.92478805997377123, 13.49999999999999645 ) ) ;
#2459=EDGE_LOOP ( 'NONE', ( #19977, #1433, #19535, #7625 ) ) ;
#2461=ORIENTED_EDGE ( 'NONE', *, *, #10506, .F. ) ;
#2462=ORIENTED_EDGE ( 'NONE', *, *, #7530, .T. ) ;
#2463=DIRECTION ( 'NONE',  ( 0.000000000000000000, 0.000000000000000000, 1.000000000000000000 ) ) ;
#2466=CIRCLE ( 'NONE', #9259, 0.5000000000000004441 ) ;
#2467=VERTEX_POINT ( 'NONE', #21997 ) ;
#2471=AXIS2_PLACEMENT_3D ( 'NONE', #16263, #947, #14604 ) ;
#2472=ORIENTED_EDGE ( 'NONE', *, *, #11020, .F. ) ;
#2474=CARTESIAN_POINT ( 'NONE',  ( 15.95292532278785913, -32.11873716947361856, 42.50000000000000711 ) ) ;
#2477=ADVANCED_FACE ( 'NONE', ( #5208 ), #8342, .T. ) ;
#2478=CARTESIAN_POINT ( 'NONE',  ( 15.21174975910707161, 42.11054587065083155, 13.50000000000000000 ) ) ;
#2480=DIRECTION ( 'NONE',  ( 0.000000000000000000, 0.000000000000000000, 1.000000000000000000 ) ) ;
#2482=ADVANCED_FACE ( 'NONE', ( #13363 ), #13690, .F. ) ;
#2485=CIRCLE ( 'NONE', #21091, 0.5000000000000004441 ) ;
#2488=ORIENTED_EDGE ( 'NONE', *, *, #15415, .T. ) ;
#2489=DIRECTION ( 'NONE',  ( 0.000000000000000000, -0.000000000000000000, -1.000000000000000000 ) ) ;
#2490=VERTEX_POINT ( 'NONE', #11902 ) ;
#2493=DIRECTION ( 'NONE',  ( 0.000000000000000000, 0.000000000000000000, 1.000000000000000000 ) ) ;
#2496=VERTEX_POINT ( 'NONE', #18515 ) ;
#2499=CARTESIAN_POINT ( 'NONE',  ( -28.71290943744531177, 6.649236572130504896, 13.47739020623642325 ) ) ;
#2500=FACE_OUTER_BOUND ( 'NONE', #6431, .T. ) ;
#2501=PLANE ( 'NONE',  #2352 ) ;
#2502=EDGE_CURVE ( 'NONE', #17966, #9603, #6418, .T. ) ;
#2503=VERTEX_POINT ( 'NONE', #3307 ) ;
#2504=CARTESIAN_POINT ( 'NONE',  ( 28.86382559268571057, -6.505889654322387194, 13.29319881794719294 ) ) ;
#2506=EDGE_CURVE ( 'NONE', #17693, #22137, #2466, .T. ) ;
#2507=DIRECTION ( 'NONE',  ( -0.000000000000000000, -0.000000000000000000, -1.000000000000000000 ) ) ;
#2508=EDGE_LOOP ( 'NONE', ( #3186, #12936, #4883, #8474 ) ) ;
#2509=ORIENTED_EDGE ( 'NONE', *, *, #21702, .F. ) ;
#2511=DIRECTION ( 'NONE',  ( 0.000000000000000000, -0.000000000000000000, 1.000000000000000000 ) ) ;
#2512=TOROIDAL_SURFACE ( 'NONE', #18960, 4.700000000000004619, 0.2999999999999999889 ) ;
#2513=DIRECTION ( 'NONE',  ( 0.000000000000000000, 1.000000000000000000, -0.000000000000000000 ) ) ;
#2517=ORIENTED_EDGE ( 'NONE', *, *, #10993, .F. ) ;
#2519=DIRECTION ( 'NONE',  ( 1.000000000000000000, 0.000000000000000000, 0.000000000000000000 ) ) ;
#2520=EDGE_CURVE ( 'NONE', #706, #13756, #8575, .T. ) ;
#2523=DIRECTION ( 'NONE',  ( -0.000000000000000000, -0.000000000000000000, -1.000000000000000000 ) ) ;
#2526=CYLINDRICAL_SURFACE ( 'NONE', #5262, 0.5000000000000004441 ) ;
#2527=LINE ( 'NONE', #2420, #4970 ) ;
#2528=VECTOR ( 'NONE', #6351, 1000.000000000000000 ) ;
#2529=AXIS2_PLACEMENT_3D ( 'NONE', #19784, #6367, #9377 ) ;
#2530=CARTESIAN_POINT ( 'NONE',  ( 0.000000000000000000, -51.61873716947361856, 14.00000000000000000 ) ) ;
#2533=LINE ( 'NONE', #14718, #10552 ) ;
#2536=VERTEX_POINT ( 'NONE', #3531 ) ;
#2537=DIRECTION ( 'NONE',  ( 0.000000000000000000, 1.000000000000000000, 0.000000000000000000 ) ) ;
#2538=EDGE_CURVE ( 'NONE', #7977, #6397, #15384, .T. ) ;
#2540=VERTEX_POINT ( 'NONE', #6676 ) ;
#2541=ORIENTED_EDGE ( 'NONE', *, *, #3942, .T. ) ;
#2543=CARTESIAN_POINT ( 'NONE',  ( 25.37540678000427263, 68.74634676501045760, 7.200000000000000178 ) ) ;
#2544=ADVANCED_FACE ( 'NONE', ( #1735 ), #8683, .T. ) ;
#2545=CARTESIAN_POINT ( 'NONE',  ( 9.641460742840918030, -32.93424481021354921, 68.50000000000000000 ) ) ;
#2547=ORIENTED_EDGE ( 'NONE', *, *, #570, .T. ) ;
#2548=AXIS2_PLACEMENT_3D ( 'NONE', #4315, #9346, #11349 ) ;
#2551=ORIENTED_EDGE ( 'NONE', *, *, #9413, .T. ) ;
#2552=DIRECTION ( 'NONE',  ( 0.000000000000000000, 1.000000000000000000, -0.000000000000000000 ) ) ;
#2556=DIRECTION ( 'NONE',  ( -1.000000000000000000, -0.000000000000000000, 0.000000000000000000 ) ) ;
#2557=AXIS2_PLACEMENT_3D ( 'NONE', #13671, #6770, #20514 ) ;
#2558=VECTOR ( 'NONE', #11883, 1000.000000000000000 ) ;
#2559=FACE_OUTER_BOUND ( 'NONE', #8880, .T. ) ;
#2560=PLANE ( 'NONE',  #19605 ) ;
#2561=ORIENTED_EDGE ( 'NONE', *, *, #2948, .F. ) ;
#2565=CARTESIAN_POINT ( 'NONE',  ( -14.66174975910705136, -51.76873716947361714, 13.50000000000000000 ) ) ;
#2568=CARTESIAN_POINT ( 'NONE',  ( -31.50000000000002132, -72.00000000000001421, 1.800000000000000044 ) ) ;
#2569=ORIENTED_EDGE ( 'NONE', *, *, #17322, .F. ) ;
#2574=AXIS2_PLACEMENT_3D ( 'NONE', #9858, #10312, #18459 ) ;
#2575=ORIENTED_EDGE ( 'NONE', *, *, #11279, .T. ) ;
#2576=AXIS2_PLACEMENT_3D ( 'NONE', #11286, #18238, #7626 ) ;
#2577=AXIS2_PLACEMENT_3D ( 'NONE', #13536, #5152, #17320 ) ;
#2578=ORIENTED_EDGE ( 'NONE', *, *, #10121, .F. ) ;
#2579=VECTOR ( 'NONE', #16443, 1000.000000000000000 ) ;
#2580=DIRECTION ( 'NONE',  ( 0.000000000000000000, 0.000000000000000000, -1.000000000000000000 ) ) ;
#2581=CARTESIAN_POINT ( 'NONE',  ( 15.95292532278785913, 32.11873716947361856, 68.50000000000000000 ) ) ;
#2582=ORIENTED_EDGE ( 'NONE', *, *, #17921, .F. ) ;
#2583=DIRECTION ( 'NONE',  ( -0.000000000000000000, -0.000000000000000000, -1.000000000000000000 ) ) ;
#2585=EDGE_CURVE ( 'NONE', #11808, #6249, #21864, .T. ) ;
#2586=CARTESIAN_POINT ( 'NONE',  ( 25.37540678000427263, -63.74634676501045050, 13.19999999999999929 ) ) ;
#2587=CARTESIAN_POINT ( 'NONE',  ( 8.641460742840918030, -33.93424481021354921, 68.00000000000000000 ) ) ;
#2588=EDGE_CURVE ( 'NONE', #1357, #6635, #4874, .T. ) ;
#2589=DIRECTION ( 'NONE',  ( 0.000000000000000000, -1.000000000000000000, 0.000000000000000000 ) ) ;
#2590=VECTOR ( 'NONE', #18925, 1000.000000000000000 ) ;
#2591=SPHERICAL_SURFACE ( 'NONE', #1833, 0.5000000000000000000 ) ;
#2592=AXIS2_PLACEMENT_3D ( 'NONE', #21206, #4073, #477 ) ;
#2597=ORIENTED_EDGE ( 'NONE', *, *, #8247, .T. ) ;
#2601=ORIENTED_EDGE ( 'NONE', *, *, #4453, .T. ) ;
#2602=DIRECTION ( 'NONE',  ( 0.000000000000000000, 0.000000000000000000, 1.000000000000000000 ) ) ;
#2603=EDGE_CURVE ( 'NONE', #12236, #6333, #19002, .T. ) ;
#2605=VERTEX_POINT ( 'NONE', #17379 ) ;
#2607=DIRECTION ( 'NONE',  ( 0.000000000000000000, 0.000000000000000000, 1.000000000000000000 ) ) ;
#2608=CARTESIAN_POINT ( 'NONE',  ( 14.90249074828138198, 52.32070855728485981, 13.50000000000000000 ) ) ;
#2609=DIRECTION ( 'NONE',  ( 1.000000000000000000, 0.000000000000000000, 0.000000000000000000 ) ) ;
#2611=ORIENTED_EDGE ( 'NONE', *, *, #3078, .T. ) ;
#2613=CARTESIAN_POINT ( 'NONE',  ( 17.45292532278785913, 50.11873716947361856, 14.00000000000000000 ) ) ;
#2614=EDGE_LOOP ( 'NONE', ( #19265, #8650, #9650, #7642, #3004 ) ) ;
#2615=ORIENTED_EDGE ( 'NONE', *, *, #19798, .T. ) ;
#2616=ORIENTED_EDGE ( 'NONE', *, *, #5816, .T. ) ;
#2617=CARTESIAN_POINT ( 'NONE',  ( 14.96243083687292597, 51.84435441965536029, 13.82657707279502013 ) ) ;
#2618=CARTESIAN_POINT ( 'NONE',  ( 15.21174975910705918, -51.86873716947361856, 13.05380965755522737 ) ) ;
#2619=ORIENTED_EDGE ( 'NONE', *, *, #3524, .F. ) ;
#2620=EDGE_CURVE ( 'NONE', #4038, #444, #16841, .T. ) ;
#2622=ORIENTED_EDGE ( 'NONE', *, *, #9442, .T. ) ;
#2623=FACE_OUTER_BOUND ( 'NONE', #3403, .T. ) ;
#2625=EDGE_CURVE ( 'NONE', #4860, #6694, #15765, .T. ) ;
#2627=CARTESIAN_POINT ( 'NONE',  ( 23.02398829872513986, -2.157133568460768647, 13.19999999999999929 ) ) ;
#2630=DIRECTION ( 'NONE',  ( 1.000000000000000000, 0.000000000000000000, 0.000000000000000000 ) ) ;
#2631=ORIENTED_EDGE ( 'NONE', *, *, #9324, .T. ) ;
#2633=CARTESIAN_POINT ( 'NONE',  ( -27.67540678000428400, -10.94079601157914716, 13.50000000000000000 ) ) ;
#2637=ORIENTED_EDGE ( 'NONE', *, *, #1108, .T. ) ;
#2638=( NAMED_UNIT ( * ) SI_UNIT ( $, .STERADIAN. ) SOLID_ANGLE_UNIT ( ) );
#2640=ORIENTED_EDGE ( 'NONE', *, *, #700, .F. ) ;
#2641=DIRECTION ( 'NONE',  ( -0.000000000000000000, -1.000000000000000000, -0.000000000000000000 ) ) ;
#2644=ORIENTED_EDGE ( 'NONE', *, *, #224, .F. ) ;
#2645=AXIS2_PLACEMENT_3D ( 'NONE', #11903, #22123, #9909 ) ;
#2646=EDGE_LOOP ( 'NONE', ( #20927, #13409, #19193, #18001 ) ) ;
#2647=CARTESIAN_POINT ( 'NONE',  ( -15.21174975910705029, 52.10286008774955491, 13.87500000000000000 ) ) ;
#2649=FACE_OUTER_BOUND ( 'NONE', #3275, .T. ) ;
#2650=ORIENTED_EDGE ( 'NONE', *, *, #22050, .T. ) ;
#2653=EDGE_CURVE ( 'NONE', #1327, #5533, #8894, .T. ) ;
#2655=CARTESIAN_POINT ( 'NONE',  ( -23.02398829872514696, -2.211005166399017341, 13.20000000000005969 ) ) ;
#2656=EDGE_CURVE ( 'NONE', #19855, #19467, #17199, .T. ) ;
#2660=CARTESIAN_POINT ( 'NONE',  ( 0.000000000000000000, 38.74634676501045760, 42.50000000000000000 ) ) ;
#2664=DIRECTION ( 'NONE',  ( 1.000000000000000000, 0.000000000000000000, 0.000000000000000000 ) ) ;
#2666=DIRECTION ( 'NONE',  ( 1.000000000000000000, 0.000000000000000000, 0.000000000000000000 ) ) ;
#2668=EDGE_CURVE ( 'NONE', #21435, #13945, #12322, .T. ) ;
#2671=ORIENTED_EDGE ( 'NONE', *, *, #16402, .T. ) ;
#2672=AXIS2_PLACEMENT_3D ( 'NONE', #21976, #13451, #20291 ) ;
#2673=CYLINDRICAL_SURFACE ( 'NONE', #4954, 2.000000000000000000 ) ;
#2676=DIRECTION ( 'NONE',  ( 0.000000000000000000, 0.000000000000000000, 1.000000000000000000 ) ) ;
#2678=CARTESIAN_POINT ( 'NONE',  ( -24.43662752439705343, 0.000000000000000000, 3.799999999999999822 ) ) ;
#2679=EDGE_CURVE ( 'NONE', #3260, #11867, #18633, .T. ) ;
#2680=ORIENTED_EDGE ( 'NONE', *, *, #1292, .F. ) ;
#2682=DIRECTION ( 'NONE',  ( -1.000000000000000000, 0.000000000000000000, 0.000000000000000000 ) ) ;
#2684=LINE ( 'NONE', #9302, #19885 ) ;
#2685=AXIS2_PLACEMENT_3D ( 'NONE', #8692, #8902, #14029 ) ;
#2686=COLOUR_RGB ( '', 0.31764706, 0.68627451, 0.89019608) ;
#2690=LINE ( 'NONE', #5755, #13005 ) ;
#2691=VERTEX_POINT ( 'NONE', #15806 ) ;
#2692=CARTESIAN_POINT ( 'NONE',  ( -15.21174975910705207, 51.61873716947361856, 68.50000000000000000 ) ) ;
#2693=CYLINDRICAL_SURFACE ( 'NONE', #15621, 1.999999999999991340 ) ;
#2695=ORIENTED_EDGE ( 'NONE', *, *, #19331, .T. ) ;
#2698=DIRECTION ( 'NONE',  ( -0.000000000000000000, -0.000000000000000000, 1.000000000000000000 ) ) ;
#2699=EDGE_CURVE ( 'NONE', #13403, #17454, #10422, .T. ) ;
#2701=AXIS2_PLACEMENT_3D ( 'NONE', #7085, #13882, #447 ) ;
#2702=AXIS2_PLACEMENT_3D ( 'NONE', #15585, #10564, #17382 ) ;
#2704=ORIENTED_EDGE ( 'NONE', *, *, #21393, .T. ) ;
#2706=EDGE_CURVE ( 'NONE', #6037, #15847, #8637, .T. ) ;
#2708=CARTESIAN_POINT ( 'NONE',  ( 0.000000000000000000, -42.11054587065083155, 13.79999999999999893 ) ) ;
#2709=VECTOR ( 'NONE', #13004, 1000.000000000000000 ) ;
#2713=FACE_OUTER_BOUND ( 'NONE', #8196, .T. ) ;
#2715=CARTESIAN_POINT ( 'NONE',  ( 15.16923466928735742, 52.00603548408893317, 13.50000000000000000 ) ) ;
#2716=CARTESIAN_POINT ( 'NONE',  ( 9.141460742840918030, -32.93424481021354921, 42.50000000000000000 ) ) ;
#2718=CIRCLE ( 'NONE', #16284, 0.2500000000000002220 ) ;
#2720=DIRECTION ( 'NONE',  ( -1.000000000000000000, 0.000000000000000000, -0.000000000000000000 ) ) ;
#2721=DIRECTION ( 'NONE',  ( 0.000000000000000000, 0.000000000000000000, 1.000000000000000000 ) ) ;
#2722=VERTEX_POINT ( 'NONE', #17606 ) ;
#2724=ORIENTED_EDGE ( 'NONE', *, *, #4967, .T. ) ;
#2725=DIRECTION ( 'NONE',  ( 0.000000000000000000, 0.000000000000000000, -1.000000000000000000 ) ) ;
#2726=CARTESIAN_POINT ( 'NONE',  ( 23.32398829872514412, -3.528912754968634768, 13.50000000000000000 ) ) ;
#2731=AXIS2_PLACEMENT_3D ( 'NONE', #21669, #1392, #21893 ) ;
#2732=AXIS2_PLACEMENT_3D ( 'NONE', #4775, #18308, #8458 ) ;
#2734=AXIS2_PLACEMENT_3D ( 'NONE', #9850, #1552, #3250 ) ;
#2735=ORIENTED_EDGE ( 'NONE', *, *, #960, .F. ) ;
#2737=AXIS2_PLACEMENT_3D ( 'NONE', #6294, #796, #14432 ) ;
#2739=DIRECTION ( 'NONE',  ( -1.000000000000000000, -0.000000000000000000, -0.000000000000000000 ) ) ;
#2742=DIRECTION ( 'NONE',  ( 1.000000000000000000, 0.000000000000000000, 0.000000000000000000 ) ) ;
#2747=CARTESIAN_POINT ( 'NONE',  ( -15.21174975910705207, 52.10286008774954780, 13.87500000000000000 ) ) ;
#2749=ORIENTED_EDGE ( 'NONE', *, *, #8772, .T. ) ;
#2751=VECTOR ( 'NONE', #18342, 1000.000000000000000 ) ;
#2753=DIRECTION ( 'NONE',  ( -2.546383084002652634E-16, 0.000000000000000000, -1.000000000000000000 ) ) ;
#2755=VERTEX_POINT ( 'NONE', #12653 ) ;
#2757=VECTOR ( 'NONE', #10667, 1000.000000000000000 ) ;
#2758=CARTESIAN_POINT ( 'NONE',  ( -23.02398829872514696, -2.279713943076945526, 13.43059441564925649 ) ) ;
#2759=ORIENTED_EDGE ( 'NONE', *, *, #6572, .T. ) ;
#2762=CARTESIAN_POINT ( 'NONE',  ( -14.71432566477614579, 52.07267295633236870, 13.50000000000000000 ) ) ;
#2763=CARTESIAN_POINT ( 'NONE',  ( -15.95292532278785913, 50.11873716947361856, 13.79999999999999893 ) ) ;
#2764=EDGE_CURVE ( 'NONE', #11913, #3158, #10072, .T. ) ;
#2765=CARTESIAN_POINT ( 'NONE',  ( -17.95292532278785913, 38.74634676501045760, 13.99999999999999822 ) ) ;
#2767=ORIENTED_EDGE ( 'NONE', *, *, #21139, .T. ) ;
#2769=DIRECTION ( 'NONE',  ( 0.000000000000000000, 0.000000000000000000, 1.000000000000000000 ) ) ;
#2772=DIRECTION ( 'NONE',  ( -1.000000000000000000, 0.000000000000000000, 0.000000000000000000 ) ) ;
#2773=FACE_OUTER_BOUND ( 'NONE', #16639, .T. ) ;
#2774=DIRECTION ( 'NONE',  ( 0.000000000000000000, 1.000000000000000000, 0.000000000000000000 ) ) ;
#2776=DIRECTION ( 'NONE',  ( -0.000000000000000000, -0.000000000000000000, -1.000000000000000000 ) ) ;
#2777=DIRECTION ( 'NONE',  ( 0.000000000000000000, 1.000000000000000000, -0.000000000000000000 ) ) ;
#2779=EDGE_CURVE ( 'NONE', #10550, #6305, #11839, .T. ) ;
#2780=CARTESIAN_POINT ( 'NONE',  ( -29.50000000000001421, -69.00000000000000000, 0.1242640687119232062 ) ) ;
#2785=AXIS2_PLACEMENT_3D ( 'NONE', #9123, #7573, #19316 ) ;
#2790=ADVANCED_FACE ( 'NONE', ( #19843 ), #16479, .T. ) ;
#2791=EDGE_CURVE ( 'NONE', #16467, #14127, #21148, .T. ) ;
#2794=EDGE_CURVE ( 'NONE', #19805, #620, #7653, .T. ) ;
#2795=CIRCLE ( 'NONE', #12765, 0.2999999999999999334 ) ;
#2798=LINE ( 'NONE', #9397, #17452 ) ;
#2799=CIRCLE ( 'NONE', #21033, 1.974596669241483804 ) ;
#2801=DIRECTION ( 'NONE',  ( 1.000000000000000000, -0.000000000000000000, -0.000000000000000000 ) ) ;
#2802=CARTESIAN_POINT ( 'NONE',  ( 0.000000000000000000, -51.61873716947361856, 68.00000000000000000 ) ) ;
#2805=VERTEX_POINT ( 'NONE', #19620 ) ;
#2808=EDGE_CURVE ( 'NONE', #20015, #6058, #16234, .T. ) ;
#2810=AXIS2_PLACEMENT_3D ( 'NONE', #18188, #622, #4098 ) ;
#2811=CIRCLE ( 'NONE', #3891, 1.999999999999991340 ) ;
#2812=DIRECTION ( 'NONE',  ( 0.000000000000000000, 0.000000000000000000, -1.000000000000000000 ) ) ;
#2815=VECTOR ( 'NONE', #20240, 1000.000000000000000 ) ;
#2817=DIRECTION ( 'NONE',  ( 1.000000000000000000, 0.000000000000000000, 0.000000000000000000 ) ) ;
#2818=ADVANCED_FACE ( 'NONE', ( #13234 ), #4399, .F. ) ;
#2821=ADVANCED_FACE ( 'NONE', ( #6316 ), #6098, .T. ) ;
#2826=DIRECTION ( 'NONE',  ( -1.000000000000000000, 0.000000000000000000, 0.000000000000000000 ) ) ;
#2827=ADVANCED_FACE ( 'NONE', ( #21425 ), #2843, .F. ) ;
#2829=DIRECTION ( 'NONE',  ( 0.000000000000000000, -1.000000000000000000, 0.000000000000000000 ) ) ;
#2833=VERTEX_POINT ( 'NONE', #8102 ) ;
#2837=EDGE_CURVE ( 'NONE', #10741, #6249, #7938, .T. ) ;
#2838=CARTESIAN_POINT ( 'NONE',  ( 15.06741964789885024, -51.94542257242142824, 13.49999999999999645 ) ) ;
#2839=DIRECTION ( 'NONE',  ( 0.000000000000000000, 0.000000000000000000, 1.000000000000000000 ) ) ;
#2840=ORIENTED_EDGE ( 'NONE', *, *, #21774, .F. ) ;
#2843=CYLINDRICAL_SURFACE ( 'NONE', #20442, 0.3000000000000016542 ) ;
#2844=AXIS2_PLACEMENT_3D ( 'NONE', #3025, #5770, #10790 ) ;
#2847=EDGE_LOOP ( 'NONE', ( #16270, #4302, #21018, #2695 ) ) ;
#2850=ORIENTED_EDGE ( 'NONE', *, *, #12933, .T. ) ;
#2851=VERTEX_POINT ( 'NONE', #7990 ) ;
#2852=DIRECTION ( 'NONE',  ( 0.000000000000000000, 0.000000000000000000, 1.000000000000000000 ) ) ;
#2853=EDGE_CURVE ( 'NONE', #2179, #22131, #8681, .T. ) ;
#2857=FACE_OUTER_BOUND ( 'NONE', #12159, .T. ) ;
#2859=TOROIDAL_SURFACE ( 'NONE', #16428, 1.000000000000000000, 0.5000000000000000000 ) ;
#2861=FACE_OUTER_BOUND ( 'NONE', #5265, .T. ) ;
#2862=DIRECTION ( 'NONE',  ( -0.000000000000000000, -1.000000000000000000, -0.000000000000000000 ) ) ;
#2864=CARTESIAN_POINT ( 'NONE',  ( 23.02398829872513986, 2.157133568460765538, 13.19999999999999929 ) ) ;
#2865=FACE_OUTER_BOUND ( 'NONE', #7165, .T. ) ;
#2867=CARTESIAN_POINT ( 'NONE',  ( -3.627054932750481964, -33.93424481021354921, 68.50000000000000000 ) ) ;
#2869=EDGE_CURVE ( 'NONE', #2394, #19800, #5830, .T. ) ;
#2873=CARTESIAN_POINT ( 'NONE',  ( -23.02398829872513986, 7.027230193580998154E-15, 13.79999999999999893 ) ) ;
#2876=CYLINDRICAL_SURFACE ( 'NONE', #14111, 0.3000000000000016542 ) ;
#2879=ORIENTED_EDGE ( 'NONE', *, *, #19114, .F. ) ;
#2880=VECTOR ( 'NONE', #12883, 1000.000000000000000 ) ;
#2882=CARTESIAN_POINT ( 'NONE',  ( 8.641460742840918030, 33.43424481021354921, 68.50000000000000000 ) ) ;
#2883=ORIENTED_EDGE ( 'NONE', *, *, #11039, .T. ) ;
#2886=DIRECTION ( 'NONE',  ( 0.000000000000000000, 0.000000000000000000, 1.000000000000000000 ) ) ;
#2888=FACE_OUTER_BOUND ( 'NONE', #568, .T. ) ;
#2889=ORIENTED_EDGE ( 'NONE', *, *, #5928, .F. ) ;
#2891=PRODUCT_DEFINITION ( 'UNKNOWN', '', #18732, #13558 ) ;
#2892=CARTESIAN_POINT ( 'NONE',  ( 29.50000000000002132, 69.00000000000000000, 0.2999999999999947153 ) ) ;
#2894=FACE_OUTER_BOUND ( 'NONE', #2909, .T. ) ;
#2895=CARTESIAN_POINT ( 'NONE',  ( -23.02398829872513986, -2.681050038336388663, 13.50121499737458564 ) ) ;
#2902=EDGE_LOOP ( 'NONE', ( #11148, #3601, #20243, #1179 ) ) ;
#2903=ADVANCED_FACE ( 'NONE', ( #21308 ), #18488, .F. ) ;
#2906=LINE ( 'NONE', #8167, #17228 ) ;
#2909=EDGE_LOOP ( 'NONE', ( #3326, #19451, #17481, #12974 ) ) ;
#2913=AXIS2_PLACEMENT_3D ( 'NONE', #20867, #5440, #12227 ) ;
#2914=LINE ( 'NONE', #4370, #780 ) ;
#2916=CARTESIAN_POINT ( 'NONE',  ( -23.02398829872514341, -5.683640910026986681, 13.79999999999999893 ) ) ;
#2917=AXIS2_PLACEMENT_3D ( 'NONE', #3747, #3541, #10569 ) ;
#2920=FACE_OUTER_BOUND ( 'NONE', #5704, .T. ) ;
#2921=DIRECTION ( 'NONE',  ( -0.000000000000000000, 1.000000000000000000, -0.000000000000000000 ) ) ;
#2923=CARTESIAN_POINT ( 'NONE',  ( 17.92752199202934094, 50.11873716947361856, 13.79999999999999893 ) ) ;
#2925=CARTESIAN_POINT ( 'NONE',  ( 31.63662752439705272, 0.000000000000000000, -18.50000000000000000 ) ) ;
#2926=CARTESIAN_POINT ( 'NONE',  ( 28.87540678000427263, -6.494748934539262386, 7.720760203330568672 ) ) ;
#2927=ORIENTED_EDGE ( 'NONE', *, *, #15789, .T. ) ;
#2928=VECTOR ( 'NONE', #12425, 1000.000000000000000 ) ;
#2929=CARTESIAN_POINT ( 'NONE',  ( 32.20000000000001705, 0.000000000000000000, 3.200000000000000178 ) ) ;
#2930=VERTEX_POINT ( 'NONE', #10337 ) ;
#2931=DIRECTION ( 'NONE',  ( -0.000000000000000000, 1.000000000000000000, -0.000000000000000000 ) ) ;
#2935=EDGE_LOOP ( 'NONE', ( #12583, #7081, #8810, #14553 ) ) ;
#2936=LINE ( 'NONE', #4492, #18148 ) ;
#2938=ADVANCED_FACE ( 'NONE', ( #5075 ), #19756, .F. ) ;
#2942=ORIENTED_EDGE ( 'NONE', *, *, #21673, .T. ) ;
#2946=DIRECTION ( 'NONE',  ( 1.000000000000000000, 0.000000000000000000, 0.000000000000000000 ) ) ;
#2947=VECTOR ( 'NONE', #4027, 1000.000000000000000 ) ;
#2948=EDGE_CURVE ( 'NONE', #852, #15775, #11520, .T. ) ;
#2950=EDGE_LOOP ( 'NONE', ( #7873, #20500, #10760, #2671 ) ) ;
#2952=DIRECTION ( 'NONE',  ( -1.000000000000000000, 0.000000000000000000, 0.000000000000000000 ) ) ;
#2953=DIRECTION ( 'NONE',  ( 0.000000000000000000, 0.000000000000000000, 1.000000000000000000 ) ) ;
#2954=CYLINDRICAL_SURFACE ( 'NONE', #5235, 0.3000000000000003775 ) ;
#2956=ORIENTED_EDGE ( 'NONE', *, *, #17439, .F. ) ;
#2957=EDGE_LOOP ( 'NONE', ( #20095, #16910, #376, #14085 ) ) ;
#2960=CARTESIAN_POINT ( 'NONE',  ( 25.37540678000426908, 36.74634676501047181, 42.50000000000000000 ) ) ;
#2961=EDGE_CURVE ( 'NONE', #170, #13966, #5482, .T. ) ;
#2962=ORIENTED_EDGE ( 'NONE', *, *, #2506, .T. ) ;
#2963=CARTESIAN_POINT ( 'NONE',  ( 25.37540678000427263, 68.44634676501046044, 7.500000000000000000 ) ) ;
#2966=CARTESIAN_POINT ( 'NONE',  ( -9.141460742840918030, 33.43424481021354921, 68.00000000000000000 ) ) ;
#2967=DIRECTION ( 'NONE',  ( -0.000000000000000000, -0.000000000000000000, -1.000000000000000000 ) ) ;
#2970=VERTEX_POINT ( 'NONE', #12100 ) ;
#2971=CARTESIAN_POINT ( 'NONE',  ( -15.95292532278785913, -50.11873716947361856, 13.79999999999999893 ) ) ;
#2972=EDGE_CURVE ( 'NONE', #8448, #6694, #9999, .T. ) ;
#2973=CYLINDRICAL_SURFACE ( 'NONE', #7494, 0.2999999999999999334 ) ;
#2976=ORIENTED_EDGE ( 'NONE', *, *, #1124, .F. ) ;
#2977=DIRECTION ( 'NONE',  ( 0.000000000000000000, 0.000000000000000000, 1.000000000000000000 ) ) ;
#2978=CARTESIAN_POINT ( 'NONE',  ( -31.50000000000002132, -71.00000000000001421, 1.500000000000000000 ) ) ;
#2980=EDGE_LOOP ( 'NONE', ( #13397, #22070, #7365, #9979 ) ) ;
#2982=CYLINDRICAL_SURFACE ( 'NONE', #933, 0.2999999999999999334 ) ;
#2986=CARTESIAN_POINT ( 'NONE',  ( -29.50000000000001421, 69.00000000000000000, 0.1242640687119232062 ) ) ;
#2987=DIRECTION ( 'NONE',  ( 1.000000000000000000, 0.000000000000000000, 0.000000000000000000 ) ) ;
#2989=ORIENTED_EDGE ( 'NONE', *, *, #10202, .T. ) ;
#2992=EDGE_LOOP ( 'NONE', ( #2283, #15480, #16801, #15062 ) ) ;
#2993=LINE ( 'NONE', #7935, #12879 ) ;
#2994=DIRECTION ( 'NONE',  ( 0.000000000000000000, 0.000000000000000000, 1.000000000000000000 ) ) ;
#2995=CARTESIAN_POINT ( 'NONE',  ( -23.02398829872514341, -2.558844643945016539, 13.47100117844888700 ) ) ;
#2996=CARTESIAN_POINT ( 'NONE',  ( 15.21174975910705918, 51.61873716947361856, 14.00000000000000000 ) ) ;
#2997=DIRECTION ( 'NONE',  ( 0.000000000000000000, 0.000000000000000000, 1.000000000000000000 ) ) ;
#2998=DIRECTION ( 'NONE',  ( -0.000000000000000000, -1.000000000000000000, -0.000000000000000000 ) ) ;
#3001=DIRECTION ( 'NONE',  ( 1.000000000000000000, 0.000000000000000000, 0.000000000000000000 ) ) ;
#3002=FACE_OUTER_BOUND ( 'NONE', #7067, .T. ) ;
#3004=ORIENTED_EDGE ( 'NONE', *, *, #7645, .F. ) ;
#3007=DIRECTION ( 'NONE',  ( 0.000000000000000000, 0.000000000000000000, 1.000000000000000000 ) ) ;
#3009=DIRECTION ( 'NONE',  ( 0.000000000000000000, 0.000000000000000000, 1.000000000000000000 ) ) ;
#3013=VERTEX_POINT ( 'NONE', #11983 ) ;
#3014=CARTESIAN_POINT ( 'NONE',  ( 29.33570557543480462, -2.657597333499439607, 0.02220207281669739699 ) ) ;
#3015=ADVANCED_FACE ( 'NONE', ( #20626 ), #2267, .F. ) ;
#3017=EDGE_CURVE ( 'NONE', #4254, #18602, #7265, .T. ) ;
#3018=CIRCLE ( 'NONE', #8375, 0.5000000000000000000 ) ;
#3020=ORIENTED_EDGE ( 'NONE', *, *, #2273, .T. ) ;
#3021=DIRECTION ( 'NONE',  ( 0.000000000000000000, 0.000000000000000000, -1.000000000000000000 ) ) ;
#3022=DIRECTION ( 'NONE',  ( -0.000000000000000000, -0.000000000000000000, -1.000000000000000000 ) ) ;
#3025=CARTESIAN_POINT ( 'NONE',  ( -30.67540678000427690, 6.000000000000000000, 3.799999999999999822 ) ) ;
#3026=CYLINDRICAL_SURFACE ( 'NONE', #5409, 0.5000000000000004441 ) ;
#3034=ORIENTED_EDGE ( 'NONE', *, *, #996, .T. ) ;
#3035=DIRECTION ( 'NONE',  ( 1.000000000000000000, 0.000000000000000000, 0.000000000000000000 ) ) ;
#3036=CYLINDRICAL_SURFACE ( 'NONE', #4222, 2.000000000000000000 ) ;
#3037=ORIENTED_EDGE ( 'NONE', *, *, #5928, .T. ) ;
#3039=CARTESIAN_POINT ( 'NONE',  ( -3.627054932750481964, -33.43424481021354921, 7.321391277662001151 ) ) ;
#3043=ORIENTED_EDGE ( 'NONE', *, *, #11546, .T. ) ;
#3044=ORIENTED_EDGE ( 'NONE', *, *, #14343, .F. ) ;
#3045=CIRCLE ( 'NONE', #19472, 3.500000000000003109 ) ;
#3047=CYLINDRICAL_SURFACE ( 'NONE', #12741, 0.2999999999999999334 ) ;
#3048=DIRECTION ( 'NONE',  ( 0.000000000000000000, 0.000000000000000000, 1.000000000000000000 ) ) ;
#3050=CARTESIAN_POINT ( 'NONE',  ( 8.641460742840918030, -33.43424481021354921, 42.50000000000000000 ) ) ;
#3053=VECTOR ( 'NONE', #3022, 1000.000000000000000 ) ;
#3056=TOROIDAL_SURFACE ( 'NONE', #1615, 1.500000000000000000, 0.5000000000000000000 ) ;
#3060=EDGE_LOOP ( 'NONE', ( #3393, #5780, #14038, #161, #18929, #3020 ) ) ;
#3061=DIRECTION ( 'NONE',  ( 0.000000000000000000, 0.000000000000000000, -1.000000000000000000 ) ) ;
#3064=EDGE_CURVE ( 'NONE', #5550, #14977, #4748, .T. ) ;
#3069=DIRECTION ( 'NONE',  ( 0.000000000000000000, 1.000000000000000000, 0.000000000000000000 ) ) ;
#3072=VECTOR ( 'NONE', #7659, 1000.000000000000000 ) ;
#3073=CARTESIAN_POINT ( 'NONE',  ( -15.21174975910705207, -51.61873716947361856, 68.50000000000000000 ) ) ;
#3076=DIRECTION ( 'NONE',  ( -1.000000000000000000, 0.000000000000000000, 0.000000000000000000 ) ) ;
#3078=EDGE_CURVE ( 'NONE', #808, #1813, #16914, .T. ) ;
#3082=VERTEX_POINT ( 'NONE', #7533 ) ;
#3087=VECTOR ( 'NONE', #7688, 1000.000000000000000 ) ;
#3089=AXIS2_PLACEMENT_3D ( 'NONE', #2996, #9938, #9824 ) ;
#3091=CARTESIAN_POINT ( 'NONE',  ( -15.21174975910705385, 52.00603550409435627, 13.50000000000000000 ) ) ;
#3092=EDGE_CURVE ( 'NONE', #5901, #13985, #5753, .T. ) ;
#3093=DIRECTION ( 'NONE',  ( 0.000000000000000000, 0.000000000000000000, 1.000000000000000000 ) ) ;
#3094=ADVANCED_FACE ( 'NONE', ( #4051 ), #21185, .F. ) ;
#3095=ORIENTED_EDGE ( 'NONE', *, *, #473, .F. ) ;
#3098=ORIENTED_EDGE ( 'NONE', *, *, #8129, .T. ) ;
#3099=VERTEX_POINT ( 'NONE', #16551 ) ;
#3100=DIRECTION ( 'NONE',  ( 0.000000000000000000, 0.000000000000000000, 1.000000000000000000 ) ) ;
#3101=DIRECTION ( 'NONE',  ( -1.000000000000000000, 0.000000000000000000, 0.000000000000000000 ) ) ;
#3103=FACE_OUTER_BOUND ( 'NONE', #18280, .T. ) ;
#3106=TOROIDAL_SURFACE ( 'NONE', #10975, 2.274596669241483848, 0.2999999999999999889 ) ;
#3108=DIRECTION ( 'NONE',  ( 0.000000000000000000, -1.000000000000000000, 0.000000000000000000 ) ) ;
#3111=CIRCLE ( 'NONE', #8487, 4.700000000000002842 ) ;
#3125=AXIS2_PLACEMENT_3D ( 'NONE', #7723, #14523, #19694 ) ;
#3126=AXIS2_PLACEMENT_3D ( 'NONE', #3812, #9286, #19034 ) ;
#3128=FACE_OUTER_BOUND ( 'NONE', #332, .T. ) ;
#3131=CIRCLE ( 'NONE', #12075, 2.500000000000002220 ) ;
#3133=DIRECTION ( 'NONE',  ( 0.000000000000000000, 0.000000000000000000, 1.000000000000000000 ) ) ;
#3137=AXIS2_PLACEMENT_3D ( 'NONE', #13305, #5146, #11950 ) ;
#3140=DIRECTION ( 'NONE',  ( 1.000000000000000000, 0.000000000000000000, 0.000000000000000000 ) ) ;
#3141=CARTESIAN_POINT ( 'NONE',  ( 15.95292532278785913, 50.11873716947361856, 13.87499999999999822 ) ) ;
#3142=ADVANCED_FACE ( 'NONE', ( #14428 ), #2591, .T. ) ;
#3143=CARTESIAN_POINT ( 'NONE',  ( 23.02398829872513986, 2.157133568460765538, 42.50000000000000000 ) ) ;
#3144=VECTOR ( 'NONE', #20147, 1000.000000000000000 ) ;
#3145=DIRECTION ( 'NONE',  ( 0.000000000000000000, 0.000000000000000000, 1.000000000000000000 ) ) ;
#3148=VECTOR ( 'NONE', #17258, 1000.000000000000000 ) ;
#3150=APPLICATION_CONTEXT ( 'automotive_design' ) ;
#3152=ORIENTED_EDGE ( 'NONE', *, *, #4213, .F. ) ;
#3157=DIRECTION ( 'NONE',  ( -0.000000000000000000, -0.000000000000000000, -1.000000000000000000 ) ) ;
#3158=VERTEX_POINT ( 'NONE', #16109 ) ;
#3160=CIRCLE ( 'NONE', #12087, 0.5000000000000004441 ) ;
#3161=DIRECTION ( 'NONE',  ( 1.000000000000000000, 0.000000000000000000, 0.000000000000000000 ) ) ;
#3163=ORIENTED_EDGE ( 'NONE', *, *, #14368, .F. ) ;
#3165=TOROIDAL_SURFACE ( 'NONE', #16377, 5.299999999999999822, 0.2999999999999999889 ) ;
#3168=CARTESIAN_POINT ( 'NONE',  ( 29.37540678000427619, -5.000000000000000000, 3.799999999999999822 ) ) ;
#3169=DIRECTION ( 'NONE',  ( 0.000000000000000000, 0.000000000000000000, -1.000000000000000000 ) ) ;
#3173=EDGE_CURVE ( 'NONE', #16033, #8961, #14072, .T. ) ;
#3174=DIRECTION ( 'NONE',  ( 0.000000000000000000, 0.000000000000000000, 1.000000000000000000 ) ) ;
#3180=ORIENTED_EDGE ( 'NONE', *, *, #11427, .F. ) ;
#3185=DIRECTION ( 'NONE',  ( 0.000000000000000000, 0.000000000000000000, 1.000000000000000000 ) ) ;
#3186=ORIENTED_EDGE ( 'NONE', *, *, #11639, .T. ) ;
#3187=LINE ( 'NONE', #10671, #21683 ) ;
#3188=ORIENTED_EDGE ( 'NONE', *, *, #1284, .T. ) ;
#3189=CARTESIAN_POINT ( 'NONE',  ( -32.20000000000001705, -71.00000000000001421, 1.800000000000000044 ) ) ;
#3190=DIRECTION ( 'NONE',  ( 1.000000000000000000, 0.000000000000000000, -0.000000000000000000 ) ) ;
#3191=AXIS2_PLACEMENT_3D ( 'NONE', #1449, #1671, #1 ) ;
#3192=PLANE ( 'NONE',  #15929 ) ;
#3194=DIRECTION ( 'NONE',  ( 0.000000000000000000, 0.000000000000000000, -1.000000000000000000 ) ) ;
#3198=DIRECTION ( 'NONE',  ( 0.000000000000000000, 0.000000000000000000, 1.000000000000000000 ) ) ;
#3201=LINE ( 'NONE', #20320, #19349 ) ;
#3206=CARTESIAN_POINT ( 'NONE',  ( 30.37540678000427619, 63.74634676501045050, 3.799999999999999822 ) ) ;
#3209=ORIENTED_EDGE ( 'NONE', *, *, #487, .F. ) ;
#3211=FACE_OUTER_BOUND ( 'NONE', #4765, .T. ) ;
#3213=VECTOR ( 'NONE', #16353, 1000.000000000000000 ) ;
#3215=ORIENTED_EDGE ( 'NONE', *, *, #6424, .T. ) ;
#3218=EDGE_CURVE ( 'NONE', #18098, #18442, #3367, .T. ) ;
#3219=EDGE_LOOP ( 'NONE', ( #15618, #14376, #8373, #15070 ) ) ;
#3220=CARTESIAN_POINT ( 'NONE',  ( -23.02398829872513986, 7.027230193580998154E-15, 13.79999999999999893 ) ) ;
#3222=CARTESIAN_POINT ( 'NONE',  ( -29.20000000000002061, 68.70000000000001705, 0.000000000000000000 ) ) ;
#3223=LINE ( 'NONE', #12941, #8117 ) ;
#3224=CARTESIAN_POINT ( 'NONE',  ( 25.37540678000427263, -67.54634676501045476, 7.500000000000000000 ) ) ;
#3226=CARTESIAN_POINT ( 'NONE',  ( 26.56227312273159313, -9.958410664601842655, 42.50000000000000000 ) ) ;
#3232=CARTESIAN_POINT ( 'NONE',  ( -29.20000000000002061, -2.799282752659324025, 0.000000000000000000 ) ) ;
#3234=LINE ( 'NONE', #10163, #7000 ) ;
#3236=CARTESIAN_POINT ( 'NONE',  ( -3.627054932750481964, -32.61873716947361856, 68.00000000000000000 ) ) ;
#3237=ORIENTED_EDGE ( 'NONE', *, *, #16885, .T. ) ;
#3238=CARTESIAN_POINT ( 'NONE',  ( -25.37540678000427263, 69.04634676501045476, 3.799999999999999822 ) ) ;
#3241=ORIENTED_EDGE ( 'NONE', *, *, #9266, .T. ) ;
#3242=DIRECTION ( 'NONE',  ( 0.000000000000000000, 0.000000000000000000, -1.000000000000000000 ) ) ;
#3243=AXIS2_PLACEMENT_3D ( 'NONE', #11895, #8335, #15142 ) ;
#3244=EDGE_CURVE ( 'NONE', #17577, #12310, #4435, .T. ) ;
#3247=DIRECTION ( 'NONE',  ( -1.000000000000000000, -0.000000000000000000, -0.000000000000000000 ) ) ;
#3249=CARTESIAN_POINT ( 'NONE',  ( -31.50000000000002132, -71.00000000000001421, 1.800000000000000044 ) ) ;
#3250=DIRECTION ( 'NONE',  ( 1.000000000000000000, 0.000000000000000000, 0.000000000000000000 ) ) ;
#3251=EDGE_CURVE ( 'NONE', #497, #18691, #489, .T. ) ;
#3254=EDGE_CURVE ( 'NONE', #16058, #12787, #11932, .T. ) ;
#3255=CIRCLE ( 'NONE', #19342, 4.051418481279135619 ) ;
#3256=CARTESIAN_POINT ( 'NONE',  ( -30.07540678000427548, 6.000000000000000000, 7.200000000000000178 ) ) ;
#3257=FACE_OUTER_BOUND ( 'NONE', #191, .T. ) ;
#3260=VERTEX_POINT ( 'NONE', #1673 ) ;
#3261=DIRECTION ( 'NONE',  ( 0.000000000000000000, -1.000000000000000000, 0.000000000000000000 ) ) ;
#3263=VERTEX_POINT ( 'NONE', #112 ) ;
#3268=CIRCLE ( 'NONE', #2917, 1.999999999999991340 ) ;
#3269=( BOUNDED_CURVE ( )  B_SPLINE_CURVE ( 3, ( #13677, #18955, #18611, #3625 ),
 .UNSPECIFIED., .F., .T. ) 
 B_SPLINE_CURVE_WITH_KNOTS ( ( 4, 4 ),
 ( 3.141592653589746931, 4.712388980384689674 ),
 .UNSPECIFIED. ) 
 CURVE ( )  GEOMETRIC_REPRESENTATION_ITEM ( )  RATIONAL_B_SPLINE_CURVE ( ( 1.000000000000000000, 0.8047378541243541683, 0.8047378541243541683, 1.000000000000000000 ) ) 
 REPRESENTATION_ITEM ( '' )  );
#3272=ORIENTED_EDGE ( 'NONE', *, *, #19757, .T. ) ;
#3273=AXIS2_PLACEMENT_3D ( 'NONE', #10904, #5685, #7464 ) ;
#3274=EDGE_CURVE ( 'NONE', #7310, #12787, #15140, .T. ) ;
#3275=EDGE_LOOP ( 'NONE', ( #11869, #3310, #5036, #12665 ) ) ;
#3281=ORIENTED_EDGE ( 'NONE', *, *, #21219, .F. ) ;
#3283=ADVANCED_FACE ( 'NONE', ( #11959 ), #9857, .F. ) ;
#3286=FACE_OUTER_BOUND ( 'NONE', #17670, .T. ) ;
#3287=FACE_OUTER_BOUND ( 'NONE', #21478, .T. ) ;
#3289=VERTEX_POINT ( 'NONE', #10186 ) ;
#3290=EDGE_LOOP ( 'NONE', ( #14582, #17613, #13227, #20690 ) ) ;
#3291=EDGE_LOOP ( 'NONE', ( #10644, #3095, #16394, #3422 ) ) ;
#3292=DIRECTION ( 'NONE',  ( -0.000000000000000000, -0.000000000000000000, -1.000000000000000000 ) ) ;
#3293=CARTESIAN_POINT ( 'NONE',  ( -29.20000000000002061, -2.799282752659324025, 0.000000000000000000 ) ) ;
#3294=EDGE_LOOP ( 'NONE', ( #3624, #10727, #3964, #13933, #16073 ) ) ;
#3296=CIRCLE ( 'NONE', #19379, 1.000000000000000888 ) ;
#3297=CIRCLE ( 'NONE', #19022, 0.5000000000000004441 ) ;
#3300=EDGE_CURVE ( 'NONE', #19588, #13533, #2288, .T. ) ;
#3301=DIRECTION ( 'NONE',  ( -0.000000000000000000, -0.000000000000000000, -1.000000000000000000 ) ) ;
#3302=DIRECTION ( 'NONE',  ( 0.000000000000000000, 0.000000000000000000, 1.000000000000000000 ) ) ;
#3303=CARTESIAN_POINT ( 'NONE',  ( 0.000000000000000000, -69.00000000000000000, 0.2999999999999947153 ) ) ;
#3304=ORIENTED_EDGE ( 'NONE', *, *, #2620, .F. ) ;
#3307=CARTESIAN_POINT ( 'NONE',  ( -15.95292532278785913, 32.11873716947361856, 42.50000000000000711 ) ) ;
#3309=LINE ( 'NONE', #10468, #20425 ) ;
#3310=ORIENTED_EDGE ( 'NONE', *, *, #7013, .F. ) ;
#3311=CARTESIAN_POINT ( 'NONE',  ( -15.95292532278785913, -52.39333383871510108, 13.79999999999999716 ) ) ;
#3312=VECTOR ( 'NONE', #13862, 1000.000000000000000 ) ;
#3316=CARTESIAN_POINT ( 'NONE',  ( -14.96174975910705207, -42.31054587065082728, 68.25000000000000000 ) ) ;
#3318=ORIENTED_EDGE ( 'NONE', *, *, #14610, .F. ) ;
#3319=EDGE_LOOP ( 'NONE', ( #11753, #21197, #21247, #19836 ) ) ;
#3320=ORIENTED_EDGE ( 'NONE', *, *, #8209, .F. ) ;
#3321=DIRECTION ( 'NONE',  ( 0.000000000000000000, 0.000000000000000000, 1.000000000000000000 ) ) ;
#3326=ORIENTED_EDGE ( 'NONE', *, *, #15555, .F. ) ;
#3327=VERTEX_POINT ( 'NONE', #20151 ) ;
#3329=VERTEX_POINT ( 'NONE', #13543 ) ;
#3334=ORIENTED_EDGE ( 'NONE', *, *, #10865, .F. ) ;
#3335=CARTESIAN_POINT ( 'NONE',  ( 28.87540678000427619, -6.494748934539263274, 7.799999999999999822 ) ) ;
#3336=LINE ( 'NONE', #8368, #16010 ) ;
#3338=CARTESIAN_POINT ( 'NONE',  ( 23.32398829872514057, 5.683640910026983128, 13.50000000000000000 ) ) ;
#3341=EDGE_CURVE ( 'NONE', #8501, #18098, #9084, .T. ) ;
#3348=EDGE_CURVE ( 'NONE', #124, #17663, #1794, .T. ) ;
#3349=ORIENTED_EDGE ( 'NONE', *, *, #143, .T. ) ;
#3350=DIRECTION ( 'NONE',  ( -1.000000000000000000, 0.000000000000000000, 0.000000000000000000 ) ) ;
#3351=ORIENTED_EDGE ( 'NONE', *, *, #11911, .F. ) ;
#3356=DIRECTION ( 'NONE',  ( 1.000000000000000000, 0.000000000000000000, 0.000000000000000000 ) ) ;
#3357=DIRECTION ( 'NONE',  ( -0.000000000000000000, -0.000000000000000000, 1.000000000000000000 ) ) ;
#3358=ADVANCED_FACE ( 'NONE', ( #20382 ), #8631, .T. ) ;
#3359=CIRCLE ( 'NONE', #15848, 0.2999999999999999334 ) ;
#3360=DIRECTION ( 'NONE',  ( 0.000000000000000000, 0.000000000000000000, 1.000000000000000000 ) ) ;
#3362=FACE_OUTER_BOUND ( 'NONE', #9982, .T. ) ;
#3365=ORIENTED_EDGE ( 'NONE', *, *, #18336, .F. ) ;
#3366=LINE ( 'NONE', #13213, #14867 ) ;
#3367=CIRCLE ( 'NONE', #1916, 4.351418481279137218 ) ;
#3369=VECTOR ( 'NONE', #14023, 1000.000000000000000 ) ;
#3370=ORIENTED_EDGE ( 'NONE', *, *, #18965, .T. ) ;
#3371=DIRECTION ( 'NONE',  ( -0.000000000000000000, -0.000000000000000000, -1.000000000000000000 ) ) ;
#3374=ORIENTED_EDGE ( 'NONE', *, *, #10981, .F. ) ;
#3377=EDGE_LOOP ( 'NONE', ( #21208, #3401, #18696, #15393 ) ) ;
#3381=CYLINDRICAL_SURFACE ( 'NONE', #10424, 0.5000000000000004441 ) ;
#3382=DIRECTION ( 'NONE',  ( 0.000000000000000000, 0.000000000000000000, -1.000000000000000000 ) ) ;
#3383=AXIS2_PLACEMENT_3D ( 'NONE', #15467, #6885, #10542 ) ;
#3384=DIRECTION ( 'NONE',  ( 0.000000000000000000, 1.000000000000000000, -0.000000000000000000 ) ) ;
#3386=CARTESIAN_POINT ( 'NONE',  ( 27.67540678000428045, 7.839012376739720627E-15, 13.79999999999999893 ) ) ;
#3387=DIRECTION ( 'NONE',  ( -1.000000000000000000, 0.000000000000000000, 0.000000000000000000 ) ) ;
#3389=EDGE_CURVE ( 'NONE', #1657, #8381, #21948, .T. ) ;
#3393=ORIENTED_EDGE ( 'NONE', *, *, #12383, .F. ) ;
#3397=ORIENTED_EDGE ( 'NONE', *, *, #7908, .T. ) ;
#3398=CIRCLE ( 'NONE', #21279, 0.2999999999999999334 ) ;
#3399=DIRECTION ( 'NONE',  ( 0.000000000000000000, 0.000000000000000000, 1.000000000000000000 ) ) ;
#3401=ORIENTED_EDGE ( 'NONE', *, *, #8232, .F. ) ;
#3403=EDGE_LOOP ( 'NONE', ( #10006, #6323, #7621, #7260 ) ) ;
#3404=DIRECTION ( 'NONE',  ( 1.000000000000000000, 0.000000000000000000, 0.000000000000000000 ) ) ;
#3406=DIRECTION ( 'NONE',  ( 0.000000000000000000, 0.000000000000000000, 1.000000000000000000 ) ) ;
#3409=CARTESIAN_POINT ( 'NONE',  ( 18.22752199202934520, 38.74634676501045760, 13.50000000000000000 ) ) ;
#3412=FACE_OUTER_BOUND ( 'NONE', #19014, .T. ) ;
#3414=DIRECTION ( 'NONE',  ( 0.000000000000000000, 0.000000000000000000, 1.000000000000000000 ) ) ;
#3416=VECTOR ( 'NONE', #9438, 1000.000000000000000 ) ;
#3417=ADVANCED_FACE ( 'NONE', ( #15532, #21046 ), #2227, .F. ) ;
#3418=EDGE_LOOP ( 'NONE', ( #16905, #13400, #6180, #10258 ) ) ;
#3422=ORIENTED_EDGE ( 'NONE', *, *, #15194, .F. ) ;
#3427=EDGE_LOOP ( 'NONE', ( #19693, #15433, #2178, #18069 ) ) ;
#3428=PLANE ( 'NONE',  #3498 ) ;
#3429=VECTOR ( 'NONE', #19814, 1000.000000000000000 ) ;
#3432=AXIS2_PLACEMENT_3D ( 'NONE', #15993, #3825, #19469 ) ;
#3433=TOROIDAL_SURFACE ( 'NONE', #15524, 1.300000000000000044, 0.2999999999999999889 ) ;
#3436=DIRECTION ( 'NONE',  ( -1.000000000000000000, 0.000000000000000000, 0.000000000000000000 ) ) ;
#3440=DIRECTION ( 'NONE',  ( -0.000000000000000000, -1.000000000000000000, -0.000000000000000000 ) ) ;
#3441=ORIENTED_EDGE ( 'NONE', *, *, #19638, .T. ) ;
#3442=CARTESIAN_POINT ( 'NONE',  ( 23.10708008847558759, 2.595912616485783087, 13.38952209624200584 ) ) ;
#3444=CARTESIAN_POINT ( 'NONE',  ( -25.37540678000427263, 68.74634676501045760, 7.200000000000000178 ) ) ;
#3449=AXIS2_PLACEMENT_3D ( 'NONE', #19594, #12527, #14325 ) ;
#3450=ADVANCED_FACE ( 'NONE', ( #20711 ), #325, .T. ) ;
#3451=DIRECTION ( 'NONE',  ( 1.000000000000000000, 0.000000000000000000, 0.000000000000000000 ) ) ;
#3453=CIRCLE ( 'NONE', #18081, 0.5000000000000004441 ) ;
#3455=FACE_OUTER_BOUND ( 'NONE', #20544, .T. ) ;
#3458=DIRECTION ( 'NONE',  ( 1.000000000000000000, 0.000000000000000000, 0.000000000000000000 ) ) ;
#3459=ORIENTED_EDGE ( 'NONE', *, *, #21583, .F. ) ;
#3460=AXIS2_PLACEMENT_3D ( 'NONE', #14713, #4657, #17959 ) ;
#3462=AXIS2_PLACEMENT_3D ( 'NONE', #2586, #1003, #6072 ) ;
#3464=DIRECTION ( 'NONE',  ( -0.000000000000000000, 1.000000000000000000, 0.000000000000000000 ) ) ;
#3466=CARTESIAN_POINT ( 'NONE',  ( 23.02398829872513986, 7.027230193580998154E-15, 13.79999999999999893 ) ) ;
#3467=CIRCLE ( 'NONE', #9532, 0.5000000000000004441 ) ;
#3468=FACE_OUTER_BOUND ( 'NONE', #21574, .T. ) ;
#3469=DIRECTION ( 'NONE',  ( 0.000000000000000000, 0.000000000000000000, 1.000000000000000000 ) ) ;
#3471=EDGE_CURVE ( 'NONE', #11153, #2242, #17823, .T. ) ;
#3475=ADVANCED_FACE ( 'NONE', ( #7175 ), #12176, .F. ) ;
#3476=CARTESIAN_POINT ( 'NONE',  ( -15.04741597961255728, -51.92573430214628871, 13.50000000000006750 ) ) ;
#3477=CIRCLE ( 'NONE', #15958, 2.000000000000000000 ) ;
#3478=VECTOR ( 'NONE', #11113, 1000.000000000000000 ) ;
#3479=AXIS2_PLACEMENT_3D ( 'NONE', #5245, #15307, #5025 ) ;
#3480=CARTESIAN_POINT ( 'NONE',  ( -29.17540678000427690, 63.74634676501045050, 7.500000000000000000 ) ) ;
#3481=LINE ( 'NONE', #11754, #20253 ) ;
#3483=DIRECTION ( 'NONE',  ( -0.000000000000000000, -0.000000000000000000, -1.000000000000000000 ) ) ;
#3484=ORIENTED_EDGE ( 'NONE', *, *, #18523, .T. ) ;
#3485=AXIS2_PLACEMENT_3D ( 'NONE', #7130, #20212, #4887 ) ;
#3487=FACE_OUTER_BOUND ( 'NONE', #12812, .T. ) ;
#3490=SURFACE_SIDE_STYLE ('',( #15116 ) ) ;
#3491=ORIENTED_EDGE ( 'NONE', *, *, #13198, .F. ) ;
#3494=AXIS2_PLACEMENT_3D ( 'NONE', #15072, #2772, #12938 ) ;
#3495=CIRCLE ( 'NONE', #3126, 0.2999999999999999334 ) ;
#3496=CARTESIAN_POINT ( 'NONE',  ( -4.127054932750482408, -32.93424481021354921, 7.321391277662001151 ) ) ;
#3497=CARTESIAN_POINT ( 'NONE',  ( 9.641460742840918030, -32.61873716947361856, 68.00000000000000000 ) ) ;
#3498=AXIS2_PLACEMENT_3D ( 'NONE', #5120, #1627, #15286 ) ;
#3499=DIRECTION ( 'NONE',  ( 0.000000000000000000, -0.000000000000000000, -1.000000000000000000 ) ) ;
#3500=AXIS2_PLACEMENT_3D ( 'NONE', #16487, #1153, #6445 ) ;
#3504=CARTESIAN_POINT ( 'NONE',  ( 15.95292532278785913, 50.11873716947361856, 13.79999999999999893 ) ) ;
#3505=EDGE_CURVE ( 'NONE', #9791, #6172, #18923, .T. ) ;
#3507=CARTESIAN_POINT ( 'NONE',  ( 23.21392692125925450, -3.086569931169083514, 13.48002932626963712 ) ) ;
#3508=CYLINDRICAL_SURFACE ( 'NONE', #9653, 0.2999999999999999334 ) ;
#3509=EDGE_CURVE ( 'NONE', #104, #20269, #5716, .T. ) ;
#3510=DIRECTION ( 'NONE',  ( 0.000000000000000000, 0.000000000000000000, 1.000000000000000000 ) ) ;
#3511=AXIS2_PLACEMENT_3D ( 'NONE', #20677, #5356, #2079 ) ;
#3518=ORIENTED_EDGE ( 'NONE', *, *, #5988, .F. ) ;
#3521=CIRCLE ( 'NONE', #17434, 0.3000000000000003775 ) ;
#3522=ADVANCED_FACE ( 'NONE', ( #4032 ), #4625, .T. ) ;
#3523=CARTESIAN_POINT ( 'NONE',  ( -14.66174975910705136, -42.11054587065083155, 13.50000000000000000 ) ) ;
#3524=EDGE_CURVE ( 'NONE', #8381, #225, #9626, .T. ) ;
#3525=DIRECTION ( 'NONE',  ( 1.000000000000000000, 0.000000000000000000, 0.000000000000000000 ) ) ;
#3526=CIRCLE ( 'NONE', #6034, 4.700000000000002842 ) ;
#3527=CARTESIAN_POINT ( 'NONE',  ( 15.95292532278785913, -50.11873716947361856, 13.99999999999999822 ) ) ;
#3529=DIRECTION ( 'NONE',  ( -0.000000000000000000, -0.000000000000000000, -1.000000000000000000 ) ) ;
#3530=PLANE ( 'NONE',  #13539 ) ;
#3531=CARTESIAN_POINT ( 'NONE',  ( -3.627054932750481964, 32.93424481021354921, 42.50000000000000000 ) ) ;
#3535=CARTESIAN_POINT ( 'NONE',  ( 15.95292532278785913, -32.61873716947361856, 68.50000000000000000 ) ) ;
#3541=DIRECTION ( 'NONE',  ( 0.000000000000000000, 0.000000000000000000, 1.000000000000000000 ) ) ;
#3544=ORIENTED_EDGE ( 'NONE', *, *, #6618, .T. ) ;
#3546=ORIENTED_EDGE ( 'NONE', *, *, #11006, .F. ) ;
#3549=FACE_OUTER_BOUND ( 'NONE', #950, .T. ) ;
#3550=AXIS2_PLACEMENT_3D ( 'NONE', #17534, #2423, #19428 ) ;
#3552=CIRCLE ( 'NONE', #12108, 0.5000000000000004441 ) ;
#3554=LINE ( 'NONE', #168, #16832 ) ;
#3557=ORIENTED_EDGE ( 'NONE', *, *, #5875, .T. ) ;
#3558=CARTESIAN_POINT ( 'NONE',  ( -23.02398829872513986, -3.005406968599071416, 13.74590378743879882 ) ) ;
#3559=EDGE_CURVE ( 'NONE', #10410, #17454, #21374, .T. ) ;
#3560=DIRECTION ( 'NONE',  ( 0.000000000000000000, 0.000000000000000000, -1.000000000000000000 ) ) ;
#3562=CARTESIAN_POINT ( 'NONE',  ( -31.63662752439705272, 0.000000000000000000, -18.50000000000000000 ) ) ;
#3564=ORIENTED_EDGE ( 'NONE', *, *, #8385, .T. ) ;
#3565=CARTESIAN_POINT ( 'NONE',  ( 23.26572410265648116, 3.298136152264957932, 13.49420500573775428 ) ) ;
#3569=EDGE_LOOP ( 'NONE', ( #2432, #14583, #6590, #21609 ) ) ;
#3572=CARTESIAN_POINT ( 'NONE',  ( -15.95292532278785913, 34.11873716947361856, 68.00000000000000000 ) ) ;
#3573=ORIENTED_EDGE ( 'NONE', *, *, #3348, .T. ) ;
#3575=CARTESIAN_POINT ( 'NONE',  ( -29.37540678000427619, 6.000000000000000000, 7.500000000000000000 ) ) ;
#3576=ORIENTED_EDGE ( 'NONE', *, *, #14050, .T. ) ;
#3579=ORIENTED_EDGE ( 'NONE', *, *, #4705, .T. ) ;
#3584=DIRECTION ( 'NONE',  ( 2.832483164223434527E-16, 1.000000000000000000, 0.000000000000000000 ) ) ;
#3585=CIRCLE ( 'NONE', #10737, 2.299999999999993161 ) ;
#3586=TOROIDAL_SURFACE ( 'NONE', #16062, 2.274596669241483848, 0.2999999999999999889 ) ;
#3588=CARTESIAN_POINT ( 'NONE',  ( 15.95292532278785913, 52.11873716947361856, 13.99999999999999822 ) ) ;
#3589=FACE_OUTER_BOUND ( 'NONE', #14175, .T. ) ;
#3592=CARTESIAN_POINT ( 'NONE',  ( 0.000000000000000000, 5.299999999999999822, 7.200000000000000178 ) ) ;
#3594=VECTOR ( 'NONE', #16206, 1000.000000000000000 ) ;
#3595=EDGE_LOOP ( 'NONE', ( #12234, #11194, #15690, #14804 ) ) ;
#3596=DIRECTION ( 'NONE',  ( -0.000000000000000000, -0.000000000000000000, -1.000000000000000000 ) ) ;
#3597=CYLINDRICAL_SURFACE ( 'NONE', #9198, 0.2999999999999999334 ) ;
#3600=EDGE_CURVE ( 'NONE', #13259, #12460, #11063, .T. ) ;
#3601=ORIENTED_EDGE ( 'NONE', *, *, #13761, .T. ) ;
#3603=CARTESIAN_POINT ( 'NONE',  ( -30.07540678000427548, -63.74634676501045050, 7.500000000000000000 ) ) ;
#3604=VERTEX_POINT ( 'NONE', #16434 ) ;
#3609=ORIENTED_EDGE ( 'NONE', *, *, #13336, .T. ) ;
#3611=CYLINDRICAL_SURFACE ( 'NONE', #19496, 0.2999999999999999334 ) ;
#3614=CARTESIAN_POINT ( 'NONE',  ( 23.02398829872514341, 2.501746539338821851, 13.57884938331724278 ) ) ;
#3618=FACE_OUTER_BOUND ( 'NONE', #12563, .T. ) ;
#3619=DIRECTION ( 'NONE',  ( 0.000000000000000000, 0.000000000000000000, 1.000000000000000000 ) ) ;
#3620=EDGE_CURVE ( 'NONE', #19432, #5550, #16838, .T. ) ;
#3624=ORIENTED_EDGE ( 'NONE', *, *, #15709, .T. ) ;
#3625=CARTESIAN_POINT ( 'NONE',  ( 14.66174975910705847, 42.11054587065083155, 13.50000000000000000 ) ) ;
#3632=DIRECTION ( 'NONE',  ( 1.000000000000000000, 0.000000000000000000, 0.000000000000000000 ) ) ;
#3633=VECTOR ( 'NONE', #21041, 1000.000000000000000 ) ;
#3636=DIRECTION ( 'NONE',  ( 1.000000000000000000, 0.000000000000000000, 0.000000000000000000 ) ) ;
#3637=CARTESIAN_POINT ( 'NONE',  ( 17.93704824106378837, 0.000000000000000000, 13.87500000000000000 ) ) ;
#3638=ORIENTED_EDGE ( 'NONE', *, *, #14725, .F. ) ;
#3640=CYLINDRICAL_SURFACE ( 'NONE', #320, 0.2999999999999999334 ) ;
#3641=DIRECTION ( 'NONE',  ( 1.000000000000000000, -0.000000000000000000, -0.000000000000000000 ) ) ;
#3643=DIRECTION ( 'NONE',  ( 0.000000000000000000, 0.000000000000000000, -1.000000000000000000 ) ) ;
#3644=LINE ( 'NONE', #14123, #16996 ) ;
#3645=CARTESIAN_POINT ( 'NONE',  ( -1.836970198721029934E-16, 72.00000000000001421, 1.800000000000000044 ) ) ;
#3649=CARTESIAN_POINT ( 'NONE',  ( -15.95292532278785913, -34.11873716947361856, 68.00000000000000000 ) ) ;
#3653=CARTESIAN_POINT ( 'NONE',  ( -29.13662752439705272, 0.000000000000000000, 13.50000000000000000 ) ) ;
#3656=CARTESIAN_POINT ( 'NONE',  ( 29.13662752439705272, 0.000000000000000000, 3.500000000000000000 ) ) ;
#3657=CIRCLE ( 'NONE', #2576, 4.051418481279139172 ) ;
#3658=CIRCLE ( 'NONE', #11500, 0.6999999999999992895 ) ;
#3661=ORIENTED_EDGE ( 'NONE', *, *, #18724, .F. ) ;
#3662=CARTESIAN_POINT ( 'NONE',  ( -25.37540678000427263, -66.94634676501046044, 13.19999999999999929 ) ) ;
#3663=EDGE_CURVE ( 'NONE', #19429, #20933, #6780, .T. ) ;
#3664=EDGE_LOOP ( 'NONE', ( #14267, #9014, #13412, #14288, #10618, #3638 ) ) ;
#3666=LINE ( 'NONE', #1763, #18150 ) ;
#3667=DIRECTION ( 'NONE',  ( 0.000000000000000000, 0.000000000000000000, 1.000000000000000000 ) ) ;
#3669=ORIENTED_EDGE ( 'NONE', *, *, #12333, .T. ) ;
#3670=CARTESIAN_POINT ( 'NONE',  ( 23.32398829872514057, 3.528912754968628995, 13.50000000000000178 ) ) ;
#3675=CARTESIAN_POINT ( 'NONE',  ( 31.50000000000002132, -71.70000000000001705, 1.500000000000000000 ) ) ;
#3676=ORIENTED_EDGE ( 'NONE', *, *, #12398, .T. ) ;
#3682=CARTESIAN_POINT ( 'NONE',  ( 0.000000000000000000, 5.299999999999999822, 7.200000000000000178 ) ) ;
#3683=EDGE_CURVE ( 'NONE', #5528, #14977, #21602, .T. ) ;
#3685=ORIENTED_EDGE ( 'NONE', *, *, #10122, .T. ) ;
#3686=ORIENTED_EDGE ( 'NONE', *, *, #8950, .F. ) ;
#3688=ORIENTED_EDGE ( 'NONE', *, *, #680, .T. ) ;
#3689=CARTESIAN_POINT ( 'NONE',  ( -29.50000000000002842, 2.473451120191013874, 0.2503166595423103602 ) ) ;
#3693=ORIENTED_EDGE ( 'NONE', *, *, #5591, .F. ) ;
#3695=DIRECTION ( 'NONE',  ( -1.000000000000000000, 0.000000000000000000, 0.000000000000000000 ) ) ;
#3699=FACE_OUTER_BOUND ( 'NONE', #11269, .T. ) ;
#3700=CARTESIAN_POINT ( 'NONE',  ( -14.96174975910705207, 51.76873716947361714, 13.79999999999999893 ) ) ;
#3708=CARTESIAN_POINT ( 'NONE',  ( 23.20982120895258660, -3.064530420494568475, 13.47289532992770233 ) ) ;
#3709=ORIENTED_EDGE ( 'NONE', *, *, #11363, .T. ) ;
#3712=CARTESIAN_POINT ( 'NONE',  ( 31.50000000000002132, 71.00000000000001421, 1.800000000000000044 ) ) ;
#3713=AXIS2_PLACEMENT_3D ( 'NONE', #15511, #297, #1875 ) ;
#3714=CARTESIAN_POINT ( 'NONE',  ( -28.87540678000427619, 0.000000000000000000, 7.799999999999999822 ) ) ;
#3719=AXIS2_PLACEMENT_3D ( 'NONE', #6960, #20258, #3360 ) ;
#3720=PLANE ( 'NONE',  #8657 ) ;
#3722=CARTESIAN_POINT ( 'NONE',  ( 23.07462249345254790, -2.431574673422045141, 13.33584746657814080 ) ) ;
#3723=CARTESIAN_POINT ( 'NONE',  ( 14.75227361591076480, -52.14371094704548426, 13.49999999999999467 ) ) ;
#3725=EDGE_CURVE ( 'NONE', #21935, #21679, #2257, .T. ) ;
#3727=EDGE_CURVE ( 'NONE', #12867, #1401, #17813, .T. ) ;
#3728=CARTESIAN_POINT ( 'NONE',  ( -3.127054932750481964, 32.61873716947361856, 68.00000000000000000 ) ) ;
#3729=VERTEX_POINT ( 'NONE', #7421 ) ;
#3733=ORIENTED_EDGE ( 'NONE', *, *, #925, .F. ) ;
#3734=ORIENTED_EDGE ( 'NONE', *, *, #3909, .T. ) ;
#3735=ADVANCED_FACE ( 'NONE', ( #18230 ), #18541, .F. ) ;
#3737=CARTESIAN_POINT ( 'NONE',  ( -30.37540678000427619, -63.74634676501045050, 7.500000000000000000 ) ) ;
#3738=ORIENTED_EDGE ( 'NONE', *, *, #7498, .F. ) ;
#3739=DIRECTION ( 'NONE',  ( -1.000000000000000000, -0.000000000000000000, -0.000000000000000000 ) ) ;
#3740=DIRECTION ( 'NONE',  ( 1.000000000000000000, 0.000000000000000000, 0.000000000000000000 ) ) ;
#3741=DIRECTION ( 'NONE',  ( 1.000000000000000000, 7.973140176887192922E-16, 0.000000000000000000 ) ) ;
#3746=EDGE_CURVE ( 'NONE', #19066, #11236, #989, .T. ) ;
#3747=CARTESIAN_POINT ( 'NONE',  ( 25.37540678000426908, 36.74634676501047181, 13.79999999999999893 ) ) ;
#3750=LINE ( 'NONE', #17507, #8481 ) ;
#3751=ORIENTED_EDGE ( 'NONE', *, *, #11193, .T. ) ;
#3752=AXIS2_PLACEMENT_3D ( 'NONE', #1342, #8299, #8195 ) ;
#3755=CARTESIAN_POINT ( 'NONE',  ( 27.75399754406947750, -2.121775353753131643, 0.1432465332877360387 ) ) ;
#3757=FACE_OUTER_BOUND ( 'NONE', #6833, .T. ) ;
#3761=ADVANCED_FACE ( 'NONE', ( #19918 ), #7715, .T. ) ;
#3762=ORIENTED_EDGE ( 'NONE', *, *, #7767, .T. ) ;
#3763=CARTESIAN_POINT ( 'NONE',  ( 31.50000000000002132, 71.70000000000001705, 1.500000000000000000 ) ) ;
#3766=CYLINDRICAL_SURFACE ( 'NONE', #12197, 0.5000000000000004441 ) ;
#3767=CIRCLE ( 'NONE', #5199, 1.299999999999999156 ) ;
#3768=CARTESIAN_POINT ( 'NONE',  ( 29.13662752439705272, 0.000000000000000000, 13.19999999999999929 ) ) ;
#3770=CARTESIAN_POINT ( 'NONE',  ( 23.13120573414546399, 2.711843391866131103, 13.41529098820777222 ) ) ;
#3774=ORIENTED_EDGE ( 'NONE', *, *, #14689, .T. ) ;
#3775=CARTESIAN_POINT ( 'NONE',  ( 17.45292532278785913, 0.000000000000000000, 14.00000000000000000 ) ) ;
#3776=EDGE_CURVE ( 'NONE', #7580, #13533, #18105, .T. ) ;
#3777=ORIENTED_EDGE ( 'NONE', *, *, #10168, .T. ) ;
#3780=DIRECTION ( 'NONE',  ( -0.000000000000000000, -0.000000000000000000, 1.000000000000000000 ) ) ;
#3782=CIRCLE ( 'NONE', #15543, 0.2999999999999999334 ) ;
#3783=VERTEX_POINT ( 'NONE', #16536 ) ;
#3785=EDGE_CURVE ( 'NONE', #7349, #16038, #17993, .T. ) ;
#3787=ORIENTED_EDGE ( 'NONE', *, *, #100, .F. ) ;
#3789=ORIENTED_EDGE ( 'NONE', *, *, #15261, .T. ) ;
#3790=AXIS2_PLACEMENT_3D ( 'NONE', #3311, #8579, #3414 ) ;
#3791=CIRCLE ( 'NONE', #21298, 0.3000000000000003775 ) ;
#3796=CIRCLE ( 'NONE', #7038, 0.5000000000000004441 ) ;
#3800=CARTESIAN_POINT ( 'NONE',  ( 29.01868551570922605, 6.499165645473476971, 7.532495484408729958 ) ) ;
#3801=CYLINDRICAL_SURFACE ( 'NONE', #16725, 0.5000000000000004441 ) ;
#3802=ADVANCED_FACE ( 'NONE', ( #20033 ), #14855, .T. ) ;
#3804=ORIENTED_EDGE ( 'NONE', *, *, #637, .T. ) ;
#3805=CARTESIAN_POINT ( 'NONE',  ( 26.37540678000427619, 10.94079601157914539, 13.79999999999999893 ) ) ;
#3807=VECTOR ( 'NONE', #15902, 1000.000000000000000 ) ;
#3808=DIRECTION ( 'NONE',  ( -1.000000000000000000, 0.000000000000000000, 0.000000000000000000 ) ) ;
#3812=CARTESIAN_POINT ( 'NONE',  ( -23.32398829872514057, 5.683640910026983128, 13.79999999999999893 ) ) ;
#3813=DIRECTION ( 'NONE',  ( 0.000000000000000000, 0.000000000000000000, 1.000000000000000000 ) ) ;
#3816=CIRCLE ( 'NONE', #13805, 0.2999999999999999334 ) ;
#3817=ORIENTED_EDGE ( 'NONE', *, *, #2205, .F. ) ;
#3818=TOROIDAL_SURFACE ( 'NONE', #1289, 1.500000000000000000, 0.5000000000000000000 ) ;
#3822=CARTESIAN_POINT ( 'NONE',  ( 23.02398829872514341, -2.157133714763071364, 13.26827027136048720 ) ) ;
#3824=VERTEX_POINT ( 'NONE', #21930 ) ;
#3825=DIRECTION ( 'NONE',  ( -0.000000000000000000, -0.000000000000000000, -1.000000000000000000 ) ) ;
#3826=EDGE_CURVE ( 'NONE', #11974, #1033, #11727, .T. ) ;
#3828=DIRECTION ( 'NONE',  ( -1.000000000000000000, 0.000000000000000000, 0.000000000000000000 ) ) ;
#3829=CIRCLE ( 'NONE', #21714, 0.5000000000000004441 ) ;
#3831=EDGE_CURVE ( 'NONE', #18, #15927, #13401, .T. ) ;
#3840=CARTESIAN_POINT ( 'NONE',  ( -29.17540678000427690, 0.000000000000000000, 7.799999999999999822 ) ) ;
#3841=CARTESIAN_POINT ( 'NONE',  ( -15.05282292896044005, -52.05812657117054698, 13.87232935072191964 ) ) ;
#3844=DIRECTION ( 'NONE',  ( -0.000000000000000000, -0.000000000000000000, 1.000000000000000000 ) ) ;
#3845=CARTESIAN_POINT ( 'NONE',  ( 4.127054932750481520, 32.93424481021354921, 68.00000000000000000 ) ) ;
#3846=EDGE_LOOP ( 'NONE', ( #2048, #8028, #20970 ) ) ;
#3848=VECTOR ( 'NONE', #17551, 1000.000000000000000 ) ;
#3853=AXIS2_PLACEMENT_3D ( 'NONE', #7641, #5226, #12135 ) ;
#3854=ADVANCED_FACE ( 'NONE', ( #6501 ), #18667, .F. ) ;
#3858=DIRECTION ( 'NONE',  ( 1.000000000000000000, -0.000000000000000000, 0.000000000000000000 ) ) ;
#3860=CARTESIAN_POINT ( 'NONE',  ( -31.50000000000002132, -71.70000000000001705, 1.800000000000000044 ) ) ;
#3861=FACE_OUTER_BOUND ( 'NONE', #15919, .T. ) ;
#3863=AXIS2_PLACEMENT_3D ( 'NONE', #7830, #8259, #3101 ) ;
#3865=VECTOR ( 'NONE', #11253, 1000.000000000000000 ) ;
#3866=DIRECTION ( 'NONE',  ( 1.000000000000000000, 0.000000000000000000, 0.000000000000000000 ) ) ;
#3867=DIRECTION ( 'NONE',  ( -1.000000000000000000, 0.000000000000000000, 0.000000000000000000 ) ) ;
#3868=ORIENTED_EDGE ( 'NONE', *, *, #21691, .F. ) ;
#3869=CARTESIAN_POINT ( 'NONE',  ( -17.95292532278785913, -38.74634676501045760, 109.6002446535588319 ) ) ;
#3870=CARTESIAN_POINT ( 'NONE',  ( -31.50000000000002132, 71.00000000000001421, 3.200000000000000178 ) ) ;
#3872=CARTESIAN_POINT ( 'NONE',  ( -4.127054932750482408, 32.93424481021354921, 68.50000000000000000 ) ) ;
#3873=EDGE_LOOP ( 'NONE', ( #4239, #18841, #20135, #8926 ) ) ;
#3874=VECTOR ( 'NONE', #2489, 1000.000000000000000 ) ;
#3875=ORIENTED_EDGE ( 'NONE', *, *, #14973, .T. ) ;
#3876=CARTESIAN_POINT ( 'NONE',  ( 26.61833302554978786, -9.663695060508651125, 13.50000000000000000 ) ) ;
#3877=DIRECTION ( 'NONE',  ( -1.000000000000000000, 0.000000000000000000, 0.000000000000000000 ) ) ;
#3878=AXIS2_PLACEMENT_3D ( 'NONE', #6966, #8742, #215 ) ;
#3879=CARTESIAN_POINT ( 'NONE',  ( -23.83662752439705201, 0.000000000000000000, 7.200000000000000178 ) ) ;
#3880=ORIENTED_EDGE ( 'NONE', *, *, #12416, .F. ) ;
#3882=EDGE_LOOP ( 'NONE', ( #8952, #17672, #4314, #13954, #3868 ) ) ;
#3885=AXIS2_PLACEMENT_3D ( 'NONE', #21490, #21597, #10059 ) ;
#3886=ADVANCED_FACE ( 'NONE', ( #20578 ), #20136, .F. ) ;
#3888=ADVANCED_FACE ( 'NONE', ( #18333 ), #4956, .F. ) ;
#3891=AXIS2_PLACEMENT_3D ( 'NONE', #2960, #15137, #21983 ) ;
#3892=CARTESIAN_POINT ( 'NONE',  ( -18.22752199202934520, -38.74634676501045760, 13.50000000000000000 ) ) ;
#3893=VECTOR ( 'NONE', #7183, 1000.000000000000000 ) ;
#3898=CARTESIAN_POINT ( 'NONE',  ( -32.50000000000002132, 72.00000000000001421, 3.500000000000000000 ) ) ;
#3901=ORIENTED_EDGE ( 'NONE', *, *, #14416, .F. ) ;
#3904=LINE ( 'NONE', #9140, #4117 ) ;
#3909=EDGE_CURVE ( 'NONE', #6564, #8381, #10674, .T. ) ;
#3911=VECTOR ( 'NONE', #20198, 1000.000000000000000 ) ;
#3913=AXIS2_PLACEMENT_3D ( 'NONE', #14493, #21474, #19668 ) ;
#3918=DIRECTION ( 'NONE',  ( 0.000000000000000000, 0.000000000000000000, 1.000000000000000000 ) ) ;
#3920=DIRECTION ( 'NONE',  ( 1.000000000000000000, 0.000000000000000000, 0.000000000000000000 ) ) ;
#3921=CARTESIAN_POINT ( 'NONE',  ( 28.90801073195815718, 6.496214187273303686, 7.643093741255248652 ) ) ;
#3922=EDGE_CURVE ( 'NONE', #12867, #12488, #5032, .T. ) ;
#3923=FACE_OUTER_BOUND ( 'NONE', #10614, .T. ) ;
#3925=DIRECTION ( 'NONE',  ( 0.000000000000000000, 0.000000000000000000, -1.000000000000000000 ) ) ;
#3927=CARTESIAN_POINT ( 'NONE',  ( -32.20000000000001705, 0.000000000000000000, 1.800000000000000044 ) ) ;
#3929=DIRECTION ( 'NONE',  ( -0.000000000000000000, 0.000000000000000000, 1.000000000000000000 ) ) ;
#3933=ORIENTED_EDGE ( 'NONE', *, *, #13752, .T. ) ;
#3934=ORIENTED_EDGE ( 'NONE', *, *, #11504, .F. ) ;
#3938=AXIS2_PLACEMENT_3D ( 'NONE', #21110, #7019, #387 ) ;
#3940=CARTESIAN_POINT ( 'NONE',  ( 23.04273161205366449, -2.261511134070602225, 13.23413512703649531 ) ) ;
#3941=ORIENTED_EDGE ( 'NONE', *, *, #21945, .T. ) ;
#3942=EDGE_CURVE ( 'NONE', #17693, #2296, #19254, .T. ) ;
#3945=CARTESIAN_POINT ( 'NONE',  ( -32.50000000000002132, -71.00000000000001421, 3.500000000000000000 ) ) ;
#3946=DIRECTION ( 'NONE',  ( 0.000000000000000000, -1.000000000000000000, 0.000000000000000000 ) ) ;
#3949=CARTESIAN_POINT ( 'NONE',  ( -32.20000000000001705, -71.00000000000001421, 3.200000000000000178 ) ) ;
#3950=CIRCLE ( 'NONE', #19308, 1.000000000000000888 ) ;
#3952=DIRECTION ( 'NONE',  ( -1.000000000000000000, 0.000000000000000000, 0.000000000000000000 ) ) ;
#3954=CARTESIAN_POINT ( 'NONE',  ( 23.14079623692856202, -2.756488901337828423, 13.42422799743261130 ) ) ;
#3955=CARTESIAN_POINT ( 'NONE',  ( -25.37540678000426908, 36.74634676501047181, 13.79999999999999893 ) ) ;
#3956=CARTESIAN_POINT ( 'NONE',  ( 30.37540678000427619, -63.74634676501045050, 7.200000000000000178 ) ) ;
#3957=ORIENTED_EDGE ( 'NONE', *, *, #13340, .F. ) ;
#3958=ORIENTED_EDGE ( 'NONE', *, *, #21151, .F. ) ;
#3959=DIRECTION ( 'NONE',  ( 1.000000000000000000, 0.000000000000000000, 0.000000000000000000 ) ) ;
#3961=DIRECTION ( 'NONE',  ( 1.000000000000000000, 0.000000000000000000, 0.000000000000000000 ) ) ;
#3964=ORIENTED_EDGE ( 'NONE', *, *, #4895, .F. ) ;
#3966=VECTOR ( 'NONE', #15376, 1000.000000000000000 ) ;
#3967=VECTOR ( 'NONE', #4270, 1000.000000000000000 ) ;
#3973=CARTESIAN_POINT ( 'NONE',  ( 14.96174975910705918, 41.81054587065082728, 13.80000000000001315 ) ) ;
#3975=CARTESIAN_POINT ( 'NONE',  ( 9.641460742840918030, -32.11873716947361856, 42.50000000000000711 ) ) ;
#3978=LINE ( 'NONE', #19628, #19350 ) ;
#3980=CARTESIAN_POINT ( 'NONE',  ( -17.45292532278785913, 50.11873716947361856, 68.50000000000000000 ) ) ;
#3983=VERTEX_POINT ( 'NONE', #14289 ) ;
#3985=CARTESIAN_POINT ( 'NONE',  ( -28.87540678000427619, -6.494748934539263274, 7.720760502796167657 ) ) ;
#3987=ADVANCED_FACE ( 'NONE', ( #17543 ), #17642, .F. ) ;
#3988=ORIENTED_EDGE ( 'NONE', *, *, #21149, .T. ) ;
#3989=EDGE_CURVE ( 'NONE', #19805, #2320, #660, .T. ) ;
#3990=PLANE ( 'NONE',  #17070 ) ;
#3991=VECTOR ( 'NONE', #5102, 1000.000000000000000 ) ;
#3996=DIRECTION ( 'NONE',  ( 0.000000000000000000, 0.000000000000000000, 1.000000000000000000 ) ) ;
#3998=CARTESIAN_POINT ( 'NONE',  ( -23.04273156199908357, -2.261510999192740901, 13.19999999999999929 ) ) ;
#4004=DIRECTION ( 'NONE',  ( 1.000000000000000000, 0.000000000000000000, 0.000000000000000000 ) ) ;
#4006=CARTESIAN_POINT ( 'NONE',  ( 14.96174975910707161, 51.61873716947361856, 68.25000000000000000 ) ) ;
#4007=VERTEX_POINT ( 'NONE', #15518 ) ;
#4011=ORIENTED_EDGE ( 'NONE', *, *, #2853, .T. ) ;
#4013=CARTESIAN_POINT ( 'NONE',  ( 3.127054932750481964, 32.93424481021354921, 68.50000000000000000 ) ) ;
#4018=EDGE_CURVE ( 'NONE', #15927, #1798, #13881, .T. ) ;
#4024=CYLINDRICAL_SURFACE ( 'NONE', #1335, 0.2500000000000002220 ) ;
#4027=DIRECTION ( 'NONE',  ( 1.000000000000000000, -0.000000000000000000, -0.000000000000000000 ) ) ;
#4028=DIRECTION ( 'NONE',  ( 0.000000000000000000, 0.000000000000000000, 1.000000000000000000 ) ) ;
#4029=ADVANCED_FACE ( 'NONE', ( #15952 ), #5372, .T. ) ;
#4030=EDGE_LOOP ( 'NONE', ( #15499, #14800, #11070, #20164 ) ) ;
#4031=DIRECTION ( 'NONE',  ( -0.000000000000000000, -0.000000000000000000, 1.000000000000000000 ) ) ;
#4032=FACE_OUTER_BOUND ( 'NONE', #5420, .T. ) ;
#4034=ORIENTED_EDGE ( 'NONE', *, *, #16966, .F. ) ;
#4037=ADVANCED_FACE ( 'NONE', ( #850 ), #4607, .T. ) ;
#4038=VERTEX_POINT ( 'NONE', #4440 ) ;
#4040=FACE_OUTER_BOUND ( 'NONE', #11642, .T. ) ;
#4043=LINE ( 'NONE', #9070, #7588 ) ;
#4045=DIRECTION ( 'NONE',  ( 0.000000000000000000, 0.000000000000000000, -1.000000000000000000 ) ) ;
#4047=DIRECTION ( 'NONE',  ( 0.000000000000000000, 1.000000000000000000, 0.000000000000000000 ) ) ;
#4051=FACE_OUTER_BOUND ( 'NONE', #14789, .T. ) ;
#4052=CYLINDRICAL_SURFACE ( 'NONE', #19019, 0.5000000000000004441 ) ;
#4053=CARTESIAN_POINT ( 'NONE',  ( -25.37540678000426908, 39.04634676501046187, 13.79999999999999893 ) ) ;
#4055=EDGE_CURVE ( 'NONE', #16591, #13276, #7844, .T. ) ;
#4061=EDGE_CURVE ( 'NONE', #21319, #10096, #16411, .T. ) ;
#4066=LINE ( 'NONE', #10883, #11993 ) ;
#4068=LINE ( 'NONE', #699, #717 ) ;
#4069=CARTESIAN_POINT ( 'NONE',  ( -23.32398829872514057, 2.157133568460765982, 13.19999999999999929 ) ) ;
#4070=EDGE_CURVE ( 'NONE', #18637, #16490, #19779, .T. ) ;
#4072=CARTESIAN_POINT ( 'NONE',  ( 15.12813070831323969, 51.99253567353609640, 13.49999999999999822 ) ) ;
#4073=DIRECTION ( 'NONE',  ( 1.000000000000000000, -0.000000000000000000, -0.000000000000000000 ) ) ;
#4074=CARTESIAN_POINT ( 'NONE',  ( -25.37540678000427263, -69.04634676501045476, 3.500000000000000000 ) ) ;
#4075=AXIS2_PLACEMENT_3D ( 'NONE', #4100, #948, #9358 ) ;
#4077=DIRECTION ( 'NONE',  ( -1.000000000000000000, 0.000000000000000000, -0.000000000000000000 ) ) ;
#4081=EDGE_LOOP ( 'NONE', ( #11201, #10599, #2640, #14360 ) ) ;
#4083=EDGE_CURVE ( 'NONE', #8790, #18066, #21418, .T. ) ;
#4092=CARTESIAN_POINT ( 'NONE',  ( -28.71290943744531177, -6.649236572130504896, 13.47739020623642325 ) ) ;
#4093=DIRECTION ( 'NONE',  ( 1.000000000000000000, 0.000000000000000000, 0.000000000000000000 ) ) ;
#4096=ORIENTED_EDGE ( 'NONE', *, *, #19214, .F. ) ;
#4098=DIRECTION ( 'NONE',  ( 1.000000000000000000, 0.000000000000000000, 0.000000000000000000 ) ) ;
#4099=EDGE_CURVE ( 'NONE', #8904, #7257, #14603, .T. ) ;
#4100=CARTESIAN_POINT ( 'NONE',  ( -27.37540678000427619, 7.754037881813018962E-15, 42.50000000000000000 ) ) ;
#4102=VERTEX_POINT ( 'NONE', #7928 ) ;
#4104=DIRECTION ( 'NONE',  ( 1.000000000000000000, 0.000000000000000000, 0.000000000000000000 ) ) ;
#4106=ORIENTED_EDGE ( 'NONE', *, *, #18160, .T. ) ;
#4107=DIRECTION ( 'NONE',  ( -0.000000000000000000, -0.000000000000000000, -1.000000000000000000 ) ) ;
#4108=DIRECTION ( 'NONE',  ( 1.000000000000000000, 0.000000000000000000, 0.000000000000000000 ) ) ;
#4112=CARTESIAN_POINT ( 'NONE',  ( -0.000000000000000000, 51.61873716947361856, 68.50000000000000000 ) ) ;
#4113=VERTEX_POINT ( 'NONE', #11375 ) ;
#4116=EDGE_CURVE ( 'NONE', #16814, #2496, #744, .T. ) ;
#4117=VECTOR ( 'NONE', #10606, 1000.000000000000000 ) ;
#4118=AXIS2_PLACEMENT_3D ( 'NONE', #10061, #21820, #6605 ) ;
#4119=VERTEX_POINT ( 'NONE', #16068 ) ;
#4121=LINE ( 'NONE', #2221, #7958 ) ;
#4125=CARTESIAN_POINT ( 'NONE',  ( -9.141460742840918030, -32.61873716947361856, 68.00000000000000000 ) ) ;
#4126=VERTEX_POINT ( 'NONE', #7820 ) ;
#4127=AXIS2_PLACEMENT_3D ( 'NONE', #7840, #12837, #16433 ) ;
#4129=PLANE ( 'NONE',  #19747 ) ;
#4133=ORIENTED_EDGE ( 'NONE', *, *, #20262, .T. ) ;
#4135=ORIENTED_EDGE ( 'NONE', *, *, #16489, .F. ) ;
#4140=ORIENTED_EDGE ( 'NONE', *, *, #6373, .F. ) ;
#4141=VERTEX_POINT ( 'NONE', #2543 ) ;
#4145=CARTESIAN_POINT ( 'NONE',  ( -25.37540678000427263, -68.74634676501045760, 3.799999999999999822 ) ) ;
#4149=CARTESIAN_POINT ( 'NONE',  ( 30.67540678000428045, -63.74634676501045050, 3.799999999999999822 ) ) ;
#4150=FACE_OUTER_BOUND ( 'NONE', #15721, .T. ) ;
#4151=CARTESIAN_POINT ( 'NONE',  ( -4.127054932750482408, 33.93424481021354921, 68.50000000000000000 ) ) ;
#4153=DIRECTION ( 'NONE',  ( -0.000000000000000000, 0.000000000000000000, -1.000000000000000000 ) ) ;
#4155=DIRECTION ( 'NONE',  ( 1.000000000000000000, 2.832483164223434527E-16, -0.000000000000000000 ) ) ;
#4159=CIRCLE ( 'NONE', #14161, 0.2999999999999999334 ) ;
#4160=TOROIDAL_SURFACE ( 'NONE', #20249, 5.300000000000004263, 0.2999999999999999889 ) ;
#4161=DIRECTION ( 'NONE',  ( -0.000000000000000000, 0.000000000000000000, 1.000000000000000000 ) ) ;
#4162=ORIENTED_EDGE ( 'NONE', *, *, #8286, .T. ) ;
#4163=AXIS2_PLACEMENT_3D ( 'NONE', #17815, #9529, #21628 ) ;
#4164=ORIENTED_EDGE ( 'NONE', *, *, #16909, .F. ) ;
#4165=LINE ( 'NONE', #21193, #10313 ) ;
#4166=PLANE ( 'NONE',  #7070 ) ;
#4168=ORIENTED_EDGE ( 'NONE', *, *, #4594, .F. ) ;
#4172=TOROIDAL_SURFACE ( 'NONE', #18110, 0.7000000000000000666, 0.2999999999999999889 ) ;
#4173=CARTESIAN_POINT ( 'NONE',  ( -14.71432562863492066, -52.07267296161941061, 13.50000000000000000 ) ) ;
#4176=CIRCLE ( 'NONE', #2031, 0.2999999999999999334 ) ;
#4177=ORIENTED_EDGE ( 'NONE', *, *, #12589, .F. ) ;
#4178=CARTESIAN_POINT ( 'NONE',  ( 17.93704824106378837, -50.11873716947361856, 13.87500000000000000 ) ) ;
#4179=ADVANCED_FACE ( 'NONE', ( #16739 ), #797, .F. ) ;
#4180=DIRECTION ( 'NONE',  ( 1.000000000000000000, 0.000000000000000000, 0.000000000000000000 ) ) ;
#4183=CARTESIAN_POINT ( 'NONE',  ( -23.11756190325308680, 2.646657027129579287, 13.40142076604336019 ) ) ;
#4185=DIRECTION ( 'NONE',  ( 0.000000000000000000, -0.000000000000000000, 1.000000000000000000 ) ) ;
#4187=AXIS2_PLACEMENT_3D ( 'NONE', #8975, #19271, #3828 ) ;
#4188=CYLINDRICAL_SURFACE ( 'NONE', #9541, 0.2999999999999999334 ) ;
#4189=ORIENTED_EDGE ( 'NONE', *, *, #7989, .F. ) ;
#4193=EDGE_LOOP ( 'NONE', ( #20995, #12184, #15162, #16561 ) ) ;
#4194=CARTESIAN_POINT ( 'NONE',  ( -29.20000000000002061, 0.000000000000000000, 0.2999999999999947153 ) ) ;
#4195=DIRECTION ( 'NONE',  ( 0.000000000000000000, 0.000000000000000000, -1.000000000000000000 ) ) ;
#4196=EDGE_CURVE ( 'NONE', #21191, #21353, #16337, .T. ) ;
#4197=CIRCLE ( 'NONE', #4921, 1.000000000000000000 ) ;
#4200=ORIENTED_EDGE ( 'NONE', *, *, #13550, .F. ) ;
#4201=CARTESIAN_POINT ( 'NONE',  ( 9.641460742840918030, 32.61873716947361856, 109.6002446535588319 ) ) ;
#4204=LINE ( 'NONE', #21333, #4939 ) ;
#4206=AXIS2_PLACEMENT_3D ( 'NONE', #16886, #3464, #3133 ) ;
#4207=AXIS2_PLACEMENT_3D ( 'NONE', #8946, #10834, #2325 ) ;
#4209=PLANE ( 'NONE',  #15060 ) ;
#4213=EDGE_CURVE ( 'NONE', #14801, #5317, #10996, .T. ) ;
#4217=CARTESIAN_POINT ( 'NONE',  ( -23.11743451022279316, -2.646042693280195923, 13.40127653599240887 ) ) ;
#4219=( LENGTH_UNIT ( ) NAMED_UNIT ( * ) SI_UNIT ( .MILLI., .METRE. ) );
#4221=DIRECTION ( 'NONE',  ( -1.000000000000000000, 0.000000000000000000, 0.000000000000000000 ) ) ;
#4222=AXIS2_PLACEMENT_3D ( 'NONE', #9420, #19950, #21525 ) ;
#4223=EDGE_LOOP ( 'NONE', ( #16220, #5972, #20805, #1103 ) ) ;
#4226=ORIENTED_EDGE ( 'NONE', *, *, #17322, .T. ) ;
#4229=CARTESIAN_POINT ( 'NONE',  ( 30.37540678000427619, 0.000000000000000000, 7.500000000000000000 ) ) ;
#4230=CIRCLE ( 'NONE', #3511, 5.300000000000006040 ) ;
#4231=AXIS2_PLACEMENT_3D ( 'NONE', #14290, #10830, #5713 ) ;
#4234=ADVANCED_FACE ( 'NONE', ( #8698 ), #12406, .F. ) ;
#4235=AXIS2_PLACEMENT_3D ( 'NONE', #424, #15643, #526 ) ;
#4239=ORIENTED_EDGE ( 'NONE', *, *, #18724, .T. ) ;
#4240=CYLINDRICAL_SURFACE ( 'NONE', #11709, 5.000000000000004441 ) ;
#4242=CARTESIAN_POINT ( 'NONE',  ( 15.21174975910707161, 51.61873716947361856, 68.25000000000000000 ) ) ;
#4245=VERTEX_POINT ( 'NONE', #385 ) ;
#4247=CARTESIAN_POINT ( 'NONE',  ( -28.87540678000427619, -6.494748934539263274, 13.19999999999999929 ) ) ;
#4249=CIRCLE ( 'NONE', #19611, 5.000000000000004441 ) ;
#4254=VERTEX_POINT ( 'NONE', #21288 ) ;
#4255=ORIENTED_EDGE ( 'NONE', *, *, #9755, .F. ) ;
#4256=LINE ( 'NONE', #17889, #9959 ) ;
#4258=ORIENTED_EDGE ( 'NONE', *, *, #8634, .T. ) ;
#4259=EDGE_LOOP ( 'NONE', ( #2461, #19521, #926, #13192 ) ) ;
#4260=EDGE_CURVE ( 'NONE', #21299, #15569, #12026, .T. ) ;
#4261=B_SPLINE_CURVE_WITH_KNOTS ( 'NONE', 3,
 ( #2383, #16658, #1337, #6518, #2271, #1007, #20048, #18346, #9214, #21097, #19398, #16329 ),
 .UNSPECIFIED., .F., .F.,
 ( 4, 2, 2, 2, 2, 4 ),
 ( 0.000000000000000000, 0.0006847042422322839909, 0.001027056363348426583, 0.001198232423906498041, 0.001283820454185535071, 0.001369408484464571885 ),
 .UNSPECIFIED. ) ;
#4263=ORIENTED_EDGE ( 'NONE', *, *, #7348, .T. ) ;
#4264=DIRECTION ( 'NONE',  ( 0.000000000000000000, -0.000000000000000000, 1.000000000000000000 ) ) ;
#4267=CARTESIAN_POINT ( 'NONE',  ( 27.77120804565220169, -2.094189496455408861, -150.0833101980363722 ) ) ;
#4270=DIRECTION ( 'NONE',  ( 0.000000000000000000, 0.000000000000000000, 1.000000000000000000 ) ) ;
#4272=DIRECTION ( 'NONE',  ( 0.000000000000000000, 0.000000000000000000, 1.000000000000000000 ) ) ;
#4276=AXIS2_PLACEMENT_3D ( 'NONE', #12942, #2776, #21592 ) ;
#4277=AXIS2_PLACEMENT_3D ( 'NONE', #18951, #13672, #10446 ) ;
#4282=CARTESIAN_POINT ( 'NONE',  ( -15.21174975910705207, 51.61873716947361856, 68.25000000000000000 ) ) ;
#4286=AXIS2_PLACEMENT_3D ( 'NONE', #22017, #5233, #8596 ) ;
#4288=DIRECTION ( 'NONE',  ( 0.000000000000000000, -0.000000000000000000, -1.000000000000000000 ) ) ;
#4289=AXIS2_PLACEMENT_3D ( 'NONE', #12446, #19177, #17603 ) ;
#4293=EDGE_CURVE ( 'NONE', #8378, #8119, #5307, .T. ) ;
#4294=DIRECTION ( 'NONE',  ( -0.000000000000000000, -0.000000000000000000, -1.000000000000000000 ) ) ;
#4299=CARTESIAN_POINT ( 'NONE',  ( 28.64417692495746692, -6.713479613976641502, 13.50000000000000000 ) ) ;
#4300=DIRECTION ( 'NONE',  ( 0.000000000000000000, -0.000000000000000000, 1.000000000000000000 ) ) ;
#4302=ORIENTED_EDGE ( 'NONE', *, *, #17016, .T. ) ;
#4303=EDGE_LOOP ( 'NONE', ( #2109, #8572, #3518, #10200 ) ) ;
#4304=EDGE_LOOP ( 'NONE', ( #2472, #19545, #17213, #17566 ) ) ;
#4309=ORIENTED_EDGE ( 'NONE', *, *, #2603, .T. ) ;
#4310=VECTOR ( 'NONE', #14656, 1000.000000000000000 ) ;
#4314=ORIENTED_EDGE ( 'NONE', *, *, #11025, .F. ) ;
#4315=CARTESIAN_POINT ( 'NONE',  ( 0.000000000000000000, 0.000000000000000000, 13.50000000000000000 ) ) ;
#4319=DIRECTION ( 'NONE',  ( -2.388292521039847891E-16, -0.000000000000000000, -1.000000000000000000 ) ) ;
#4322=FACE_OUTER_BOUND ( 'NONE', #12132, .T. ) ;
#4326=DIRECTION ( 'NONE',  ( -0.000000000000000000, -0.000000000000000000, -1.000000000000000000 ) ) ;
#4328=ORIENTED_EDGE ( 'NONE', *, *, #13137, .T. ) ;
#4330=CARTESIAN_POINT ( 'NONE',  ( -15.21174975910705207, 41.81054587065082728, 68.50000000000000000 ) ) ;
#4333=DIRECTION ( 'NONE',  ( 1.000000000000000000, 0.000000000000000000, 0.000000000000000000 ) ) ;
#4334=VERTEX_POINT ( 'NONE', #8908 ) ;
#4335=ORIENTED_EDGE ( 'NONE', *, *, #19403, .F. ) ;
#4336=CARTESIAN_POINT ( 'NONE',  ( -29.20000000000002061, 68.70000000000001705, 0.000000000000000000 ) ) ;
#4338=AXIS2_PLACEMENT_3D ( 'NONE', #7681, #17415, #17632 ) ;
#4345=EDGE_LOOP ( 'NONE', ( #1134, #1048, #9718, #6847 ) ) ;
#4346=CARTESIAN_POINT ( 'NONE',  ( -8.641460742840918030, 33.93424481021354921, 68.50000000000000000 ) ) ;
#4348=DIRECTION ( 'NONE',  ( 0.000000000000000000, -1.000000000000000000, 0.000000000000000000 ) ) ;
#4349=VECTOR ( 'NONE', #475, 1000.000000000000000 ) ;
#4351=CARTESIAN_POINT ( 'NONE',  ( 32.20000000000001705, 71.00000000000001421, 3.500000000000000000 ) ) ;
#4352=DIRECTION ( 'NONE',  ( 0.000000000000000000, 1.000000000000000000, 0.000000000000000000 ) ) ;
#4354=DIRECTION ( 'NONE',  ( -0.000000000000000000, -1.000000000000000000, 0.000000000000000000 ) ) ;
#4358=EDGE_CURVE ( 'NONE', #2540, #16676, #4616, .T. ) ;
#4360=CARTESIAN_POINT ( 'NONE',  ( -17.95292532278785913, -34.11873716947361856, 68.00000000000000000 ) ) ;
#4364=DIRECTION ( 'NONE',  ( -1.000000000000000000, 0.000000000000000000, 0.000000000000000000 ) ) ;
#4365=EDGE_CURVE ( 'NONE', #852, #16858, #14886, .T. ) ;
#4366=AXIS2_PLACEMENT_3D ( 'NONE', #18801, #3145, #11855 ) ;
#4368=AXIS2_PLACEMENT_3D ( 'NONE', #14298, #5824, #19562 ) ;
#4369=ORIENTED_EDGE ( 'NONE', *, *, #17605, .T. ) ;
#4370=CARTESIAN_POINT ( 'NONE',  ( 27.67540678000429111, -36.74634676501047181, 13.50000000000000000 ) ) ;
#4371=EDGE_LOOP ( 'NONE', ( #21084, #6360, #7295, #4438 ) ) ;
#4374=CYLINDRICAL_SURFACE ( 'NONE', #3449, 0.2999999999999999334 ) ;
#4375=DIRECTION ( 'NONE',  ( 0.000000000000000000, 0.000000000000000000, 1.000000000000000000 ) ) ;
#4377=ADVANCED_FACE ( 'NONE', ( #20159 ), #3036, .T. ) ;
#4378=CARTESIAN_POINT ( 'NONE',  ( -27.37540678000427974, -5.683640910026986681, 13.79999999999999893 ) ) ;
#4379=VECTOR ( 'NONE', #3643, 1000.000000000000000 ) ;
#4380=DIRECTION ( 'NONE',  ( -0.000000000000000000, 0.000000000000000000, 1.000000000000000000 ) ) ;
#4383=VERTEX_POINT ( 'NONE', #19720 ) ;
#4385=CARTESIAN_POINT ( 'NONE',  ( -23.32398829872514057, 7.118794219358020148E-15, 13.50000000000000000 ) ) ;
#4387=ORIENTED_EDGE ( 'NONE', *, *, #12213, .T. ) ;
#4388=CARTESIAN_POINT ( 'NONE',  ( 15.95292532278785913, 51.61873716947361856, 68.50000000000000000 ) ) ;
#4390=ORIENTED_EDGE ( 'NONE', *, *, #10868, .T. ) ;
#4391=ORIENTED_EDGE ( 'NONE', *, *, #12969, .T. ) ;
#4393=ADVANCED_FACE ( 'NONE', ( #9865 ), #10298, .T. ) ;
#4395=DIRECTION ( 'NONE',  ( -1.000000000000000000, 0.000000000000000000, 0.000000000000000000 ) ) ;
#4396=ORIENTED_EDGE ( 'NONE', *, *, #20754, .F. ) ;
#4399=PLANE ( 'NONE',  #11120 ) ;
#4402=DIRECTION ( 'NONE',  ( 1.000000000000000000, 0.000000000000000000, 0.000000000000000000 ) ) ;
#4403=ORIENTED_EDGE ( 'NONE', *, *, #20998, .T. ) ;
#4404=CARTESIAN_POINT ( 'NONE',  ( 15.21174975910705918, -41.81054587065082728, 13.79999999999999893 ) ) ;
#4409=CARTESIAN_POINT ( 'NONE',  ( 31.50000000000002132, -71.00000000000001421, 3.200000000000000178 ) ) ;
#4411=ORIENTED_EDGE ( 'NONE', *, *, #10122, .F. ) ;
#4412=CARTESIAN_POINT ( 'NONE',  ( 27.37540678000428684, -36.74634676501047181, 42.50000000000000000 ) ) ;
#4414=ORIENTED_EDGE ( 'NONE', *, *, #21321, .F. ) ;
#4416=CARTESIAN_POINT ( 'NONE',  ( -17.45292532278785913, -38.74634676501045760, 13.99999999999999822 ) ) ;
#4417=DIRECTION ( 'NONE',  ( 0.000000000000000000, 0.000000000000000000, 1.000000000000000000 ) ) ;
#4420=DIRECTION ( 'NONE',  ( 1.000000000000000000, 0.000000000000000000, 0.000000000000000000 ) ) ;
#4421=ORIENTED_EDGE ( 'NONE', *, *, #16881, .T. ) ;
#4423=CARTESIAN_POINT ( 'NONE',  ( -14.83748569039512155, 41.93480993936275070, 13.50000000000000000 ) ) ;
#4424=EDGE_CURVE ( 'NONE', #4126, #19345, #14201, .T. ) ;
#4426=CIRCLE ( 'NONE', #3713, 1.500000000000001332 ) ;
#4427=ADVANCED_FACE ( 'NONE', ( #16342 ), #2693, .T. ) ;
#4428=CARTESIAN_POINT ( 'NONE',  ( -27.67540678000427690, 10.94079601157914539, 13.50000000000000000 ) ) ;
#4429=CARTESIAN_POINT ( 'NONE',  ( 30.07540678000427548, 63.74634676501045050, 7.500000000000000000 ) ) ;
#4431=PRESENTATION_STYLE_ASSIGNMENT (( #14382 ) ) ;
#4432=DIRECTION ( 'NONE',  ( -0.000000000000000000, -0.000000000000000000, -1.000000000000000000 ) ) ;
#4434=CYLINDRICAL_SURFACE ( 'NONE', #13041, 0.5000000000000004441 ) ;
#4435=CIRCLE ( 'NONE', #9432, 0.5000000000000004441 ) ;
#4436=CARTESIAN_POINT ( 'NONE',  ( 29.13662752439705272, 4.700000000000000178, 3.799999999999999822 ) ) ;
#4437=ORIENTED_EDGE ( 'NONE', *, *, #3620, .T. ) ;
#4438=ORIENTED_EDGE ( 'NONE', *, *, #6555, .T. ) ;
#4439=DIRECTION ( 'NONE',  ( -0.9823853469773031755, -0.1868663427273193067, -0.000000000000000000 ) ) ;
#4440=CARTESIAN_POINT ( 'NONE',  ( 17.92752199202934094, -50.11873716947361856, 13.79999999999999893 ) ) ;
#4442=ORIENTED_EDGE ( 'NONE', *, *, #169, .F. ) ;
#4443=EDGE_CURVE ( 'NONE', #20393, #2605, #16218, .T. ) ;
#4444=ORIENTED_EDGE ( 'NONE', *, *, #7123, .T. ) ;
#4446=CARTESIAN_POINT ( 'NONE',  ( -14.96174975910705385, -41.81054587065082728, 13.62426406871192874 ) ) ;
#4447=CARTESIAN_POINT ( 'NONE',  ( -23.02398829872513986, -2.333317872336245102, 13.47139736055071602 ) ) ;
#4449=LINE ( 'NONE', #11263, #17491 ) ;
#4450=DIRECTION ( 'NONE',  ( 0.000000000000000000, 0.000000000000000000, 1.000000000000000000 ) ) ;
#4453=EDGE_CURVE ( 'NONE', #8198, #20854, #21368, .T. ) ;
#4454=CARTESIAN_POINT ( 'NONE',  ( -29.50000000000002132, -69.00000000000000000, 0.2999999999999947153 ) ) ;
#4462=ORIENTED_EDGE ( 'NONE', *, *, #15105, .F. ) ;
#4463=DIRECTION ( 'NONE',  ( -0.000000000000000000, -0.000000000000000000, -1.000000000000000000 ) ) ;
#4467=ORIENTED_EDGE ( 'NONE', *, *, #9413, .F. ) ;
#4469=ADVANCED_FACE ( 'NONE', ( #13092 ), #1230, .T. ) ;
#4471=EDGE_CURVE ( 'NONE', #21679, #6512, #3521, .T. ) ;
#4473=CYLINDRICAL_SURFACE ( 'NONE', #15251, 0.5000000000000004441 ) ;
#4474=ORIENTED_EDGE ( 'NONE', *, *, #7259, .F. ) ;
#4475=LINE ( 'NONE', #4267, #6669 ) ;
#4476=CARTESIAN_POINT ( 'NONE',  ( 29.50000000000002132, 0.000000000000000000, -150.0833101980363722 ) ) ;
#4477=DIRECTION ( 'NONE',  ( 1.000000000000000000, 0.000000000000000000, 0.000000000000000000 ) ) ;
#4478=DIRECTION ( 'NONE',  ( -0.000000000000000000, -0.000000000000000000, -1.000000000000000000 ) ) ;
#4480=VECTOR ( 'NONE', #2753, 1000.000000000000000 ) ;
#4481=LINE ( 'NONE', #21732, #3967 ) ;
#4488=DIRECTION ( 'NONE',  ( -0.000000000000000000, 0.000000000000000000, 1.000000000000000000 ) ) ;
#4492=CARTESIAN_POINT ( 'NONE',  ( 0.000000000000000000, -32.11873716947361856, 42.50000000000000711 ) ) ;
#4496=EDGE_CURVE ( 'NONE', #2381, #11265, #8403, .T. ) ;
#4500=CARTESIAN_POINT ( 'NONE',  ( 14.90249074828138198, -52.32070855728485981, 13.50000000000000000 ) ) ;
#4502=AXIS2_PLACEMENT_3D ( 'NONE', #303, #13836, #2096 ) ;
#4508=CARTESIAN_POINT ( 'NONE',  ( -15.95292532278785913, 50.11873716947361856, 13.99999999999999822 ) ) ;
#4509=CARTESIAN_POINT ( 'NONE',  ( -23.32398829872514057, 3.528912754968630328, 13.50000000000000000 ) ) ;
#4510=AXIS2_PLACEMENT_3D ( 'NONE', #9670, #13231, #14903 ) ;
#4511=ORIENTED_EDGE ( 'NONE', *, *, #13957, .F. ) ;
#4512=LINE ( 'NONE', #21875, #17221 ) ;
#4515=EDGE_CURVE ( 'NONE', #21509, #22135, #16000, .T. ) ;
#4517=ORIENTED_EDGE ( 'NONE', *, *, #5530, .F. ) ;
#4518=CARTESIAN_POINT ( 'NONE',  ( 0.000000000000000000, 4.700000000000000178, 3.500000000000000000 ) ) ;
#4522=TOROIDAL_SURFACE ( 'NONE', #15945, 1.500000000000000000, 0.5000000000000000000 ) ;
#4524=CIRCLE ( 'NONE', #7745, 0.3000000000000003775 ) ;
#4529=AXIS2_PLACEMENT_3D ( 'NONE', #14664, #894, #17911 ) ;
#4531=CARTESIAN_POINT ( 'NONE',  ( 23.02398829872514341, -3.262290859344324723, 13.80000000000000071 ) ) ;
#4532=CARTESIAN_POINT ( 'NONE',  ( 15.95292532278785913, -32.11873716947361856, 68.00000000000000000 ) ) ;
#4535=ORIENTED_EDGE ( 'NONE', *, *, #16088, .F. ) ;
#4536=FACE_OUTER_BOUND ( 'NONE', #18518, .T. ) ;
#4542=ORIENTED_EDGE ( 'NONE', *, *, #7809, .T. ) ;
#4545=SURFACE_SIDE_STYLE ('',( #7586 ) ) ;
#4546=CARTESIAN_POINT ( 'NONE',  ( 17.45292532278785913, -50.11873716947361856, 14.00000000000000000 ) ) ;
#4548=ORIENTED_EDGE ( 'NONE', *, *, #12903, .T. ) ;
#4550=CIRCLE ( 'NONE', #17048, 0.2999999999999999334 ) ;
#4551=CARTESIAN_POINT ( 'NONE',  ( -9.641460742840918030, 32.61873716947361856, 42.50000000000000711 ) ) ;
#4553=EDGE_LOOP ( 'NONE', ( #106, #5224, #17633, #17602 ) ) ;
#4556=DIRECTION ( 'NONE',  ( 1.000000000000000000, 0.000000000000000000, -0.000000000000000000 ) ) ;
#4559=ORIENTED_EDGE ( 'NONE', *, *, #6252, .F. ) ;
#4562=ORIENTED_EDGE ( 'NONE', *, *, #4196, .F. ) ;
#4565=CARTESIAN_POINT ( 'NONE',  ( 25.37540678000427263, -68.44634676501046044, 7.500000000000000000 ) ) ;
#4566=CARTESIAN_POINT ( 'NONE',  ( -23.07496371939382129, -2.433385307706763978, 13.33569868627438559 ) ) ;
#4569=CIRCLE ( 'NONE', #21738, 3.500000000000003109 ) ;
#4572=LINE ( 'NONE', #6048, #7760 ) ;
#4573=CARTESIAN_POINT ( 'NONE',  ( -30.37540678000427619, 0.000000000000000000, 7.200000000000000178 ) ) ;
#4580=VECTOR ( 'NONE', #16859, 1000.000000000000000 ) ;
#4581=ORIENTED_EDGE ( 'NONE', *, *, #11069, .F. ) ;
#4585=AXIS2_PLACEMENT_3D ( 'NONE', #21152, #5600, #10837 ) ;
#4587=CIRCLE ( 'NONE', #7455, 1.000000000000000888 ) ;
#4588=DIRECTION ( 'NONE',  ( 0.000000000000000000, 0.000000000000000000, -1.000000000000000000 ) ) ;
#4589=CIRCLE ( 'NONE', #19237, 6.499999999999999112 ) ;
#4591=EDGE_CURVE ( 'NONE', #10531, #12330, #3666, .T. ) ;
#4593=ORIENTED_EDGE ( 'NONE', *, *, #11664, .T. ) ;
#4594=EDGE_CURVE ( 'NONE', #8084, #11165, #17294, .T. ) ;
#4595=CYLINDRICAL_SURFACE ( 'NONE', #21173, 0.5000000000000004441 ) ;
#4604=CARTESIAN_POINT ( 'NONE',  ( 0.000000000000000000, -66.94634676501046044, 13.19999999999999929 ) ) ;
#4607=TOROIDAL_SURFACE ( 'NONE', #1028, 0.7000000000000000666, 0.2999999999999999889 ) ;
#4610=DIRECTION ( 'NONE',  ( -1.000000000000000000, 0.000000000000000000, 0.000000000000000000 ) ) ;
#4611=CYLINDRICAL_SURFACE ( 'NONE', #5551, 0.2999999999999999334 ) ;
#4612=ORIENTED_EDGE ( 'NONE', *, *, #11921, .T. ) ;
#4614=CARTESIAN_POINT ( 'NONE',  ( 15.95292532278785913, -52.11873716947361856, 68.00000000000000000 ) ) ;
#4615=CIRCLE ( 'NONE', #4965, 0.2999999999999999334 ) ;
#4616=LINE ( 'NONE', #14665, #9943 ) ;
#4618=CARTESIAN_POINT ( 'NONE',  ( 9.641460742840918030, -32.11873716947361856, 109.6002446535588319 ) ) ;
#4623=EDGE_LOOP ( 'NONE', ( #12492, #15536, #18232, #18909 ) ) ;
#4625=TOROIDAL_SURFACE ( 'NONE', #12821, 1.500000000000000000, 0.5000000000000000000 ) ;
#4626=ORIENTED_EDGE ( 'NONE', *, *, #19090, .F. ) ;
#4630=VERTEX_POINT ( 'NONE', #5357 ) ;
#4631=CYLINDRICAL_SURFACE ( 'NONE', #8608, 0.5000000000000004441 ) ;
#4633=AXIS2_PLACEMENT_3D ( 'NONE', #4812, #15437, #111 ) ;
#4635=CARTESIAN_POINT ( 'NONE',  ( -27.37540678000428684, -36.74634676501047181, 13.79999999999999893 ) ) ;
#4636=EDGE_CURVE ( 'NONE', #4677, #11393, #14942, .T. ) ;
#4637=ORIENTED_EDGE ( 'NONE', *, *, #15199, .F. ) ;
#4638=LINE ( 'NONE', #9555, #21870 ) ;
#4640=ORIENTED_EDGE ( 'NONE', *, *, #19813, .T. ) ;
#4645=ORIENTED_EDGE ( 'NONE', *, *, #15304, .F. ) ;
#4651=VERTEX_POINT ( 'NONE', #10270 ) ;
#4654=DIRECTION ( 'NONE',  ( 0.000000000000000000, 0.000000000000000000, -1.000000000000000000 ) ) ;
#4655=CYLINDRICAL_SURFACE ( 'NONE', #20583, 0.2999999999999999334 ) ;
#4657=DIRECTION ( 'NONE',  ( 0.000000000000000000, 0.000000000000000000, 1.000000000000000000 ) ) ;
#4658=DIRECTION ( 'NONE',  ( 0.000000000000000000, 0.000000000000000000, -1.000000000000000000 ) ) ;
#4659=B_SPLINE_CURVE_WITH_KNOTS ( 'NONE', 3,
 ( #6414, #2926, #11625, #9754, #13210, #16553 ),
 .UNSPECIFIED., .F., .F.,
 ( 4, 2, 4 ),
 ( 0.000000000000000000, 0.0002343433793794306779, 0.0004686867587588613559 ),
 .UNSPECIFIED. ) ;
#4662=EDGE_LOOP ( 'NONE', ( #16737, #21248, #2462, #1151 ) ) ;
#4664=CARTESIAN_POINT ( 'NONE',  ( -25.37540678000427263, -68.74634676501045760, 7.200000000000000178 ) ) ;
#4666=EDGE_CURVE ( 'NONE', #10568, #8021, #17091, .T. ) ;
#4668=CIRCLE ( 'NONE', #13230, 0.3000000000000016542 ) ;
#4669=CARTESIAN_POINT ( 'NONE',  ( -27.37540678000426908, 36.74634676501047181, 42.50000000000000000 ) ) ;
#4670=CARTESIAN_POINT ( 'NONE',  ( -14.96174975910705207, 51.86873716947361856, 68.00000000000000000 ) ) ;
#4671=EDGE_CURVE ( 'NONE', #16591, #4986, #5325, .T. ) ;
#4674=VERTEX_POINT ( 'NONE', #12034 ) ;
#4676=CARTESIAN_POINT ( 'NONE',  ( 26.37540678000427619, 10.94079601157914539, 42.50000000000000000 ) ) ;
#4677=VERTEX_POINT ( 'NONE', #8601 ) ;
#4678=VERTEX_POINT ( 'NONE', #22025 ) ;
#4681=LINE ( 'NONE', #1299, #11333 ) ;
#4682=CARTESIAN_POINT ( 'NONE',  ( -23.04884263981454140, -2.295195349811812946, 13.26498523032724997 ) ) ;
#4687=DIRECTION ( 'NONE',  ( 1.000000000000000000, 0.000000000000000000, 0.000000000000000000 ) ) ;
#4689=CARTESIAN_POINT ( 'NONE',  ( -29.50000000000002132, 0.000000000000000000, 0.2999999999999947153 ) ) ;
#4690=CARTESIAN_POINT ( 'NONE',  ( 9.641460742840918030, -32.61873716947361856, 68.00000000000000000 ) ) ;
#4694=EDGE_CURVE ( 'NONE', #22137, #4942, #17800, .T. ) ;
#4695=CARTESIAN_POINT ( 'NONE',  ( -24.43662752439705343, 0.000000000000000000, 3.500000000000000000 ) ) ;
#4701=CARTESIAN_POINT ( 'NONE',  ( -8.641460742840918030, -33.93424481021354921, 68.50000000000000000 ) ) ;
#4702=AXIS2_PLACEMENT_3D ( 'NONE', #14022, #4180, #13913 ) ;
#4703=EDGE_LOOP ( 'NONE', ( #19111, #18557, #15737, #10475 ) ) ;
#4704=VECTOR ( 'NONE', #18184, 1000.000000000000000 ) ;
#4705=EDGE_CURVE ( 'NONE', #17039, #11890, #4589, .T. ) ;
#4707=DIRECTION ( 'NONE',  ( 0.000000000000000000, 0.000000000000000000, 1.000000000000000000 ) ) ;
#4709=( BOUNDED_CURVE ( )  B_SPLINE_CURVE ( 3, ( #8149, #9477, #4784, #2892 ),
 .UNSPECIFIED., .F., .T. ) 
 B_SPLINE_CURVE_WITH_KNOTS ( ( 4, 4 ),
 ( 1.570796326794896558, 3.141592653589793116 ),
 .UNSPECIFIED. ) 
 CURVE ( )  GEOMETRIC_REPRESENTATION_ITEM ( )  RATIONAL_B_SPLINE_CURVE ( ( 1.000000000000000000, 0.8047378541243649375, 0.8047378541243649375, 1.000000000000000000 ) ) 
 REPRESENTATION_ITEM ( '' )  );
#4710=DIRECTION ( 'NONE',  ( 2.832483164223434527E-16, -1.000000000000000000, 0.000000000000000000 ) ) ;
#4712=CARTESIAN_POINT ( 'NONE',  ( 15.95292532278785913, -52.11873716947361856, 109.6002446535588319 ) ) ;
#4714=ADVANCED_FACE ( 'NONE', ( #14373 ), #22108, .T. ) ;
#4715=CARTESIAN_POINT ( 'NONE',  ( -17.45292532278785913, 34.11873716947361856, 68.00000000000000000 ) ) ;
#4716=EDGE_CURVE ( 'NONE', #13159, #2540, #13511, .T. ) ;
#4717=FACE_OUTER_BOUND ( 'NONE', #12537, .T. ) ;
#4720=ORIENTED_EDGE ( 'NONE', *, *, #21987, .F. ) ;
#4723=EDGE_LOOP ( 'NONE', ( #16532, #9709, #19344, #10484 ) ) ;
#4724=DIRECTION ( 'NONE',  ( -0.000000000000000000, 0.000000000000000000, 1.000000000000000000 ) ) ;
#4727=DIRECTION ( 'NONE',  ( 1.000000000000000000, 0.000000000000000000, 0.000000000000000000 ) ) ;
#4728=VERTEX_POINT ( 'NONE', #14150 ) ;
#4730=CARTESIAN_POINT ( 'NONE',  ( 8.641460742840918030, 33.43424481021354921, 68.00000000000000000 ) ) ;
#4733=EDGE_LOOP ( 'NONE', ( #16963, #8147, #1884, #6727 ) ) ;
#4734=EDGE_CURVE ( 'NONE', #17367, #14785, #15638, .T. ) ;
#4740=DIRECTION ( 'NONE',  ( 0.000000000000000000, -0.000000000000000000, 1.000000000000000000 ) ) ;
#4742=CARTESIAN_POINT ( 'NONE',  ( -23.32398829872514057, 3.528912754968630328, 13.50000000000000000 ) ) ;
#4744=CARTESIAN_POINT ( 'NONE',  ( -15.95292532278785913, -50.11873716947361856, 13.50000000000000000 ) ) ;
#4746=CARTESIAN_POINT ( 'NONE',  ( 28.57540678000427548, -6.494748934539263274, 13.50000000000000000 ) ) ;
#4747=FACE_OUTER_BOUND ( 'NONE', #21178, .T. ) ;
#4748=CIRCLE ( 'NONE', #6553, 0.5000000000000004441 ) ;
#4751=ORIENTED_EDGE ( 'NONE', *, *, #18376, .F. ) ;
#4753=ORIENTED_EDGE ( 'NONE', *, *, #9935, .F. ) ;
#4754=CARTESIAN_POINT ( 'NONE',  ( 17.95292532278785913, 50.11873716947361856, 109.6002446535588319 ) ) ;
#4756=EDGE_LOOP ( 'NONE', ( #7377, #21979, #9379, #3777, #5288, #14281 ) ) ;
#4757=DIRECTION ( 'NONE',  ( 0.000000000000000000, 0.000000000000000000, 1.000000000000000000 ) ) ;
#4758=EDGE_CURVE ( 'NONE', #20751, #2319, #2799, .T. ) ;
#4759=ORIENTED_EDGE ( 'NONE', *, *, #12873, .T. ) ;
#4762=EDGE_CURVE ( 'NONE', #15775, #21768, #10911, .T. ) ;
#4763=CARTESIAN_POINT ( 'NONE',  ( 0.000000000000000000, -71.70000000000001705, 1.500000000000000000 ) ) ;
#4765=EDGE_LOOP ( 'NONE', ( #16034, #11762, #18041 ) ) ;
#4766=CARTESIAN_POINT ( 'NONE',  ( -8.641460742840918030, 32.93424481021354921, 7.321391277662001151 ) ) ;
#4767=CARTESIAN_POINT ( 'NONE',  ( -24.13662752439704917, 0.000000000000000000, 7.500000000000000000 ) ) ;
#4770=ORIENTED_EDGE ( 'NONE', *, *, #21113, .F. ) ;
#4773=VERTEX_POINT ( 'NONE', #12675 ) ;
#4775=CARTESIAN_POINT ( 'NONE',  ( -26.33662752439704846, 0.000000000000000000, 0.3000000000000016542 ) ) ;
#4776=EDGE_LOOP ( 'NONE', ( #15723, #20634, #16976, #536 ) ) ;
#4777=ORIENTED_EDGE ( 'NONE', *, *, #17161, .T. ) ;
#4778=ORIENTED_EDGE ( 'NONE', *, *, #2699, .F. ) ;
#4780=CARTESIAN_POINT ( 'NONE',  ( 17.95292532278785913, -38.74634676501045760, 14.00000000000000000 ) ) ;
#4784=CARTESIAN_POINT ( 'NONE',  ( 29.50000000000001421, 69.00000000000000000, 0.1242640687119232062 ) ) ;
#4786=CARTESIAN_POINT ( 'NONE',  ( -29.13662752439705272, 0.000000000000000000, 0.000000000000000000 ) ) ;
#4787=CARTESIAN_POINT ( 'NONE',  ( -23.18291235612340273, -2.947575143997166247, 13.45754841673216085 ) ) ;
#4792=EDGE_LOOP ( 'NONE', ( #12574, #17888, #8310, #13332 ) ) ;
#4795=DIRECTION ( 'NONE',  ( 1.000000000000000000, 0.000000000000000000, 0.000000000000000000 ) ) ;
#4796=FACE_OUTER_BOUND ( 'NONE', #9758, .T. ) ;
#4797=ORIENTED_EDGE ( 'NONE', *, *, #21691, .T. ) ;
#4801=ORIENTED_EDGE ( 'NONE', *, *, #13708, .F. ) ;
#4803=ADVANCED_FACE ( 'NONE', ( #14045 ), #16047, .F. ) ;
#4804=EDGE_LOOP ( 'NONE', ( #5009, #1772, #2418, #17777 ) ) ;
#4805=CYLINDRICAL_SURFACE ( 'NONE', #20985, 0.5000000000000004441 ) ;
#4807=EDGE_CURVE ( 'NONE', #8747, #19185, #4204, .T. ) ;
#4809=CARTESIAN_POINT ( 'NONE',  ( 3.627054932750481964, -32.93424481021354921, 68.50000000000000000 ) ) ;
#4811=DIRECTION ( 'NONE',  ( 0.000000000000000000, -1.000000000000000000, 0.000000000000000000 ) ) ;
#4812=CARTESIAN_POINT ( 'NONE',  ( -32.20000000000001705, 71.00000000000001421, 1.800000000000000044 ) ) ;
#4813=CARTESIAN_POINT ( 'NONE',  ( -29.13662752439705272, 0.000000000000000000, 13.19999999999999929 ) ) ;
#4815=DIRECTION ( 'NONE',  ( 2.388292521039847891E-16, -0.000000000000000000, 1.000000000000000000 ) ) ;
#4816=FACE_OUTER_BOUND ( 'NONE', #10267, .T. ) ;
#4817=AXIS2_PLACEMENT_3D ( 'NONE', #17420, #2313, #631 ) ;
#4820=VERTEX_POINT ( 'NONE', #11130 ) ;
#4821=DIRECTION ( 'NONE',  ( 1.000000000000000000, 0.000000000000000000, 0.000000000000000000 ) ) ;
#4822=EDGE_LOOP ( 'NONE', ( #6918, #1515, #7430, #16958 ) ) ;
#4823=CARTESIAN_POINT ( 'NONE',  ( -27.67540678000426979, 36.74634676501047181, 13.50000000000000000 ) ) ;
#4825=ORIENTED_EDGE ( 'NONE', *, *, #16153, .T. ) ;
#4827=DIRECTION ( 'NONE',  ( 0.000000000000000000, 0.000000000000000000, 1.000000000000000000 ) ) ;
#4829=ORIENTED_EDGE ( 'NONE', *, *, #7348, .F. ) ;
#4830=LINE ( 'NONE', #16567, #3213 ) ;
#4831=ORIENTED_EDGE ( 'NONE', *, *, #10604, .T. ) ;
#4833=ORIENTED_EDGE ( 'NONE', *, *, #14040, .F. ) ;
#4834=EDGE_CURVE ( 'NONE', #19467, #9554, #7381, .T. ) ;
#4840=ORIENTED_EDGE ( 'NONE', *, *, #19475, .T. ) ;
#4842=CARTESIAN_POINT ( 'NONE',  ( -23.02398829872514341, 2.928406208502772667, 13.54172988673450639 ) ) ;
#4843=PLANE ( 'NONE',  #74 ) ;
#4844=FACE_OUTER_BOUND ( 'NONE', #523, .T. ) ;
#4846=EDGE_CURVE ( 'NONE', #961, #1826, #7793, .T. ) ;
#4847=DIRECTION ( 'NONE',  ( 0.000000000000000000, -0.000000000000000000, -1.000000000000000000 ) ) ;
#4848=ORIENTED_EDGE ( 'NONE', *, *, #5728, .F. ) ;
#4849=TOROIDAL_SURFACE ( 'NONE', #7732, 0.2500000000000000000, 0.2500000000000000000 ) ;
#4850=ORIENTED_EDGE ( 'NONE', *, *, #3471, .F. ) ;
#4851=CIRCLE ( 'NONE', #19489, 4.051418481279135619 ) ;
#4856=VERTEX_POINT ( 'NONE', #7907 ) ;
#4859=ADVANCED_FACE ( 'NONE', ( #12912 ), #18434, .F. ) ;
#4860=VERTEX_POINT ( 'NONE', #11979 ) ;
#4865=DIRECTION ( 'NONE',  ( 1.000000000000000000, -0.000000000000000000, -0.000000000000000000 ) ) ;
#4868=VECTOR ( 'NONE', #17578, 1000.000000000000000 ) ;
#4869=CARTESIAN_POINT ( 'NONE',  ( -31.50000000000002132, 71.70000000000001705, 3.200000000000000178 ) ) ;
#4870=VECTOR ( 'NONE', #17054, 1000.000000000000000 ) ;
#4874=LINE ( 'NONE', #20865, #4349 ) ;
#4881=DIRECTION ( 'NONE',  ( 0.000000000000000000, 0.000000000000000000, -1.000000000000000000 ) ) ;
#4883=ORIENTED_EDGE ( 'NONE', *, *, #19816, .F. ) ;
#4887=DIRECTION ( 'NONE',  ( 1.000000000000000000, 0.000000000000000000, 0.000000000000000000 ) ) ;
#4893=VERTEX_POINT ( 'NONE', #4957 ) ;
#4894=CARTESIAN_POINT ( 'NONE',  ( 29.37540678000427619, -4.700000000000000178, 3.500000000000000000 ) ) ;
#4895=EDGE_CURVE ( 'NONE', #14054, #10473, #6642, .T. ) ;
#4896=DIRECTION ( 'NONE',  ( 0.000000000000000000, 0.000000000000000000, 1.000000000000000000 ) ) ;
#4897=CARTESIAN_POINT ( 'NONE',  ( -23.02398829872490538, -3.297879325580993726, 13.54382403646240007 ) ) ;
#4899=CIRCLE ( 'NONE', #8830, 0.5000000000000004441 ) ;
#4902=DIRECTION ( 'NONE',  ( 0.000000000000000000, 0.000000000000000000, 1.000000000000000000 ) ) ;
#4904=FACE_OUTER_BOUND ( 'NONE', #3219, .T. ) ;
#4906=CARTESIAN_POINT ( 'NONE',  ( 0.000000000000000000, -5.000000000000000000, 7.200000000000000178 ) ) ;
#4908=ORIENTED_EDGE ( 'NONE', *, *, #20453, .F. ) ;
#4911=LINE ( 'NONE', #8274, #7380 ) ;
#4912=VERTEX_POINT ( 'NONE', #3168 ) ;
#4913=ADVANCED_FACE ( 'NONE', ( #8542 ), #9574, .T. ) ;
#4914=DIRECTION ( 'NONE',  ( -0.000000000000000000, -0.000000000000000000, -1.000000000000000000 ) ) ;
#4918=AXIS2_PLACEMENT_3D ( 'NONE', #7028, #1866, #8475 ) ;
#4921=AXIS2_PLACEMENT_3D ( 'NONE', #1953, #8798, #14039 ) ;
#4924=DIRECTION ( 'NONE',  ( 0.000000000000000000, 0.000000000000000000, -1.000000000000000000 ) ) ;
#4925=EDGE_LOOP ( 'NONE', ( #5572, #519, #20457, #2439 ) ) ;
#4926=B_SPLINE_CURVE_WITH_KNOTS ( 'NONE', 3,
 ( #8728, #8508, #8387, #22053, #11845, #13734, #3689, #15526 ),
 .UNSPECIFIED., .F., .F.,
 ( 4, 2, 2, 4 ),
 ( -3.464559252384133923E-06, 0.0002895415592466213275, 0.0004360446184961240686, 0.0005825476777456268639 ),
 .UNSPECIFIED. ) ;
#4927=CARTESIAN_POINT ( 'NONE',  ( -8.641460742840918030, -32.93424481021354921, 42.50000000000000000 ) ) ;
#4929=VECTOR ( 'NONE', #9846, 1000.000000000000000 ) ;
#4930=CIRCLE ( 'NONE', #4918, 0.5000000000000004441 ) ;
#4932=FACE_OUTER_BOUND ( 'NONE', #4081, .T. ) ;
#4933=CARTESIAN_POINT ( 'NONE',  ( -9.141460742840918030, -32.61873716947361856, 68.50000000000000000 ) ) ;
#4935=VECTOR ( 'NONE', #2222, 1000.000000000000000 ) ;
#4936=CARTESIAN_POINT ( 'NONE',  ( -15.13992500838820909, -52.10286008548567338, 13.87499999123205363 ) ) ;
#4938=TOROIDAL_SURFACE ( 'NONE', #2442, 2.299999999999993161, 0.2999999999999999889 ) ;
#4939=VECTOR ( 'NONE', #9349, 1000.000000000000000 ) ;
#4941=DIRECTION ( 'NONE',  ( 0.000000000000000000, 0.000000000000000000, 1.000000000000000000 ) ) ;
#4942=VERTEX_POINT ( 'NONE', #20509 ) ;
#4945=DIRECTION ( 'NONE',  ( -1.000000000000000000, 0.000000000000000000, 0.000000000000000000 ) ) ;
#4946=ORIENTED_EDGE ( 'NONE', *, *, #20132, .F. ) ;
#4947=VERTEX_POINT ( 'NONE', #4532 ) ;
#4949=ORIENTED_EDGE ( 'NONE', *, *, #1405, .T. ) ;
#4951=AXIS2_PLACEMENT_3D ( 'NONE', #17142, #3499, #20511 ) ;
#4953=VECTOR ( 'NONE', #13286, 1000.000000000000000 ) ;
#4954=AXIS2_PLACEMENT_3D ( 'NONE', #5939, #9630, #4364 ) ;
#4955=ORIENTED_EDGE ( 'NONE', *, *, #3300, .F. ) ;
#4956=TOROIDAL_SURFACE ( 'NONE', #7477, 2.274596669241483848, 0.2999999999999999889 ) ;
#4957=CARTESIAN_POINT ( 'NONE',  ( 30.37540678000427619, -63.74634676501045050, 3.799999999999999822 ) ) ;
#4960=FACE_OUTER_BOUND ( 'NONE', #13007, .T. ) ;
#4965=AXIS2_PLACEMENT_3D ( 'NONE', #12253, #17301, #10396 ) ;
#4966=CYLINDRICAL_SURFACE ( 'NONE', #3383, 0.2500000000000002220 ) ;
#4967=EDGE_CURVE ( 'NONE', #8633, #5089, #942, .T. ) ;
#4968=EDGE_CURVE ( 'NONE', #14892, #6732, #13429, .T. ) ;
#4970=VECTOR ( 'NONE', #17960, 1000.000000000000000 ) ;
#4974=DIRECTION ( 'NONE',  ( -1.000000000000000000, 0.000000000000000000, 0.000000000000000000 ) ) ;
#4975=VECTOR ( 'NONE', #14617, 1000.000000000000000 ) ;
#4977=DIRECTION ( 'NONE',  ( 0.000000000000000000, -0.000000000000000000, -1.000000000000000000 ) ) ;
#4978=ORIENTED_EDGE ( 'NONE', *, *, #20925, .F. ) ;
#4981=DIRECTION ( 'NONE',  ( 0.000000000000000000, -0.000000000000000000, -1.000000000000000000 ) ) ;
#4983=LINE ( 'NONE', #18966, #2392 ) ;
#4984=AXIS2_PLACEMENT_3D ( 'NONE', #4604, #11522, #21619 ) ;
#4985=CYLINDRICAL_SURFACE ( 'NONE', #9166, 0.2999999999999999334 ) ;
#4986=VERTEX_POINT ( 'NONE', #10210 ) ;
#4990=FACE_OUTER_BOUND ( 'NONE', #1622, .T. ) ;
#4991=ORIENTED_EDGE ( 'NONE', *, *, #1456, .T. ) ;
#4992=DIRECTION ( 'NONE',  ( -0.000000000000000000, -0.000000000000000000, -1.000000000000000000 ) ) ;
#4994=ORIENTED_EDGE ( 'NONE', *, *, #11958, .T. ) ;
#4997=FACE_OUTER_BOUND ( 'NONE', #9071, .T. ) ;
#5000=ORIENTED_EDGE ( 'NONE', *, *, #3922, .F. ) ;
#5001=VERTEX_POINT ( 'NONE', #9077 ) ;
#5002=FACE_OUTER_BOUND ( 'NONE', #2950, .T. ) ;
#5004=DIRECTION ( 'NONE',  ( 1.000000000000000000, 0.000000000000000000, 0.000000000000000000 ) ) ;
#5006=CIRCLE ( 'NONE', #21445, 2.500000000000002220 ) ;
#5007=ORIENTED_EDGE ( 'NONE', *, *, #18572, .T. ) ;
#5009=ORIENTED_EDGE ( 'NONE', *, *, #1204, .T. ) ;
#5011=CARTESIAN_POINT ( 'NONE',  ( 29.13662752439705272, 0.000000000000000000, 1.500000000000001332 ) ) ;
#5013=EDGE_CURVE ( 'NONE', #14923, #4893, #5407, .T. ) ;
#5014=ORIENTED_EDGE ( 'NONE', *, *, #13731, .T. ) ;
#5019=EDGE_LOOP ( 'NONE', ( #19442, #2889, #3686, #14614 ) ) ;
#5020=FACE_OUTER_BOUND ( 'NONE', #17538, .T. ) ;
#5024=CIRCLE ( 'NONE', #4289, 0.5000000000000004441 ) ;
#5025=DIRECTION ( 'NONE',  ( 1.000000000000000000, 0.000000000000000000, 0.000000000000000000 ) ) ;
#5026=DIRECTION ( 'NONE',  ( 0.000000000000000000, 0.000000000000000000, 1.000000000000000000 ) ) ;
#5028=DIRECTION ( 'NONE',  ( 1.000000000000000000, 0.000000000000000000, 0.000000000000000000 ) ) ;
#5031=ORIENTED_EDGE ( 'NONE', *, *, #5763, .T. ) ;
#5032=LINE ( 'NONE', #15424, #5339 ) ;
#5036=ORIENTED_EDGE ( 'NONE', *, *, #7809, .F. ) ;
#5037=FACE_OUTER_BOUND ( 'NONE', #20521, .T. ) ;
#5038=AXIS2_PLACEMENT_3D ( 'NONE', #3955, #12749, #19277 ) ;
#5041=CARTESIAN_POINT ( 'NONE',  ( 0.000000000000000000, 52.11873716947361856, 68.00000000000000000 ) ) ;
#5042=ORIENTED_EDGE ( 'NONE', *, *, #9557, .T. ) ;
#5043=FACE_OUTER_BOUND ( 'NONE', #21166, .T. ) ;
#5045=DIRECTION ( 'NONE',  ( -1.000000000000000000, -0.000000000000000000, -0.000000000000000000 ) ) ;
#5046=ADVANCED_FACE ( 'NONE', ( #127 ), #449, .F. ) ;
#5048=CARTESIAN_POINT ( 'NONE',  ( 14.96174975910707161, -51.61873716947361856, 68.25000000000000000 ) ) ;
#5049=DIRECTION ( 'NONE',  ( -1.000000000000000000, 0.000000000000000000, 0.000000000000000000 ) ) ;
#5050=CIRCLE ( 'NONE', #1831, 4.700000000000002842 ) ;
#5051=DIRECTION ( 'NONE',  ( 0.000000000000000000, 0.000000000000000000, 1.000000000000000000 ) ) ;
#5053=DIRECTION ( 'NONE',  ( -1.000000000000000000, 0.000000000000000000, 0.000000000000000000 ) ) ;
#5054=ADVANCED_FACE ( 'NONE', ( #12195 ), #3611, .F. ) ;
#5055=CARTESIAN_POINT ( 'NONE',  ( -3.627054932750481964, -32.61873716947361856, 7.321391277662001151 ) ) ;
#5065=ORIENTED_EDGE ( 'NONE', *, *, #973, .F. ) ;
#5070=VECTOR ( 'NONE', #4294, 1000.000000000000000 ) ;
#5071=ADVANCED_FACE ( 'NONE', ( #20943 ), #20841, .T. ) ;
#5072=CARTESIAN_POINT ( 'NONE',  ( 9.141460742840918030, 33.43424481021354921, 7.321391277662001151 ) ) ;
#5073=ORIENTED_EDGE ( 'NONE', *, *, #6329, .T. ) ;
#5075=FACE_OUTER_BOUND ( 'NONE', #20446, .T. ) ;
#5079=CARTESIAN_POINT ( 'NONE',  ( -29.13662752439705272, -4.700000000000000178, 3.799999999999999822 ) ) ;
#5080=CARTESIAN_POINT ( 'NONE',  ( 17.95292532278785913, 38.74634676501045760, 13.99999999999999822 ) ) ;
#5082=ORIENTED_EDGE ( 'NONE', *, *, #62, .F. ) ;
#5084=CARTESIAN_POINT ( 'NONE',  ( -30.07540678000427548, 63.74634676501045050, 7.200000000000000178 ) ) ;
#5087=ADVANCED_FACE ( 'NONE', ( #8752 ), #5598, .T. ) ;
#5088=CARTESIAN_POINT ( 'NONE',  ( -4.127054932750482408, -32.93424481021354921, 68.00000000000000000 ) ) ;
#5089=VERTEX_POINT ( 'NONE', #17347 ) ;
#5090=TOROIDAL_SURFACE ( 'NONE', #20466, 6.800000000000001599, 0.2999999999999999889 ) ;
#5091=CIRCLE ( 'NONE', #11514, 0.2500000000000002220 ) ;
#5092=ORIENTED_EDGE ( 'NONE', *, *, #16104, .F. ) ;
#5093=CARTESIAN_POINT ( 'NONE',  ( -15.95292532278785913, 52.39333383871510108, 13.79999999999999893 ) ) ;
#5094=ADVANCED_FACE ( 'NONE', ( #7086 ), #13883, .T. ) ;
#5096=CARTESIAN_POINT ( 'NONE',  ( -29.37540678000427619, -5.000000000000000000, 7.200000000000000178 ) ) ;
#5097=ORIENTED_EDGE ( 'NONE', *, *, #4666, .F. ) ;
#5102=DIRECTION ( 'NONE',  ( 0.000000000000000000, -0.000000000000000000, -1.000000000000000000 ) ) ;
#5103=ORIENTED_EDGE ( 'NONE', *, *, #10202, .F. ) ;
#5106=AXIS2_PLACEMENT_3D ( 'NONE', #767, #9624, #13058 ) ;
#5108=DIRECTION ( 'NONE',  ( -1.000000000000000000, 0.000000000000000000, 0.000000000000000000 ) ) ;
#5109=DIRECTION ( 'NONE',  ( 0.000000000000000000, 0.000000000000000000, 1.000000000000000000 ) ) ;
#5111=DIRECTION ( 'NONE',  ( 0.000000000000000000, 0.000000000000000000, 1.000000000000000000 ) ) ;
#5112=ORIENTED_EDGE ( 'NONE', *, *, #406, .T. ) ;
#5114=ORIENTED_EDGE ( 'NONE', *, *, #11639, .F. ) ;
#5117=EDGE_CURVE ( 'NONE', #1711, #9267, #20730, .T. ) ;
#5118=CARTESIAN_POINT ( 'NONE',  ( 3.127054932750481964, -32.61873716947361856, 42.50000000000000711 ) ) ;
#5119=ORIENTED_EDGE ( 'NONE', *, *, #7063, .F. ) ;
#5120=CARTESIAN_POINT ( 'NONE',  ( 17.95292532278785913, 0.000000000000000000, 109.6002446535588319 ) ) ;
#5121=ORIENTED_EDGE ( 'NONE', *, *, #20385, .F. ) ;
#5126=PLANE ( 'NONE',  #13857 ) ;
#5127=ADVANCED_FACE ( 'NONE', ( #15878 ), #556, .F. ) ;
#5131=CARTESIAN_POINT ( 'NONE',  ( 23.02398829872514341, 2.211005166399008459, 13.20000000000005791 ) ) ;
#5132=CARTESIAN_POINT ( 'NONE',  ( -3.127054932750481964, 32.11873716947361856, 68.00000000000000000 ) ) ;
#5133=FACE_OUTER_BOUND ( 'NONE', #3595, .T. ) ;
#5137=LINE ( 'NONE', #6499, #1647 ) ;
#5138=ORIENTED_EDGE ( 'NONE', *, *, #4116, .T. ) ;
#5142=ORIENTED_EDGE ( 'NONE', *, *, #16497, .F. ) ;
#5144=EDGE_LOOP ( 'NONE', ( #7513, #7102, #17750, #4759 ) ) ;
#5145=EDGE_CURVE ( 'NONE', #9228, #444, #14653, .T. ) ;
#5146=DIRECTION ( 'NONE',  ( 0.000000000000000000, 1.000000000000000000, 0.000000000000000000 ) ) ;
#5147=EDGE_LOOP ( 'NONE', ( #15006, #14341, #2121, #20232 ) ) ;
#5149=ADVANCED_FACE ( 'NONE', ( #4150 ), #4374, .T. ) ;
#5152=DIRECTION ( 'NONE',  ( 0.000000000000000000, 0.000000000000000000, 1.000000000000000000 ) ) ;
#5154=DIRECTION ( 'NONE',  ( 1.000000000000000000, 0.000000000000000000, 0.000000000000000000 ) ) ;
#5157=CARTESIAN_POINT ( 'NONE',  ( -27.37540678000427974, -5.683640910026986681, 13.50000000000000000 ) ) ;
#5162=EDGE_CURVE ( 'NONE', #17318, #5997, #7858, .T. ) ;
#5163=CARTESIAN_POINT ( 'NONE',  ( 0.000000000000000000, -52.39333383871510108, 13.79999999999999893 ) ) ;
#5164=LINE ( 'NONE', #17006, #8823 ) ;
#5166=ORIENTED_EDGE ( 'NONE', *, *, #15789, .F. ) ;
#5167=AXIS2_PLACEMENT_3D ( 'NONE', #8130, #11571, #13257 ) ;
#5171=EDGE_CURVE ( 'NONE', #808, #11153, #10971, .T. ) ;
#5172=ORIENTED_EDGE ( 'NONE', *, *, #20907, .F. ) ;
#5173=PRESENTATION_STYLE_ASSIGNMENT (( #1468 ) ) ;
#5175=ORIENTED_EDGE ( 'NONE', *, *, #6398, .F. ) ;
#5176=EDGE_LOOP ( 'NONE', ( #13608, #22158, #18759, #19831, #12843, #6196 ) ) ;
#5178=DIRECTION ( 'NONE',  ( 0.000000000000000000, 0.000000000000000000, -1.000000000000000000 ) ) ;
#5181=AXIS2_PLACEMENT_3D ( 'NONE', #18714, #18375, #8219 ) ;
#5184=CYLINDRICAL_SURFACE ( 'NONE', #2557, 0.2999999999999999334 ) ;
#5186=CARTESIAN_POINT ( 'NONE',  ( -17.45292532278785913, -50.11873716947361856, 68.00000000000000000 ) ) ;
#5187=CARTESIAN_POINT ( 'NONE',  ( 25.37540678000427263, 66.94634676501046044, 13.50000000000000000 ) ) ;
#5189=ORIENTED_EDGE ( 'NONE', *, *, #4018, .T. ) ;
#5190=CARTESIAN_POINT ( 'NONE',  ( 25.37540678000427263, 63.74634676501045050, 7.500000000000000000 ) ) ;
#5192=DIRECTION ( 'NONE',  ( 0.000000000000000000, 0.000000000000000000, 1.000000000000000000 ) ) ;
#5193=ADVANCED_FACE ( 'NONE', ( #6182 ), #17371, .T. ) ;
#5194=ORIENTED_EDGE ( 'NONE', *, *, #6674, .T. ) ;
#5196=ADVANCED_FACE ( 'NONE', ( #12965 ), #9517, .F. ) ;
#5198=CARTESIAN_POINT ( 'NONE',  ( 17.95292532278785913, 0.000000000000000000, 68.00000000000000000 ) ) ;
#5199=AXIS2_PLACEMENT_3D ( 'NONE', #12047, #17102, #5028 ) ;
#5200=DIRECTION ( 'NONE',  ( -1.000000000000000000, 0.000000000000000000, 0.000000000000000000 ) ) ;
#5201=CARTESIAN_POINT ( 'NONE',  ( -23.02398829872513986, -2.157133568460768647, 42.50000000000000000 ) ) ;
#5202=DIRECTION ( 'NONE',  ( 0.000000000000000000, 0.000000000000000000, 1.000000000000000000 ) ) ;
#5203=DIRECTION ( 'NONE',  ( 1.000000000000000000, 0.000000000000000000, -0.000000000000000000 ) ) ;
#5206=DIRECTION ( 'NONE',  ( 1.000000000000000000, 0.000000000000000000, 0.000000000000000000 ) ) ;
#5207=CYLINDRICAL_SURFACE ( 'NONE', #7134, 0.2500000000000002220 ) ;
#5208=FACE_OUTER_BOUND ( 'NONE', #14813, .T. ) ;
#5213=CARTESIAN_POINT ( 'NONE',  ( 0.000000000000000000, 52.10286008774954780, 13.87500000000000000 ) ) ;
#5216=VECTOR ( 'NONE', #590, 1000.000000000000000 ) ;
#5217=CIRCLE ( 'NONE', #7009, 0.3000000000000016542 ) ;
#5218=EDGE_LOOP ( 'NONE', ( #13090, #4517, #4096, #16617 ) ) ;
#5219=LINE ( 'NONE', #12231, #17897 ) ;
#5220=CARTESIAN_POINT ( 'NONE',  ( 0.000000000000000000, 0.000000000000000000, 68.50000000000000000 ) ) ;
#5221=CARTESIAN_POINT ( 'NONE',  ( 0.000000000000000000, 5.000000000000000000, 7.500000000000000000 ) ) ;
#5223=VERTEX_POINT ( 'NONE', #17900 ) ;
#5224=ORIENTED_EDGE ( 'NONE', *, *, #20474, .T. ) ;
#5225=FACE_OUTER_BOUND ( 'NONE', #21938, .T. ) ;
#5226=DIRECTION ( 'NONE',  ( -0.000000000000000000, -0.000000000000000000, -1.000000000000000000 ) ) ;
#5227=EDGE_CURVE ( 'NONE', #22131, #21935, #18123, .T. ) ;
#5228=DIRECTION ( 'NONE',  ( 0.000000000000000000, 0.000000000000000000, 1.000000000000000000 ) ) ;
#5229=ADVANCED_FACE ( 'NONE', ( #16446 ), #10860, .F. ) ;
#5230=DIRECTION ( 'NONE',  ( 1.000000000000000000, 0.000000000000000000, 0.000000000000000000 ) ) ;
#5232=ORIENTED_EDGE ( 'NONE', *, *, #2585, .T. ) ;
#5233=DIRECTION ( 'NONE',  ( -0.000000000000000000, -0.000000000000000000, -1.000000000000000000 ) ) ;
#5235=AXIS2_PLACEMENT_3D ( 'NONE', #9887, #19971, #10216 ) ;
#5237=EDGE_LOOP ( 'NONE', ( #881, #7667, #12836, #3365 ) ) ;
#5238=CARTESIAN_POINT ( 'NONE',  ( -23.02398829872536368, -3.053353875533148187, 13.54966661417588547 ) ) ;
#5241=CARTESIAN_POINT ( 'NONE',  ( -23.32398829872514057, -3.528912754968629439, 13.50000000000000000 ) ) ;
#5242=ORIENTED_EDGE ( 'NONE', *, *, #18803, .T. ) ;
#5243=CARTESIAN_POINT ( 'NONE',  ( 23.02398829872513986, 3.005406968599039441, 13.74590378743891250 ) ) ;
#5245=CARTESIAN_POINT ( 'NONE',  ( -31.50000000000002132, 71.00000000000001421, 3.500000000000000000 ) ) ;
#5248=ADVANCED_FACE ( 'NONE', ( #678 ), #4160, .F. ) ;
#5249=CIRCLE ( 'NONE', #8096, 5.000000000000004441 ) ;
#5251=DIRECTION ( 'NONE',  ( 1.000000000000000000, 0.000000000000000000, 0.000000000000000000 ) ) ;
#5255=AXIS2_PLACEMENT_3D ( 'NONE', #21286, #18137, #9651 ) ;
#5256=EDGE_CURVE ( 'NONE', #10046, #17759, #19470, .T. ) ;
#5260=ORIENTED_EDGE ( 'NONE', *, *, #15194, .T. ) ;
#5261=CIRCLE ( 'NONE', #14877, 2.000000000000001776 ) ;
#5262=AXIS2_PLACEMENT_3D ( 'NONE', #9353, #16159, #7678 ) ;
#5265=EDGE_LOOP ( 'NONE', ( #6307, #1889, #4106, #10509, #20237, #10454, #22118, #9174, #7779, #8884, #6322, #839, #17236, #8913, #7324, #12786, #13406, #19497, #6204, #3037, #7290, #21475, #1825, #13191, #10207, #15791, #4612, #17460, #20773, #13807 ) ) ;
#5266=CARTESIAN_POINT ( 'NONE',  ( -29.13662752439705272, 0.000000000000000000, 7.500000000000000000 ) ) ;
#5268=DIRECTION ( 'NONE',  ( 0.000000000000000000, 1.000000000000000000, -0.000000000000000000 ) ) ;
#5269=DIRECTION ( 'NONE',  ( 1.000000000000000000, 0.000000000000000000, 0.000000000000000000 ) ) ;
#5271=CARTESIAN_POINT ( 'NONE',  ( 27.37540678000427974, -10.94079601157914716, 13.79999999999999893 ) ) ;
#5273=AXIS2_PLACEMENT_3D ( 'NONE', #7217, #15800, #256 ) ;
#5274=LINE ( 'NONE', #20921, #2590 ) ;
#5275=VECTOR ( 'NONE', #16199, 1000.000000000000000 ) ;
#5276=CIRCLE ( 'NONE', #12724, 1.000000000000000000 ) ;
#5278=ORIENTED_EDGE ( 'NONE', *, *, #4471, .T. ) ;
#5281=CARTESIAN_POINT ( 'NONE',  ( 29.50000000000002132, -2.473451120191013430, 0.2999999999999947153 ) ) ;
#5285=DIRECTION ( 'NONE',  ( -1.000000000000000000, 0.000000000000000000, 0.000000000000000000 ) ) ;
#5286=ORIENTED_EDGE ( 'NONE', *, *, #17436, .F. ) ;
#5287=AXIS2_PLACEMENT_3D ( 'NONE', #14492, #21242, #17129 ) ;
#5288=ORIENTED_EDGE ( 'NONE', *, *, #21991, .T. ) ;
#5289=FACE_OUTER_BOUND ( 'NONE', #7620, .T. ) ;
#5293=( LENGTH_UNIT ( ) NAMED_UNIT ( * ) SI_UNIT ( .MILLI., .METRE. ) );
#5295=ORIENTED_EDGE ( 'NONE', *, *, #17851, .T. ) ;
#5296=AXIS2_PLACEMENT_3D ( 'NONE', #4786, #4896, #18543 ) ;
#5300=DIRECTION ( 'NONE',  ( -0.000000000000000000, -0.000000000000000000, -1.000000000000000000 ) ) ;
#5302=DIRECTION ( 'NONE',  ( -1.000000000000000000, 0.000000000000000000, -0.000000000000000000 ) ) ;
#5304=DIRECTION ( 'NONE',  ( 0.000000000000000000, 0.000000000000000000, 1.000000000000000000 ) ) ;
#5305=VECTOR ( 'NONE', #15365, 1000.000000000000000 ) ;
#5306=CARTESIAN_POINT ( 'NONE',  ( -30.07540678000427548, -6.000000000000000000, 7.200000000000000178 ) ) ;
#5307=CIRCLE ( 'NONE', #22091, 0.2999999999999999334 ) ;
#5308=CARTESIAN_POINT ( 'NONE',  ( -23.32398829872514057, 7.118794219358020148E-15, 13.79999999999999893 ) ) ;
#5311=FACE_OUTER_BOUND ( 'NONE', #9235, .T. ) ;
#5317=VERTEX_POINT ( 'NONE', #8512 ) ;
#5319=EDGE_CURVE ( 'NONE', #21932, #1327, #18685, .T. ) ;
#5325=CIRCLE ( 'NONE', #995, 0.2999999999999999334 ) ;
#5327=CARTESIAN_POINT ( 'NONE',  ( 0.000000000000000000, 32.11873716947361856, 42.50000000000000711 ) ) ;
#5328=AXIS2_PLACEMENT_3D ( 'NONE', #16174, #19893, #11152 ) ;
#5329=CARTESIAN_POINT ( 'NONE',  ( -28.87540678000427619, 0.000000000000000000, 13.50000000000000000 ) ) ;
#5331=LINE ( 'NONE', #3409, #17023 ) ;
#5333=ADVANCED_FACE ( 'NONE', ( #1333 ), #14163, .T. ) ;
#5335=VECTOR ( 'NONE', #20129, 1000.000000000000000 ) ;
#5336=DIRECTION ( 'NONE',  ( 0.000000000000000000, 0.000000000000000000, 1.000000000000000000 ) ) ;
#5337=CARTESIAN_POINT ( 'NONE',  ( -29.37540678000427619, 6.000000000000000000, 7.500000000000000000 ) ) ;
#5339=VECTOR ( 'NONE', #16981, 1000.000000000000000 ) ;
#5342=DIRECTION ( 'NONE',  ( 0.000000000000000000, 0.000000000000000000, 1.000000000000000000 ) ) ;
#5343=ORIENTED_EDGE ( 'NONE', *, *, #9449, .F. ) ;
#5347=CARTESIAN_POINT ( 'NONE',  ( -14.96174975910705207, -51.61873716947361856, 68.00000000000000000 ) ) ;
#5349=CARTESIAN_POINT ( 'NONE',  ( 0.000000000000000000, -38.74634676501045760, 13.79999999999999893 ) ) ;
#5351=AXIS2_PLACEMENT_3D ( 'NONE', #9003, #7326, #17057 ) ;
#5353=DIRECTION ( 'NONE',  ( 0.000000000000000000, 0.000000000000000000, 1.000000000000000000 ) ) ;
#5355=ORIENTED_EDGE ( 'NONE', *, *, #2679, .F. ) ;
#5356=DIRECTION ( 'NONE',  ( -0.000000000000000000, -0.000000000000000000, -1.000000000000000000 ) ) ;
#5357=CARTESIAN_POINT ( 'NONE',  ( -23.02398829872513986, 3.528912754968630328, 13.79999999999999893 ) ) ;
#5358=CARTESIAN_POINT ( 'NONE',  ( -29.13662752439705272, 0.000000000000000000, 3.799999999999999822 ) ) ;
#5361=DIRECTION ( 'NONE',  ( 1.000000000000000000, 0.000000000000000000, 0.000000000000000000 ) ) ;
#5363=EDGE_CURVE ( 'NONE', #16845, #16208, #6406, .T. ) ;
#5364=DIRECTION ( 'NONE',  ( 1.000000000000000000, -0.000000000000000000, -0.000000000000000000 ) ) ;
#5365=CARTESIAN_POINT ( 'NONE',  ( 8.641460742840918030, -32.93424481021354921, 7.321391277662001151 ) ) ;
#5367=EDGE_CURVE ( 'NONE', #1806, #9791, #10603, .T. ) ;
#5368=ORIENTED_EDGE ( 'NONE', *, *, #9851, .T. ) ;
#5369=AXIS2_PLACEMENT_3D ( 'NONE', #7438, #13080, #17604 ) ;
#5370=DIRECTION ( 'NONE',  ( 1.000000000000000000, 0.000000000000000000, 0.000000000000000000 ) ) ;
#5371=ORIENTED_EDGE ( 'NONE', *, *, #9646, .T. ) ;
#5372=CYLINDRICAL_SURFACE ( 'NONE', #5698, 0.2999999999999999334 ) ;
#5374=ORIENTED_EDGE ( 'NONE', *, *, #2588, .F. ) ;
#5379=CARTESIAN_POINT ( 'NONE',  ( 15.21174975910705918, 52.10286008774954780, 13.87500000000000000 ) ) ;
#5380=AXIS2_PLACEMENT_3D ( 'NONE', #7766, #11212, #19842 ) ;
#5381=CYLINDRICAL_SURFACE ( 'NONE', #2577, 2.000000000000001776 ) ;
#5382=EDGE_CURVE ( 'NONE', #2230, #5647, #4524, .T. ) ;
#5385=CARTESIAN_POINT ( 'NONE',  ( 29.13662752439705272, -5.000000000000000000, 7.200000000000000178 ) ) ;
#5387=CARTESIAN_POINT ( 'NONE',  ( -30.67540678000428045, -6.000000000000000000, 3.799999999999999822 ) ) ;
#5388=DIRECTION ( 'NONE',  ( 0.000000000000000000, 0.000000000000000000, 1.000000000000000000 ) ) ;
#5389=CARTESIAN_POINT ( 'NONE',  ( 30.37540678000427619, -6.000000000000000000, 3.799999999999999822 ) ) ;
#5390=ORIENTED_EDGE ( 'NONE', *, *, #11702, .T. ) ;
#5391=LINE ( 'NONE', #5055, #19208 ) ;
#5393=VECTOR ( 'NONE', #8757, 1000.000000000000000 ) ;
#5398=ADVANCED_FACE ( 'NONE', ( #2920 ), #3818, .T. ) ;
#5400=FACE_OUTER_BOUND ( 'NONE', #16610, .T. ) ;
#5402=ORIENTED_EDGE ( 'NONE', *, *, #16193, .T. ) ;
#5403=EDGE_CURVE ( 'NONE', #21455, #6635, #13787, .T. ) ;
#5404=VECTOR ( 'NONE', #563, 1000.000000000000000 ) ;
#5405=LINE ( 'NONE', #7191, #4868 ) ;
#5407=LINE ( 'NONE', #10533, #12345 ) ;
#5408=CARTESIAN_POINT ( 'NONE',  ( 15.95292532278785913, 52.10286008774954780, 13.87499999999999822 ) ) ;
#5409=AXIS2_PLACEMENT_3D ( 'NONE', #6853, #11523, #5049 ) ;
#5411=CARTESIAN_POINT ( 'NONE',  ( 9.641460742840918030, 32.61873716947361856, 68.00000000000000000 ) ) ;
#5413=CARTESIAN_POINT ( 'NONE',  ( -23.02398829872513986, 2.157133714763345367, 13.26827027136043213 ) ) ;
#5416=CARTESIAN_POINT ( 'NONE',  ( 0.000000000000000000, -32.61873716947361856, 68.00000000000000000 ) ) ;
#5417=FACE_OUTER_BOUND ( 'NONE', #17563, .T. ) ;
#5419=ORIENTED_EDGE ( 'NONE', *, *, #11402, .F. ) ;
#5420=EDGE_LOOP ( 'NONE', ( #17716, #21461, #10222, #7016 ) ) ;
#5421=DIRECTION ( 'NONE',  ( -3.052134192567367925E-16, 1.000000000000000000, -0.000000000000000000 ) ) ;
#5423=EDGE_CURVE ( 'NONE', #8790, #1357, #11302, .T. ) ;
#5425=CIRCLE ( 'NONE', #16786, 0.5000000000000004441 ) ;
#5426=VECTOR ( 'NONE', #15906, 1000.000000000000000 ) ;
#5429=AXIS2_PLACEMENT_3D ( 'NONE', #17250, #8660, #6984 ) ;
#5431=AXIS2_PLACEMENT_3D ( 'NONE', #13673, #10219, #17151 ) ;
#5433=LINE ( 'NONE', #3737, #567 ) ;
#5434=VERTEX_POINT ( 'NONE', #1529 ) ;
#5435=DIRECTION ( 'NONE',  ( -1.000000000000000000, 0.000000000000000000, 0.000000000000000000 ) ) ;
#5436=ADVANCED_FACE ( 'NONE', ( #8040 ), #16420, .T. ) ;
#5439=DIRECTION ( 'NONE',  ( 0.000000000000000000, 0.000000000000000000, 1.000000000000000000 ) ) ;
#5440=DIRECTION ( 'NONE',  ( 0.000000000000000000, 0.000000000000000000, 1.000000000000000000 ) ) ;
#5441=DIRECTION ( 'NONE',  ( -1.000000000000000000, 0.000000000000000000, 0.000000000000000000 ) ) ;
#5442=EDGE_LOOP ( 'NONE', ( #18710, #928, #2547, #9957, #20871, #7879 ) ) ;
#5444=CARTESIAN_POINT ( 'NONE',  ( 29.13662752439705272, 0.000000000000000000, 3.500000000000000000 ) ) ;
#5446=VERTEX_POINT ( 'NONE', #1092 ) ;
#5459=DIRECTION ( 'NONE',  ( 0.000000000000000000, -1.000000000000000000, 0.000000000000000000 ) ) ;
#5462=DIRECTION ( 'NONE',  ( 1.000000000000000000, 0.000000000000000000, -0.000000000000000000 ) ) ;
#5464=DIRECTION ( 'NONE',  ( 0.000000000000000000, 0.000000000000000000, 1.000000000000000000 ) ) ;
#5465=CARTESIAN_POINT ( 'NONE',  ( 0.000000000000000000, -5.299999999999999822, 7.500000000000000000 ) ) ;
#5466=DIRECTION ( 'NONE',  ( 0.000000000000000000, 0.000000000000000000, -1.000000000000000000 ) ) ;
#5468=VERTEX_POINT ( 'NONE', #6489 ) ;
#5469=DIRECTION ( 'NONE',  ( 0.000000000000000000, 0.000000000000000000, -1.000000000000000000 ) ) ;
#5479=CARTESIAN_POINT ( 'NONE',  ( -17.95292532278785913, 0.000000000000000000, 42.50000000000000711 ) ) ;
#5481=ORIENTED_EDGE ( 'NONE', *, *, #1445, .F. ) ;
#5482=CIRCLE ( 'NONE', #14019, 0.2999999999999999334 ) ;
#5484=DIRECTION ( 'NONE',  ( 0.000000000000000000, 0.000000000000000000, 1.000000000000000000 ) ) ;
#5485=VERTEX_POINT ( 'NONE', #19902 ) ;
#5486=ORIENTED_EDGE ( 'NONE', *, *, #20977, .T. ) ;
#5487=EDGE_CURVE ( 'NONE', #17759, #14667, #8819, .T. ) ;
#5488=EDGE_CURVE ( 'NONE', #9687, #20783, #8464, .T. ) ;
#5490=ADVANCED_FACE ( 'NONE', ( #3103 ), #12709, .T. ) ;
#5491=ORIENTED_EDGE ( 'NONE', *, *, #14973, .F. ) ;
#5492=DIRECTION ( 'NONE',  ( 0.000000000000000000, 0.000000000000000000, 1.000000000000000000 ) ) ;
#5494=DIRECTION ( 'NONE',  ( 1.000000000000000000, 0.000000000000000000, 0.000000000000000000 ) ) ;
#5495=FACE_OUTER_BOUND ( 'NONE', #10139, .T. ) ;
#5498=CARTESIAN_POINT ( 'NONE',  ( -17.95292532278785913, 34.11873716947361856, 109.6002446535588319 ) ) ;
#5499=DIRECTION ( 'NONE',  ( -0.000000000000000000, -0.000000000000000000, -1.000000000000000000 ) ) ;
#5500=DIRECTION ( 'NONE',  ( 1.000000000000000000, 0.000000000000000000, 0.000000000000000000 ) ) ;
#5504=CARTESIAN_POINT ( 'NONE',  ( -14.98564789012718101, 51.95085597973990588, 13.85527924978055481 ) ) ;
#5505=ORIENTED_EDGE ( 'NONE', *, *, #2256, .T. ) ;
#5508=CARTESIAN_POINT ( 'NONE',  ( -4.127054932750482408, 33.93424481021354921, 68.00000000000000000 ) ) ;
#5510=ORIENTED_EDGE ( 'NONE', *, *, #15368, .T. ) ;
#5512=LINE ( 'NONE', #12290, #19021 ) ;
#5513=ORIENTED_EDGE ( 'NONE', *, *, #8974, .T. ) ;
#5514=ORIENTED_EDGE ( 'NONE', *, *, #6871, .F. ) ;
#5515=DIRECTION ( 'NONE',  ( 0.000000000000000000, 0.000000000000000000, -1.000000000000000000 ) ) ;
#5518=CARTESIAN_POINT ( 'NONE',  ( -29.37540678000427619, 6.000000000000000000, 3.799999999999999822 ) ) ;
#5519=CARTESIAN_POINT ( 'NONE',  ( 28.64417692495746692, 6.713479613976641502, 13.50000000000000000 ) ) ;
#5521=CARTESIAN_POINT ( 'NONE',  ( -29.37540678000427619, 5.000000000000000000, 7.200000000000000178 ) ) ;
#5523=CARTESIAN_POINT ( 'NONE',  ( 14.96174975910707161, -51.86873716947361856, 68.00000000000000000 ) ) ;
#5524=TOROIDAL_SURFACE ( 'NONE', #5167, 0.7000000000000000666, 0.2999999999999999889 ) ;
#5525=CARTESIAN_POINT ( 'NONE',  ( 29.13662752439705272, 0.000000000000000000, 7.200000000000000178 ) ) ;
#5526=CARTESIAN_POINT ( 'NONE',  ( -25.37540678000427263, -67.24634676501045760, 13.19999999999999929 ) ) ;
#5528=VERTEX_POINT ( 'NONE', #21918 ) ;
#5529=CARTESIAN_POINT ( 'NONE',  ( -29.37540678000427619, 6.000000000000000000, 7.200000000000000178 ) ) ;
#5530=EDGE_CURVE ( 'NONE', #18467, #18812, #3223, .T. ) ;
#5531=CARTESIAN_POINT ( 'NONE',  ( 26.56227312273159313, -9.958410664601842655, 42.50000000000000000 ) ) ;
#5532=EDGE_CURVE ( 'NONE', #13239, #2467, #21484, .T. ) ;
#5533=VERTEX_POINT ( 'NONE', #17383 ) ;
#5535=ADVANCED_FACE ( 'NONE', ( #20869 ), #19078, .T. ) ;
#5537=DIRECTION ( 'NONE',  ( 1.000000000000000000, 0.000000000000000000, 0.000000000000000000 ) ) ;
#5538=ORIENTED_EDGE ( 'NONE', *, *, #6225, .F. ) ;
#5539=CARTESIAN_POINT ( 'NONE',  ( 23.32398829872514057, -2.157133568460767759, 13.19999999999999929 ) ) ;
#5541=EDGE_CURVE ( 'NONE', #15844, #12670, #10688, .T. ) ;
#5546=DIRECTION ( 'NONE',  ( -0.000000000000000000, 0.000000000000000000, -1.000000000000000000 ) ) ;
#5547=LINE ( 'NONE', #3869, #8273 ) ;
#5548=DIRECTION ( 'NONE',  ( 1.000000000000000000, 0.000000000000000000, 0.000000000000000000 ) ) ;
#5549=DIRECTION ( 'NONE',  ( 0.000000000000000000, 1.000000000000000000, -0.000000000000000000 ) ) ;
#5550=VERTEX_POINT ( 'NONE', #2169 ) ;
#5551=AXIS2_PLACEMENT_3D ( 'NONE', #13423, #21737, #18350 ) ;
#5553=AXIS2_PLACEMENT_3D ( 'NONE', #21188, #12973, #19480 ) ;
#5554=ORIENTED_EDGE ( 'NONE', *, *, #13761, .F. ) ;
#5555=DIRECTION ( 'NONE',  ( 0.000000000000000000, 0.000000000000000000, -1.000000000000000000 ) ) ;
#5556=CARTESIAN_POINT ( 'NONE',  ( -18.22752199202934520, 38.74634676501045760, 13.79999999999999893 ) ) ;
#5557=EDGE_CURVE ( 'NONE', #9928, #20941, #9418, .T. ) ;
#5558=DIRECTION ( 'NONE',  ( 1.000000000000000000, -0.000000000000000000, 0.000000000000000000 ) ) ;
#5560=EDGE_LOOP ( 'NONE', ( #19728, #2017, #7315, #14694 ) ) ;
#5564=ORIENTED_EDGE ( 'NONE', *, *, #13912, .F. ) ;
#5565=DIRECTION ( 'NONE',  ( 0.000000000000000000, 0.000000000000000000, 1.000000000000000000 ) ) ;
#5568=DIRECTION ( 'NONE',  ( -0.000000000000000000, -1.000000000000000000, -0.000000000000000000 ) ) ;
#5569=DIRECTION ( 'NONE',  ( 1.000000000000000000, 0.000000000000000000, 0.000000000000000000 ) ) ;
#5571=CARTESIAN_POINT ( 'NONE',  ( -15.21174975910705207, -42.11054587065083155, 13.50000000000000000 ) ) ;
#5572=ORIENTED_EDGE ( 'NONE', *, *, #517, .T. ) ;
#5578=ORIENTED_EDGE ( 'NONE', *, *, #16295, .T. ) ;
#5581=DIRECTION ( 'NONE',  ( -0.000000000000000000, -0.000000000000000000, -1.000000000000000000 ) ) ;
#5582=DIRECTION ( 'NONE',  ( 0.000000000000000000, 1.000000000000000000, -0.000000000000000000 ) ) ;
#5583=ORIENTED_EDGE ( 'NONE', *, *, #3776, .T. ) ;
#5586=DIRECTION ( 'NONE',  ( 1.000000000000000000, -0.000000000000000000, -0.000000000000000000 ) ) ;
#5590=CIRCLE ( 'NONE', #18784, 1.499999999999999556 ) ;
#5591=EDGE_CURVE ( 'NONE', #19345, #16058, #17233, .T. ) ;
#5594=CYLINDRICAL_SURFACE ( 'NONE', #2055, 0.3000000000000003775 ) ;
#5595=AXIS2_PLACEMENT_3D ( 'NONE', #8712, #10490, #17298 ) ;
#5596=VECTOR ( 'NONE', #8227, 1000.000000000000000 ) ;
#5598=TOROIDAL_SURFACE ( 'NONE', #5945, 0.7000000000000000666, 0.2999999999999999889 ) ;
#5599=DIRECTION ( 'NONE',  ( -1.000000000000000000, 0.000000000000000000, 0.000000000000000000 ) ) ;
#5600=DIRECTION ( 'NONE',  ( -0.000000000000000000, -0.000000000000000000, -1.000000000000000000 ) ) ;
#5601=CARTESIAN_POINT ( 'NONE',  ( 25.37540678000427263, 63.74634676501045050, 7.500000000000000000 ) ) ;
#5603=CARTESIAN_POINT ( 'NONE',  ( -18.22752199202934520, 39.04634676501046187, 13.50000000000000000 ) ) ;
#5606=DIRECTION ( 'NONE',  ( 0.000000000000000000, 0.000000000000000000, 1.000000000000000000 ) ) ;
#5609=B_SPLINE_CURVE_WITH_KNOTS ( 'NONE', 3,
 ( #5775, #4299, #19186, #5877, #8901, #2504, #14356, #14453 ),
 .UNSPECIFIED., .F., .F.,
 ( 4, 2, 2, 4 ),
 ( -3.470042892451968281E-06, 0.0002769752510348927397, 0.0004171978979985645165, 0.0005574205449622362391 ),
 .UNSPECIFIED. ) ;
#5612=ORIENTED_EDGE ( 'NONE', *, *, #6604, .F. ) ;
#5613=CIRCLE ( 'NONE', #11298, 0.5000000000000004441 ) ;
#5614=CIRCLE ( 'NONE', #214, 4.999999999999997335 ) ;
#5615=ORIENTED_EDGE ( 'NONE', *, *, #9770, .T. ) ;
#5617=CARTESIAN_POINT ( 'NONE',  ( -31.50000000000002132, 71.70000000000001705, 3.500000000000000000 ) ) ;
#5619=EDGE_CURVE ( 'NONE', #1813, #17313, #107, .T. ) ;
#5620=ORIENTED_EDGE ( 'NONE', *, *, #9724, .T. ) ;
#5623=CARTESIAN_POINT ( 'NONE',  ( -26.33662752439704846, 0.000000000000000000, 8.402566836762659364E-16 ) ) ;
#5624=ORIENTED_EDGE ( 'NONE', *, *, #7761, .T. ) ;
#5629=LINE ( 'NONE', #12418, #10578 ) ;
#5634=EDGE_CURVE ( 'NONE', #15404, #22008, #14994, .T. ) ;
#5635=AXIS2_PLACEMENT_3D ( 'NONE', #8951, #7061, #13855 ) ;
#5636=CARTESIAN_POINT ( 'NONE',  ( -23.07499583180669234, 2.433548416302913520, 13.33575415462846081 ) ) ;
#5641=TOROIDAL_SURFACE ( 'NONE', #14527, 2.274596669241483848, 0.2999999999999999889 ) ;
#5642=CARTESIAN_POINT ( 'NONE',  ( -14.96244602927844980, -51.84405746083547939, 13.82646097708239452 ) ) ;
#5643=VERTEX_POINT ( 'NONE', #18117 ) ;
#5645=CARTESIAN_POINT ( 'NONE',  ( 23.02398829872513986, 7.027230193580998154E-15, 13.79999999999999893 ) ) ;
#5647=VERTEX_POINT ( 'NONE', #18648 ) ;
#5648=ORIENTED_EDGE ( 'NONE', *, *, #8192, .F. ) ;
#5652=VECTOR ( 'NONE', #11018, 1000.000000000000000 ) ;
#5653=B_SPLINE_CURVE_WITH_KNOTS ( 'NONE', 3,
 ( #9694, #4531, #18392, #17954, #19991, #829, #16594, #6339, #13251, #2627 ),
 .UNSPECIFIED., .F., .F.,
 ( 4, 2, 2, 2, 4 ),
 ( 0.000000000000000000, 0.0007882085451459004124, 0.001182312817718851215, 0.001379364954005326670, 0.001576417090291802126 ),
 .UNSPECIFIED. ) ;
#5659=DIRECTION ( 'NONE',  ( 1.000000000000000000, 0.000000000000000000, 0.000000000000000000 ) ) ;
#5661=EDGE_CURVE ( 'NONE', #19800, #1806, #3782, .T. ) ;
#5663=DIRECTION ( 'NONE',  ( 0.000000000000000000, 0.000000000000000000, 1.000000000000000000 ) ) ;
#5664=LINE ( 'NONE', #15485, #3369 ) ;
#5670=DIRECTION ( 'NONE',  ( 0.000000000000000000, 0.000000000000000000, 1.000000000000000000 ) ) ;
#5676=VECTOR ( 'NONE', #19487, 1000.000000000000000 ) ;
#5677=ORIENTED_EDGE ( 'NONE', *, *, #19603, .F. ) ;
#5678=CYLINDRICAL_SURFACE ( 'NONE', #15278, 0.2999999999999999889 ) ;
#5681=ORIENTED_EDGE ( 'NONE', *, *, #9324, .F. ) ;
#5685=DIRECTION ( 'NONE',  ( 0.000000000000000000, 0.000000000000000000, 1.000000000000000000 ) ) ;
#5688=CARTESIAN_POINT ( 'NONE',  ( -29.13662752439705272, 0.000000000000000000, 3.500000000000000000 ) ) ;
#5693=LINE ( 'NONE', #17733, #1853 ) ;
#5694=TOROIDAL_SURFACE ( 'NONE', #10672, 3.200000000000003286, 0.2999999999999999889 ) ;
#5695=DIRECTION ( 'NONE',  ( -1.000000000000000000, -0.000000000000000000, 0.000000000000000000 ) ) ;
#5698=AXIS2_PLACEMENT_3D ( 'NONE', #3682, #7491, #8825 ) ;
#5701=EDGE_CURVE ( 'NONE', #2319, #10473, #12318, .T. ) ;
#5703=CARTESIAN_POINT ( 'NONE',  ( -23.21374285137841298, -3.085791193308922153, 13.47995019114138238 ) ) ;
#5704=EDGE_LOOP ( 'NONE', ( #20829, #5112, #21269, #13676 ) ) ;
#5705=CARTESIAN_POINT ( 'NONE',  ( -29.37540678000427619, 5.299999999999999822, 7.200000000000000178 ) ) ;
#5706=ORIENTED_EDGE ( 'NONE', *, *, #12217, .F. ) ;
#5707=FACE_OUTER_BOUND ( 'NONE', #15341, .T. ) ;
#5708=DIRECTION ( 'NONE',  ( 0.000000000000000000, 0.000000000000000000, -1.000000000000000000 ) ) ;
#5709=AXIS2_PLACEMENT_3D ( 'NONE', #11934, #18663, #13719 ) ;
#5710=ORIENTED_EDGE ( 'NONE', *, *, #12013, .T. ) ;
#5711=ORIENTED_EDGE ( 'NONE', *, *, #7049, .F. ) ;
#5713=DIRECTION ( 'NONE',  ( 0.000000000000000000, 0.000000000000000000, 1.000000000000000000 ) ) ;
#5714=CIRCLE ( 'NONE', #1757, 0.2999999999999999334 ) ;
#5715=ORIENTED_EDGE ( 'NONE', *, *, #12616, .F. ) ;
#5716=CIRCLE ( 'NONE', #8557, 6.499999999999999112 ) ;
#5718=ORIENTED_EDGE ( 'NONE', *, *, #9309, .F. ) ;
#5720=CARTESIAN_POINT ( 'NONE',  ( 14.96174975910705918, -51.76873716947361714, 13.79999999999999716 ) ) ;
#5722=DIRECTION ( 'NONE',  ( 0.000000000000000000, 0.000000000000000000, -1.000000000000000000 ) ) ;
#5724=CIRCLE ( 'NONE', #16041, 0.5000000000000000000 ) ;
#5728=EDGE_CURVE ( 'NONE', #20699, #13326, #14511, .T. ) ;
#5729=DIRECTION ( 'NONE',  ( -1.000000000000000000, 0.000000000000000000, 0.000000000000000000 ) ) ;
#5730=DIRECTION ( 'NONE',  ( -1.000000000000000000, -0.000000000000000000, 0.000000000000000000 ) ) ;
#5731=EDGE_LOOP ( 'NONE', ( #18643, #13729, #5119, #9922 ) ) ;
#5732=DIRECTION ( 'NONE',  ( -1.000000000000000000, 0.000000000000000000, 0.000000000000000000 ) ) ;
#5742=ORIENTED_EDGE ( 'NONE', *, *, #16209, .T. ) ;
#5744=CARTESIAN_POINT ( 'NONE',  ( 23.10703542945396549, -2.595685412882492660, 13.38944394804412852 ) ) ;
#5745=VERTEX_POINT ( 'NONE', #4247 ) ;
#5747=DIRECTION ( 'NONE',  ( 0.000000000000000000, 0.000000000000000000, 1.000000000000000000 ) ) ;
#5748=CARTESIAN_POINT ( 'NONE',  ( 15.21174975910705918, -41.81054587065082728, 13.75000000000000000 ) ) ;
#5749=DIRECTION ( 'NONE',  ( 1.000000000000000000, 0.000000000000000000, 0.000000000000000000 ) ) ;
#5750=EDGE_CURVE ( 'NONE', #712, #2722, #6052, .T. ) ;
#5751=AXIS2_PLACEMENT_3D ( 'NONE', #5093, #18733, #6664 ) ;
#5753=LINE ( 'NONE', #12531, #20119 ) ;
#5755=CARTESIAN_POINT ( 'NONE',  ( 14.96174975910707161, -41.81054587065082728, 68.25000000000000000 ) ) ;
#5756=LINE ( 'NONE', #12534, #20050 ) ;
#5761=ORIENTED_EDGE ( 'NONE', *, *, #8616, .F. ) ;
#5763=EDGE_CURVE ( 'NONE', #7158, #11635, #15197, .T. ) ;
#5766=DIRECTION ( 'NONE',  ( 1.000000000000000000, 0.000000000000000000, 0.000000000000000000 ) ) ;
#5769=DIRECTION ( 'NONE',  ( 1.000000000000000000, 0.000000000000000000, 0.000000000000000000 ) ) ;
#5770=DIRECTION ( 'NONE',  ( 0.000000000000000000, -1.000000000000000000, 0.000000000000000000 ) ) ;
#5771=CARTESIAN_POINT ( 'NONE',  ( -29.37540678000427619, -6.000000000000000000, 7.200000000000000178 ) ) ;
#5772=CARTESIAN_POINT ( 'NONE',  ( 31.50000000000002132, 71.00000000000001421, 3.200000000000000178 ) ) ;
#5774=CARTESIAN_POINT ( 'NONE',  ( -25.37540678000427263, 69.04634676501045476, 3.500000000000000000 ) ) ;
#5775=CARTESIAN_POINT ( 'NONE',  ( 28.57540678000427548, -6.776800961815481195, 13.50000000000000000 ) ) ;
#5777=FACE_OUTER_BOUND ( 'NONE', #502, .T. ) ;
#5779=ADVANCED_FACE ( 'NONE', ( #11166 ), #9833, .T. ) ;
#5780=ORIENTED_EDGE ( 'NONE', *, *, #14502, .F. ) ;
#5782=ORIENTED_EDGE ( 'NONE', *, *, #12390, .F. ) ;
#5784=FACE_OUTER_BOUND ( 'NONE', #998, .T. ) ;
#5786=CARTESIAN_POINT ( 'NONE',  ( 30.67540678000428045, 0.000000000000000000, 3.799999999999999822 ) ) ;
#5788=CIRCLE ( 'NONE', #14334, 3.200000000000001510 ) ;
#5794=DIRECTION ( 'NONE',  ( 1.000000000000000000, 0.000000000000000000, -2.388292521039847891E-16 ) ) ;
#5796=DIRECTION ( 'NONE',  ( 0.000000000000000000, 0.000000000000000000, -1.000000000000000000 ) ) ;
#5799=CARTESIAN_POINT ( 'NONE',  ( 25.37540678000427263, 63.74634676501045050, 7.200000000000000178 ) ) ;
#5801=DIRECTION ( 'NONE',  ( 0.000000000000000000, -0.000000000000000000, -1.000000000000000000 ) ) ;
#5802=DIRECTION ( 'NONE',  ( -0.000000000000000000, 0.000000000000000000, 1.000000000000000000 ) ) ;
#5803=ORIENTED_EDGE ( 'NONE', *, *, #18415, .T. ) ;
#5808=AXIS2_PLACEMENT_3D ( 'NONE', #1211, #9634, #8061 ) ;
#5811=DIRECTION ( 'NONE',  ( -0.000000000000000000, 0.000000000000000000, -1.000000000000000000 ) ) ;
#5812=ORIENTED_EDGE ( 'NONE', *, *, #13810, .T. ) ;
#5813=ORIENTED_EDGE ( 'NONE', *, *, #11151, .F. ) ;
#5814=CYLINDRICAL_SURFACE ( 'NONE', #4231, 0.3000000000000003775 ) ;
#5816=EDGE_CURVE ( 'NONE', #20280, #20277, #18099, .T. ) ;
#5824=DIRECTION ( 'NONE',  ( 0.000000000000000000, 0.000000000000000000, -1.000000000000000000 ) ) ;
#5829=CARTESIAN_POINT ( 'NONE',  ( 15.05486995871383016, 52.39333383871512240, 13.50000000000000533 ) ) ;
#5830=CIRCLE ( 'NONE', #801, 2.274596669241483848 ) ;
#5831=EDGE_CURVE ( 'NONE', #4245, #21143, #18778, .T. ) ;
#5833=FACE_OUTER_BOUND ( 'NONE', #17376, .T. ) ;
#5834=ORIENTED_EDGE ( 'NONE', *, *, #2157, .F. ) ;
#5836=ORIENTED_EDGE ( 'NONE', *, *, #18376, .T. ) ;
#5839=CARTESIAN_POINT ( 'NONE',  ( -25.37540678000426908, 36.74634676501047181, 42.50000000000000000 ) ) ;
#5844=EDGE_CURVE ( 'NONE', #8484, #11913, #3234, .T. ) ;
#5845=DIRECTION ( 'NONE',  ( -0.000000000000000000, -0.000000000000000000, 1.000000000000000000 ) ) ;
#5846=ORIENTED_EDGE ( 'NONE', *, *, #15150, .F. ) ;
#5853=ADVANCED_FACE ( 'NONE', ( #1312 ), #15083, .F. ) ;
#5854=DIRECTION ( 'NONE',  ( 0.000000000000000000, -1.000000000000000000, 0.000000000000000000 ) ) ;
#5855=CARTESIAN_POINT ( 'NONE',  ( -3.127054932750481964, -32.61873716947361856, 68.00000000000000000 ) ) ;
#5856=FACE_OUTER_BOUND ( 'NONE', #7263, .T. ) ;
#5859=ORIENTED_EDGE ( 'NONE', *, *, #2148, .T. ) ;
#5862=EDGE_CURVE ( 'NONE', #12755, #5867, #19851, .T. ) ;
#5864=VERTEX_POINT ( 'NONE', #6497 ) ;
#5867=VERTEX_POINT ( 'NONE', #8088 ) ;
#5869=ORIENTED_EDGE ( 'NONE', *, *, #18806, .T. ) ;
#5870=CARTESIAN_POINT ( 'NONE',  ( 15.95292532278785913, 50.11873716947361856, 109.6002446535588319 ) ) ;
#5872=CARTESIAN_POINT ( 'NONE',  ( 15.07117748393522483, 52.06955913406978453, 13.87289863735440321 ) ) ;
#5873=FACE_OUTER_BOUND ( 'NONE', #10495, .T. ) ;
#5875=EDGE_CURVE ( 'NONE', #20894, #13259, #3767, .T. ) ;
#5877=CARTESIAN_POINT ( 'NONE',  ( 28.79994065384636315, -6.566898051583388352, 13.40260211333369256 ) ) ;
#5883=ORIENTED_EDGE ( 'NONE', *, *, #21949, .T. ) ;
#5889=VERTEX_POINT ( 'NONE', #1773 ) ;
#5894=CARTESIAN_POINT ( 'NONE',  ( -27.67540678000426269, 36.74634676501047181, 13.79999999999999893 ) ) ;
#5895=CARTESIAN_POINT ( 'NONE',  ( 14.96174975910707161, -41.81054587065082728, 68.25000000000000000 ) ) ;
#5899=DIRECTION ( 'NONE',  ( 1.000000000000000000, 0.000000000000000000, 0.000000000000000000 ) ) ;
#5901=VERTEX_POINT ( 'NONE', #11721 ) ;
#5902=DIRECTION ( 'NONE',  ( -0.000000000000000000, -1.000000000000000000, 0.000000000000000000 ) ) ;
#5905=DIRECTION ( 'NONE',  ( 0.000000000000000000, 0.000000000000000000, 1.000000000000000000 ) ) ;
#5907=ORIENTED_EDGE ( 'NONE', *, *, #7981, .F. ) ;
#5911=CARTESIAN_POINT ( 'NONE',  ( 0.000000000000000000, -39.04634676501046187, 13.50000000000000000 ) ) ;
#5912=ORIENTED_EDGE ( 'NONE', *, *, #9196, .T. ) ;
#5913=ORIENTED_EDGE ( 'NONE', *, *, #19560, .T. ) ;
#5914=CIRCLE ( 'NONE', #1946, 0.4999999999999995559 ) ;
#5917=CARTESIAN_POINT ( 'NONE',  ( -26.56227312273159313, -9.958410664601842655, 13.79999999999999893 ) ) ;
#5919=B_SPLINE_CURVE_WITH_KNOTS ( 'NONE', 3,
 ( #12556, #7226, #19401, #9007, #15908, #17608, #16134, #2053 ),
 .UNSPECIFIED., .F., .F.,
 ( 4, 2, 2, 4 ),
 ( 0.000000000000000000, 0.0004685292328704453928, 0.0007027938493056759767, 0.0009370584657409066149 ),
 .UNSPECIFIED. ) ;
#5925=ORIENTED_EDGE ( 'NONE', *, *, #20739, .T. ) ;
#5928=EDGE_CURVE ( 'NONE', #3824, #19461, #22036, .T. ) ;
#5929=DIRECTION ( 'NONE',  ( -0.000000000000000000, -0.000000000000000000, -1.000000000000000000 ) ) ;
#5931=TOROIDAL_SURFACE ( 'NONE', #7699, 0.7000000000000000666, 0.2999999999999999889 ) ;
#5932=CIRCLE ( 'NONE', #1632, 0.5000000000000004441 ) ;
#5938=ORIENTED_EDGE ( 'NONE', *, *, #13781, .T. ) ;
#5939=CARTESIAN_POINT ( 'NONE',  ( 15.95292532278785913, -50.11873716947361856, 109.6002446535588319 ) ) ;
#5942=ORIENTED_EDGE ( 'NONE', *, *, #9569, .T. ) ;
#5945=AXIS2_PLACEMENT_3D ( 'NONE', #3712, #19048, #21070 ) ;
#5949=CIRCLE ( 'NONE', #17708, 0.5000000000000004441 ) ;
#5950=VECTOR ( 'NONE', #19174, 1000.000000000000000 ) ;
#5951=FACE_OUTER_BOUND ( 'NONE', #763, .T. ) ;
#5952=DIRECTION ( 'NONE',  ( -1.000000000000000000, 0.000000000000000000, 0.000000000000000000 ) ) ;
#5953=DIRECTION ( 'NONE',  ( -0.000000000000000000, 1.000000000000000000, -0.000000000000000000 ) ) ;
#5954=DIRECTION ( 'NONE',  ( -0.000000000000000000, -0.000000000000000000, -1.000000000000000000 ) ) ;
#5958=LINE ( 'NONE', #12747, #13996 ) ;
#5964=CARTESIAN_POINT ( 'NONE',  ( 9.641460742840918030, 32.11873716947361856, 42.50000000000000711 ) ) ;
#5966=ORIENTED_EDGE ( 'NONE', *, *, #1669, .T. ) ;
#5967=VECTOR ( 'NONE', #1227, 1000.000000000000000 ) ;
#5968=EDGE_LOOP ( 'NONE', ( #12050, #21790, #18403, #9875 ) ) ;
#5970=DIRECTION ( 'NONE',  ( 0.000000000000000000, 0.000000000000000000, 1.000000000000000000 ) ) ;
#5972=ORIENTED_EDGE ( 'NONE', *, *, #19934, .T. ) ;
#5974=AXIS2_PLACEMENT_3D ( 'NONE', #7791, #1836, #1500 ) ;
#5975=VECTOR ( 'NONE', #20895, 1000.000000000000000 ) ;
#5977=VECTOR ( 'NONE', #12945, 1000.000000000000000 ) ;
#5980=ORIENTED_EDGE ( 'NONE', *, *, #14451, .F. ) ;
#5982=DIRECTION ( 'NONE',  ( 1.000000000000000000, 0.000000000000000000, 0.000000000000000000 ) ) ;
#5983=ADVANCED_FACE ( 'NONE', ( #13722 ), #8165, .F. ) ;
#5984=DIRECTION ( 'NONE',  ( 0.000000000000000000, 1.000000000000000000, 0.000000000000000000 ) ) ;
#5985=CARTESIAN_POINT ( 'NONE',  ( -29.37540678000427619, -5.000000000000000000, 3.799999999999999822 ) ) ;
#5988=EDGE_CURVE ( 'NONE', #11011, #4007, #13742, .T. ) ;
#5992=AXIS2_PLACEMENT_3D ( 'NONE', #17348, #20731, #13991 ) ;
#5994=ORIENTED_EDGE ( 'NONE', *, *, #17066, .F. ) ;
#5995=AXIS2_PLACEMENT_3D ( 'NONE', #1439, #8280, #11837 ) ;
#5997=VERTEX_POINT ( 'NONE', #17537 ) ;
#6001=AXIS2_PLACEMENT_3D ( 'NONE', #20524, #13900, #10778 ) ;
#6002=LINE ( 'NONE', #6220, #2709 ) ;
#6005=ORIENTED_EDGE ( 'NONE', *, *, #15555, .T. ) ;
#6006=CARTESIAN_POINT ( 'NONE',  ( -9.641460742840918030, -32.61873716947361856, 68.50000000000000000 ) ) ;
#6008=ADVANCED_FACE ( 'NONE', ( #2203 ), #19107, .T. ) ;
#6009=LINE ( 'NONE', #941, #14575 ) ;
#6011=CIRCLE ( 'NONE', #9203, 0.2999999999999999334 ) ;
#6015=EDGE_LOOP ( 'NONE', ( #13329, #11202, #1240, #12083 ) ) ;
#6019=CARTESIAN_POINT ( 'NONE',  ( -14.98825539710680310, 51.95771298364782353, 13.85621828746129403 ) ) ;
#6020=DIRECTION ( 'NONE',  ( 1.000000000000000000, 0.000000000000000000, 0.000000000000000000 ) ) ;
#6022=FACE_OUTER_BOUND ( 'NONE', #14642, .T. ) ;
#6023=VECTOR ( 'NONE', #19828, 1000.000000000000000 ) ;
#6024=DIRECTION ( 'NONE',  ( 1.000000000000000000, -0.000000000000000000, -0.000000000000000000 ) ) ;
#6027=EDGE_LOOP ( 'NONE', ( #3734, #7372, #10117, #11650 ) ) ;
#6028=CARTESIAN_POINT ( 'NONE',  ( -17.92752199202934094, 50.11873716947361856, 13.79999999999999893 ) ) ;
#6030=VERTEX_POINT ( 'NONE', #9139 ) ;
#6031=EDGE_LOOP ( 'NONE', ( #3241, #13865, #16098, #18745 ) ) ;
#6034=AXIS2_PLACEMENT_3D ( 'NONE', #233, #762, #21155 ) ;
#6036=AXIS2_PLACEMENT_3D ( 'NONE', #9458, #14274, #17850 ) ;
#6037=VERTEX_POINT ( 'NONE', #8928 ) ;
#6042=LINE ( 'NONE', #19676, #14191 ) ;
#6048=CARTESIAN_POINT ( 'NONE',  ( -17.93704824106378837, 0.000000000000000000, 13.87500000000000000 ) ) ;
#6049=DIRECTION ( 'NONE',  ( 0.000000000000000000, 1.000000000000000000, 0.000000000000000000 ) ) ;
#6052=LINE ( 'NONE', #21706, #8063 ) ;
#6054=AXIS2_PLACEMENT_3D ( 'NONE', #9354, #21126, #21338 ) ;
#6055=CARTESIAN_POINT ( 'NONE',  ( -8.641460742840918030, 32.93424481021354921, 68.00000000000000000 ) ) ;
#6058=VERTEX_POINT ( 'NONE', #9039 ) ;
#6060=ORIENTED_EDGE ( 'NONE', *, *, #654, .T. ) ;
#6061=DIRECTION ( 'NONE',  ( 1.000000000000000000, -0.000000000000000000, -0.000000000000000000 ) ) ;
#6063=ORIENTED_EDGE ( 'NONE', *, *, #14513, .F. ) ;
#6064=ORIENTED_EDGE ( 'NONE', *, *, #9266, .F. ) ;
#6066=CARTESIAN_POINT ( 'NONE',  ( -25.37540678000427263, -67.24634676501045760, 13.19999999999999929 ) ) ;
#6067=ORIENTED_EDGE ( 'NONE', *, *, #20063, .T. ) ;
#6069=AXIS2_PLACEMENT_3D ( 'NONE', #3805, #1520, #5004 ) ;
#6071=DIRECTION ( 'NONE',  ( -0.000000000000000000, 1.000000000000000000, -0.000000000000000000 ) ) ;
#6072=DIRECTION ( 'NONE',  ( 1.000000000000000000, 0.000000000000000000, 0.000000000000000000 ) ) ;
#6073=CARTESIAN_POINT ( 'NONE',  ( -29.13662752439705272, 5.299999999999999822, 7.500000000000000000 ) ) ;
#6074=LINE ( 'NONE', #2478, #4310 ) ;
#6076=LINE ( 'NONE', #12863, #19729 ) ;
#6078=CARTESIAN_POINT ( 'NONE',  ( 0.000000000000000000, -5.000000000000000000, 7.200000000000000178 ) ) ;
#6085=ORIENTED_EDGE ( 'NONE', *, *, #5403, .T. ) ;
#6086=ORIENTED_EDGE ( 'NONE', *, *, #4967, .F. ) ;
#6087=CARTESIAN_POINT ( 'NONE',  ( 15.21174975910707161, -51.61873716947361856, 68.00000000000000000 ) ) ;
#6088=ORIENTED_EDGE ( 'NONE', *, *, #10656, .T. ) ;
#6089=DIRECTION ( 'NONE',  ( 0.000000000000000000, -1.000000000000000000, 0.000000000000000000 ) ) ;
#6090=EDGE_LOOP ( 'NONE', ( #15849, #6067, #15969, #13031 ) ) ;
#6094=FACE_OUTER_BOUND ( 'NONE', #18726, .T. ) ;
#6096=DIRECTION ( 'NONE',  ( -1.000000000000000000, 0.000000000000000000, 0.000000000000000000 ) ) ;
#6097=ORIENTED_EDGE ( 'NONE', *, *, #4358, .F. ) ;
#6098=CYLINDRICAL_SURFACE ( 'NONE', #13974, 1.000000000000000888 ) ;
#6099=CARTESIAN_POINT ( 'NONE',  ( 15.05577974591271051, 52.39333374568191459, 13.50000000000000000 ) ) ;
#6100=DIRECTION ( 'NONE',  ( 0.000000000000000000, 1.000000000000000000, 0.000000000000000000 ) ) ;
#6102=EDGE_CURVE ( 'NONE', #8942, #6383, #954, .T. ) ;
#6107=ORIENTED_EDGE ( 'NONE', *, *, #3251, .F. ) ;
#6108=EDGE_LOOP ( 'NONE', ( #18295, #11813, #7511, #10817 ) ) ;
#6109=DIRECTION ( 'NONE',  ( 0.000000000000000000, 0.000000000000000000, -1.000000000000000000 ) ) ;
#6111=CARTESIAN_POINT ( 'NONE',  ( 3.627054932750481964, 32.61873716947361856, 68.00000000000000000 ) ) ;
#6112=ORIENTED_EDGE ( 'NONE', *, *, #15959, .F. ) ;
#6113=CIRCLE ( 'NONE', #10034, 1.974596669241483804 ) ;
#6115=ADVANCED_FACE ( 'NONE', ( #7919 ), #2876, .F. ) ;
#6118=CARTESIAN_POINT ( 'NONE',  ( 14.96174975910705918, -41.81054587065082728, 13.80000000000001315 ) ) ;
#6119=B_SPLINE_CURVE_WITH_KNOTS ( 'NONE', 3,
 ( #6785, #11670, #16930, #1598, #18729, #8435, #6662, #22106 ),
 .UNSPECIFIED., .F., .F.,
 ( 4, 2, 2, 4 ),
 ( 0.000000000000000000, 0.0001199231866840693908, 0.0002398463733681387817, 0.0004796927467362803281 ),
 .UNSPECIFIED. ) ;
#6124=CYLINDRICAL_SURFACE ( 'NONE', #753, 0.5000000000000000000 ) ;
#6128=CIRCLE ( 'NONE', #16106, 6.500000000000002665 ) ;
#6129=CARTESIAN_POINT ( 'NONE',  ( -15.13056916446892153, 52.10286008774956201, 13.87500000000000000 ) ) ;
#6131=ORIENTED_EDGE ( 'NONE', *, *, #21899, .T. ) ;
#6132=FILL_AREA_STYLE ('',( #737 ) ) ;
#6134=EDGE_CURVE ( 'NONE', #21768, #17693, #2533, .T. ) ;
#6139=ORIENTED_EDGE ( 'NONE', *, *, #8396, .T. ) ;
#6140=CARTESIAN_POINT ( 'NONE',  ( -15.13992500838820909, 52.10286008548567338, 13.87499999123205363 ) ) ;
#6145=ORIENTED_EDGE ( 'NONE', *, *, #5423, .F. ) ;
#6146=CIRCLE ( 'NONE', #8993, 0.2999999999999999334 ) ;
#6147=ORIENTED_EDGE ( 'NONE', *, *, #22026, .F. ) ;
#6149=EDGE_CURVE ( 'NONE', #17036, #9183, #21677, .T. ) ;
#6150=DIRECTION ( 'NONE',  ( 0.000000000000000000, 0.000000000000000000, -1.000000000000000000 ) ) ;
#6151=DIRECTION ( 'NONE',  ( 0.000000000000000000, 0.000000000000000000, -1.000000000000000000 ) ) ;
#6152=AXIS2_PLACEMENT_3D ( 'NONE', #15699, #5663, #372 ) ;
#6162=( BOUNDED_SURFACE ( )  B_SPLINE_SURFACE ( 3, 2, ( 
 ( #3700, #10524, #17332 ),
 ( #13973, #12695, #2004 ),
 ( #19548, #15657, #330 ),
 ( #5504, #18204, #2762 ),
 ( #16515, #13375, #21908 ),
 ( #21580, #1180, #16613 ),
 ( #6140, #21473, #21687 ),
 ( #2647, #3091, #11250 ) ),
 .UNSPECIFIED., .F., .F., .T. ) 
 B_SPLINE_SURFACE_WITH_KNOTS ( ( 4, 2, 2, 4 ),
 ( 3, 3 ),
 ( -1.016439536705160407E-20, 0.0002312589012449743479, 0.0004625178024899486958, 0.0009250356049798973915 ),
 ( 0.000000000000000000, 1.000000000000000000 ),
 .UNSPECIFIED. ) 
 GEOMETRIC_REPRESENTATION_ITEM ( )  RATIONAL_B_SPLINE_SURFACE ( (
 ( 1.000000000000000000, 0.7071067811865475727, 1.000000000000000000),
 ( 1.000000000000000000, 0.6819975405126383894, 1.000000000000000000),
 ( 1.000000000000000000, 0.6638073299468163491, 1.000000000000000000),
 ( 1.000000000000000000, 0.6387680821201728865, 1.000000000000000000),
 ( 1.000000000000000000, 0.6313903660824350395, 1.000000000000000000),
 ( 1.000000000000000000, 0.6152524581541630733, 1.000000000000000000),
 ( 1.000000000000000000, 0.6128152994388438302, 1.000000000000000000),
 ( 1.000000000000000000, 0.6123724356957929160, 1.000000000000000000) ) ) 
 REPRESENTATION_ITEM ( '' )  SURFACE ( )  );
#6163=DIRECTION ( 'NONE',  ( 1.000000000000000000, 0.000000000000000000, 0.000000000000000000 ) ) ;
#6166=ORIENTED_EDGE ( 'NONE', *, *, #8127, .F. ) ;
#6167=EDGE_CURVE ( 'NONE', #19133, #6030, #7354, .T. ) ;
#6168=LINE ( 'NONE', #17884, #10631 ) ;
#6170=ADVANCED_FACE ( 'NONE', ( #10923 ), #1071, .T. ) ;
#6171=ADVANCED_FACE ( 'NONE', ( #6022 ), #840, .F. ) ;
#6172=VERTEX_POINT ( 'NONE', #19539 ) ;
#6179=MANIFOLD_SOLID_BREP ( 'Stock-MAS-696-1', #18843 ) ;
#6180=ORIENTED_EDGE ( 'NONE', *, *, #15811, .F. ) ;
#6181=CARTESIAN_POINT ( 'NONE',  ( -15.21174975910705207, -51.61873716947361856, 68.25000000000000000 ) ) ;
#6182=FACE_OUTER_BOUND ( 'NONE', #6749, .T. ) ;
#6184=LINE ( 'NONE', #12967, #12462 ) ;
#6190=SPHERICAL_SURFACE ( 'NONE', #14442, 0.5000000000000000000 ) ;
#6191=ADVANCED_FACE ( 'NONE', ( #1614 ), #21462, .T. ) ;
#6193=DIRECTION ( 'NONE',  ( 1.000000000000000000, 1.334402673828314029E-15, 0.000000000000000000 ) ) ;
#6195=ORIENTED_EDGE ( 'NONE', *, *, #6257, .T. ) ;
#6196=ORIENTED_EDGE ( 'NONE', *, *, #13195, .T. ) ;
#6197=CARTESIAN_POINT ( 'NONE',  ( -28.87540678000427619, 6.494748934539263274, 13.50000000000000000 ) ) ;
#6200=FACE_OUTER_BOUND ( 'NONE', #3569, .T. ) ;
#6203=LINE ( 'NONE', #10998, #1295 ) ;
#6204=ORIENTED_EDGE ( 'NONE', *, *, #22079, .T. ) ;
#6205=CARTESIAN_POINT ( 'NONE',  ( 17.92752199202934094, -38.74634676501045760, 13.79999999999999893 ) ) ;
#6212=LINE ( 'NONE', #16030, #8783 ) ;
#6214=ORIENTED_EDGE ( 'NONE', *, *, #10991, .F. ) ;
#6215=EDGE_LOOP ( 'NONE', ( #11220, #5859, #19189, #11602, #9138, #6750 ) ) ;
#6216=ORIENTED_EDGE ( 'NONE', *, *, #1223, .F. ) ;
#6217=CARTESIAN_POINT ( 'NONE',  ( 15.13073201445138949, 52.10286008774956201, 13.87500000000000178 ) ) ;
#6220=CARTESIAN_POINT ( 'NONE',  ( 25.37540678000427263, -67.24634676501045760, 13.50000000000000000 ) ) ;
#6223=CARTESIAN_POINT ( 'NONE',  ( -9.641460742840918030, 32.61873716947361856, 68.00000000000000000 ) ) ;
#6225=EDGE_CURVE ( 'NONE', #22131, #12877, #8134, .T. ) ;
#6226=DIRECTION ( 'NONE',  ( -1.000000000000000000, -0.000000000000000000, -0.000000000000000000 ) ) ;
#6230=ORIENTED_EDGE ( 'NONE', *, *, #14189, .F. ) ;
#6231=FACE_OUTER_BOUND ( 'NONE', #11768, .T. ) ;
#6232=CARTESIAN_POINT ( 'NONE',  ( -14.66174975910705136, 42.11054587065083155, 13.50000000000000000 ) ) ;
#6237=VERTEX_POINT ( 'NONE', #6679 ) ;
#6239=DIRECTION ( 'NONE',  ( 1.000000000000000000, 0.000000000000000000, 0.000000000000000000 ) ) ;
#6240=EDGE_CURVE ( 'NONE', #17330, #1152, #5590, .T. ) ;
#6241=EDGE_CURVE ( 'NONE', #3604, #2394, #20221, .T. ) ;
#6243=DIRECTION ( 'NONE',  ( 0.000000000000000000, -1.000000000000000000, 0.000000000000000000 ) ) ;
#6244=AXIS2_PLACEMENT_3D ( 'NONE', #13860, #7280, #5729 ) ;
#6246=CARTESIAN_POINT ( 'NONE',  ( 3.627054932750481964, 33.43424481021354921, 42.50000000000000000 ) ) ;
#6247=ORIENTED_EDGE ( 'NONE', *, *, #3989, .F. ) ;
#6249=VERTEX_POINT ( 'NONE', #6577 ) ;
#6250=LINE ( 'NONE', #11374, #17051 ) ;
#6252=EDGE_CURVE ( 'NONE', #11265, #1826, #14125, .T. ) ;
#6253=DIRECTION ( 'NONE',  ( 0.000000000000000000, 0.000000000000000000, 1.000000000000000000 ) ) ;
#6255=ORIENTED_EDGE ( 'NONE', *, *, #20528, .F. ) ;
#6257=EDGE_CURVE ( 'NONE', #1350, #18032, #13042, .T. ) ;
#6261=CIRCLE ( 'NONE', #16589, 1.000000000000000888 ) ;
#6264=CARTESIAN_POINT ( 'NONE',  ( 27.77120804565220169, -2.094189496455408861, 0.2999999999999947153 ) ) ;
#6265=CARTESIAN_POINT ( 'NONE',  ( 29.37540678000427619, -5.299999999999999822, 7.200000000000000178 ) ) ;
#6267=DIRECTION ( 'NONE',  ( -0.000000000000000000, -0.000000000000000000, -1.000000000000000000 ) ) ;
#6270=FACE_OUTER_BOUND ( 'NONE', #4623, .T. ) ;
#6273=CARTESIAN_POINT ( 'NONE',  ( 29.17540678000427690, 0.000000000000000000, 7.500000000000000000 ) ) ;
#6275=ORIENTED_EDGE ( 'NONE', *, *, #9102, .F. ) ;
#6278=AXIS2_PLACEMENT_3D ( 'NONE', #11062, #9389, #6163 ) ;
#6279=DIRECTION ( 'NONE',  ( 1.000000000000000000, 0.000000000000000000, 0.000000000000000000 ) ) ;
#6281=CARTESIAN_POINT ( 'NONE',  ( 0.000000000000000000, -51.61873716947361856, 68.50000000000000000 ) ) ;
#6285=CIRCLE ( 'NONE', #1980, 0.2999999999999999334 ) ;
#6286=CIRCLE ( 'NONE', #11977, 0.2500000000000002220 ) ;
#6287=CARTESIAN_POINT ( 'NONE',  ( -15.95292532278785913, -32.11873716947361856, 42.50000000000000711 ) ) ;
#6288=DIRECTION ( 'NONE',  ( 1.000000000000000000, 0.000000000000000000, 0.000000000000000000 ) ) ;
#6289=DIRECTION ( 'NONE',  ( -0.000000000000000000, -0.000000000000000000, -1.000000000000000000 ) ) ;
#6290=DIRECTION ( 'NONE',  ( -1.000000000000000000, 0.000000000000000000, 0.000000000000000000 ) ) ;
#6291=ADVANCED_FACE ( 'NONE', ( #20322 ), #6911, .T. ) ;
#6294=CARTESIAN_POINT ( 'NONE',  ( -29.13662752439705272, 0.000000000000000000, 7.500000000000000000 ) ) ;
#6299=DIRECTION ( 'NONE',  ( 0.000000000000000000, 1.000000000000000000, 0.000000000000000000 ) ) ;
#6304=VECTOR ( 'NONE', #5695, 1000.000000000000000 ) ;
#6305=VERTEX_POINT ( 'NONE', #16945 ) ;
#6306=ORIENTED_EDGE ( 'NONE', *, *, #16978, .F. ) ;
#6307=ORIENTED_EDGE ( 'NONE', *, *, #20945, .T. ) ;
#6309=CARTESIAN_POINT ( 'NONE',  ( -23.02398829872513986, 5.683640910026983128, 42.50000000000000000 ) ) ;
#6310=EDGE_CURVE ( 'NONE', #1165, #6037, #11474, .T. ) ;
#6312=DIRECTION ( 'NONE',  ( 1.000000000000000000, 0.000000000000000000, 0.000000000000000000 ) ) ;
#6313=AXIS2_PLACEMENT_3D ( 'NONE', #20148, #13645, #20489 ) ;
#6316=FACE_OUTER_BOUND ( 'NONE', #4553, .T. ) ;
#6317=CARTESIAN_POINT ( 'NONE',  ( 26.56227312273159313, -9.958410664601842655, 13.79999999999999893 ) ) ;
#6318=CARTESIAN_POINT ( 'NONE',  ( -23.04906723162513416, 2.296088124452694501, 13.26119099173120652 ) ) ;
#6319=CIRCLE ( 'NONE', #20956, 2.000000000000001776 ) ;
#6320=ORIENTED_EDGE ( 'NONE', *, *, #12933, .F. ) ;
#6321=LINE ( 'NONE', #11331, #1860 ) ;
#6322=ORIENTED_EDGE ( 'NONE', *, *, #20217, .T. ) ;
#6323=ORIENTED_EDGE ( 'NONE', *, *, #96, .F. ) ;
#6324=ORIENTED_EDGE ( 'NONE', *, *, #18554, .F. ) ;
#6325=CARTESIAN_POINT ( 'NONE',  ( 14.96174975910705918, 51.76873716947361714, 13.79999999999999716 ) ) ;
#6328=AXIS2_PLACEMENT_3D ( 'NONE', #2409, #828, #11024 ) ;
#6329=EDGE_CURVE ( 'NONE', #2605, #12981, #4851, .T. ) ;
#6333=VERTEX_POINT ( 'NONE', #267 ) ;
#6336=DIRECTION ( 'NONE',  ( -0.000000000000000000, 0.000000000000000000, 1.000000000000000000 ) ) ;
#6338=EDGE_CURVE ( 'NONE', #1535, #18691, #7121, .T. ) ;
#6339=CARTESIAN_POINT ( 'NONE',  ( 23.02398829872513986, -2.192334671524723166, 13.33121981694520564 ) ) ;
#6341=EDGE_LOOP ( 'NONE', ( #333, #8992, #9202, #19167 ) ) ;
#6349=VECTOR ( 'NONE', #20389, 1000.000000000000000 ) ;
#6350=DIRECTION ( 'NONE',  ( -0.000000000000000000, -0.000000000000000000, -1.000000000000000000 ) ) ;
#6351=DIRECTION ( 'NONE',  ( -0.000000000000000000, -0.000000000000000000, 1.000000000000000000 ) ) ;
#6354=DIRECTION ( 'NONE',  ( 0.000000000000000000, 1.000000000000000000, -0.000000000000000000 ) ) ;
#6356=LINE ( 'NONE', #3316, #17370 ) ;
#6357=ORIENTED_EDGE ( 'NONE', *, *, #12013, .F. ) ;
#6358=VERTEX_POINT ( 'NONE', #2276 ) ;
#6359=CIRCLE ( 'NONE', #8493, 0.5000000000000004441 ) ;
#6360=ORIENTED_EDGE ( 'NONE', *, *, #5117, .T. ) ;
#6361=CARTESIAN_POINT ( 'NONE',  ( 0.000000000000000000, -68.70000000000001705, 0.2999999999999947153 ) ) ;
#6366=CIRCLE ( 'NONE', #17774, 0.2999999999999999334 ) ;
#6367=DIRECTION ( 'NONE',  ( -0.000000000000000000, -0.000000000000000000, 1.000000000000000000 ) ) ;
#6368=AXIS2_PLACEMENT_3D ( 'NONE', #1987, #5492, #315 ) ;
#6371=DIRECTION ( 'NONE',  ( -1.000000000000000000, 0.000000000000000000, 0.000000000000000000 ) ) ;
#6372=LINE ( 'NONE', #19900, #17063 ) ;
#6373=EDGE_CURVE ( 'NONE', #12411, #12755, #11276, .T. ) ;
#6374=DIRECTION ( 'NONE',  ( 1.000000000000000000, 0.000000000000000000, 0.000000000000000000 ) ) ;
#6375=DIRECTION ( 'NONE',  ( -0.000000000000000000, -0.000000000000000000, -1.000000000000000000 ) ) ;
#6378=VERTEX_POINT ( 'NONE', #1940 ) ;
#6379=AXIS2_PLACEMENT_3D ( 'NONE', #2181, #13809, #17285 ) ;
#6381=CARTESIAN_POINT ( 'NONE',  ( 25.37540678000427263, -69.04634676501045476, 3.799999999999999822 ) ) ;
#6383=VERTEX_POINT ( 'NONE', #3535 ) ;
#6385=VECTOR ( 'NONE', #19758, 1000.000000000000000 ) ;
#6386=VECTOR ( 'NONE', #309, 1000.000000000000000 ) ;
#6387=ORIENTED_EDGE ( 'NONE', *, *, #8772, .F. ) ;
#6388=DIRECTION ( 'NONE',  ( 1.000000000000000000, 0.000000000000000000, 0.000000000000000000 ) ) ;
#6390=DIRECTION ( 'NONE',  ( 0.000000000000000000, 0.000000000000000000, 1.000000000000000000 ) ) ;
#6391=VERTEX_POINT ( 'NONE', #10366 ) ;
#6393=EDGE_LOOP ( 'NONE', ( #10033, #4414, #14064, #242 ) ) ;
#6394=AXIS2_PLACEMENT_3D ( 'NONE', #15112, #1462, #6537 ) ;
#6395=CARTESIAN_POINT ( 'NONE',  ( 3.127054932750481964, 32.11873716947361856, 109.6002446535588319 ) ) ;
#6396=VECTOR ( 'NONE', #13935, 1000.000000000000000 ) ;
#6397=VERTEX_POINT ( 'NONE', #12012 ) ;
#6398=EDGE_CURVE ( 'NONE', #14518, #1148, #12125, .T. ) ;
#6401=DIRECTION ( 'NONE',  ( 1.000000000000000000, 0.000000000000000000, 0.000000000000000000 ) ) ;
#6402=EDGE_CURVE ( 'NONE', #5867, #9603, #13693, .T. ) ;
#6405=DIRECTION ( 'NONE',  ( 0.000000000000000000, 0.000000000000000000, 1.000000000000000000 ) ) ;
#6406=LINE ( 'NONE', #13310, #17026 ) ;
#6408=AXIS2_PLACEMENT_3D ( 'NONE', #10228, #14916, #16706 ) ;
#6411=VECTOR ( 'NONE', #16437, 1000.000000000000000 ) ;
#6414=CARTESIAN_POINT ( 'NONE',  ( 28.87540678000427619, -6.494748934539263274, 7.799999999999999822 ) ) ;
#6418=CIRCLE ( 'NONE', #18914, 0.5000000000000004441 ) ;
#6419=CIRCLE ( 'NONE', #10678, 1.999999999999991340 ) ;
#6421=ORIENTED_EDGE ( 'NONE', *, *, #169, .T. ) ;
#6422=ORIENTED_EDGE ( 'NONE', *, *, #1699, .T. ) ;
#6424=EDGE_CURVE ( 'NONE', #4947, #6383, #5932, .T. ) ;
#6426=AXIS2_PLACEMENT_3D ( 'NONE', #20101, #1393, #13145 ) ;
#6431=EDGE_LOOP ( 'NONE', ( #20275, #7268, #6387, #3957 ) ) ;
#6432=EDGE_CURVE ( 'NONE', #6397, #8329, #19147, .T. ) ;
#6433=CARTESIAN_POINT ( 'NONE',  ( 15.04770344846787822, -51.92604205163220854, 13.50000000000000000 ) ) ;
#6434=CARTESIAN_POINT ( 'NONE',  ( -25.37540678000427263, -63.74634676501045050, 13.50000000000000000 ) ) ;
#6436=CARTESIAN_POINT ( 'NONE',  ( 29.13662752439705272, 0.000000000000000000, 7.500000000000000000 ) ) ;
#6437=DIRECTION ( 'NONE',  ( 1.000000000000000000, 0.000000000000000000, 0.000000000000000000 ) ) ;
#6438=CIRCLE ( 'NONE', #2844, 0.2999999999999999334 ) ;
#6440=CARTESIAN_POINT ( 'NONE',  ( -28.87540678000427619, 6.494748934539263274, 7.799999999999999822 ) ) ;
#6443=ORIENTED_EDGE ( 'NONE', *, *, #1158, .T. ) ;
#6444=VERTEX_POINT ( 'NONE', #20657 ) ;
#6445=DIRECTION ( 'NONE',  ( -1.000000000000000000, 0.000000000000000000, 0.000000000000000000 ) ) ;
#6446=CARTESIAN_POINT ( 'NONE',  ( -29.50000000000002132, -2.473451120191013430, 0.2999999999999947153 ) ) ;
#6447=EDGE_CURVE ( 'NONE', #8429, #2851, #3644, .T. ) ;
#6448=EDGE_LOOP ( 'NONE', ( #3043, #16856, #17133, #2064 ) ) ;
#6450=FACE_OUTER_BOUND ( 'NONE', #15903, .T. ) ;
#6452=CIRCLE ( 'NONE', #11441, 4.051418481279135619 ) ;
#6453=CIRCLE ( 'NONE', #15694, 0.2999999999999999334 ) ;
#6456=CARTESIAN_POINT ( 'NONE',  ( -29.13662752439705272, 0.000000000000000000, 0.3000000000000016542 ) ) ;
#6461=FACE_OUTER_BOUND ( 'NONE', #8348, .T. ) ;
#6466=EDGE_CURVE ( 'NONE', #19513, #18311, #15909, .T. ) ;
#6469=CARTESIAN_POINT ( 'NONE',  ( 31.50000000000002132, 71.70000000000001705, 1.800000000000000044 ) ) ;
#6470=VECTOR ( 'NONE', #4264, 1000.000000000000000 ) ;
#6471=ORIENTED_EDGE ( 'NONE', *, *, #10260, .F. ) ;
#6473=DIRECTION ( 'NONE',  ( 0.000000000000000000, 1.000000000000000000, 0.000000000000000000 ) ) ;
#6474=CARTESIAN_POINT ( 'NONE',  ( 25.37540678000426908, 38.74634676501045760, 13.79999999999999893 ) ) ;
#6475=ORIENTED_EDGE ( 'NONE', *, *, #9918, .F. ) ;
#6478=CARTESIAN_POINT ( 'NONE',  ( 15.21174975910705918, -52.39333383871510108, 13.50000000000000000 ) ) ;
#6485=CIRCLE ( 'NONE', #1814, 0.6999999999999992895 ) ;
#6487=CARTESIAN_POINT ( 'NONE',  ( -23.02398829872513986, -2.928742984578568187, 13.54178985689086190 ) ) ;
#6489=CARTESIAN_POINT ( 'NONE',  ( 14.96174975910707161, 51.86873716947361856, 68.00000000000000000 ) ) ;
#6490=CARTESIAN_POINT ( 'NONE',  ( 0.000000000000000000, -69.00000000000000000, -150.0833101980363722 ) ) ;
#6496=ORIENTED_EDGE ( 'NONE', *, *, #19073, .T. ) ;
#6497=CARTESIAN_POINT ( 'NONE',  ( 30.37540678000427619, -6.000000000000000000, 3.799999999999999822 ) ) ;
#6499=CARTESIAN_POINT ( 'NONE',  ( 3.627054932750481964, -33.43424481021354921, 42.50000000000000000 ) ) ;
#6500=EDGE_LOOP ( 'NONE', ( #145, #5913, #3762, #12595, #20800, #5189, #21042, #17465 ) ) ;
#6501=FACE_OUTER_BOUND ( 'NONE', #20109, .T. ) ;
#6503=CIRCLE ( 'NONE', #21844, 0.2999999999999999334 ) ;
#6505=EDGE_CURVE ( 'NONE', #18602, #421, #19624, .T. ) ;
#6511=FACE_OUTER_BOUND ( 'NONE', #18694, .T. ) ;
#6512=VERTEX_POINT ( 'NONE', #4074 ) ;
#6513=FACE_OUTER_BOUND ( 'NONE', #12409, .T. ) ;
#6515=CARTESIAN_POINT ( 'NONE',  ( 29.13662752439705272, 5.299999999999999822, 7.200000000000000178 ) ) ;
#6518=CARTESIAN_POINT ( 'NONE',  ( 23.14059574490499571, 2.755557770589327049, 13.42404417222474322 ) ) ;
#6519=DIRECTION ( 'NONE',  ( -0.9823853469773031755, 0.1868663427273193067, 0.000000000000000000 ) ) ;
#6522=CARTESIAN_POINT ( 'NONE',  ( 29.17540678000427690, -63.74634676501045050, 7.799999999999999822 ) ) ;
#6527=FACE_OUTER_BOUND ( 'NONE', #20357, .T. ) ;
#6529=CARTESIAN_POINT ( 'NONE',  ( 29.50000000000002132, 2.512390033608338236, 1.500000000000000000 ) ) ;
#6533=DIRECTION ( 'NONE',  ( 1.000000000000000000, 0.000000000000000000, 0.000000000000000000 ) ) ;
#6534=EDGE_LOOP ( 'NONE', ( #1075, #14313, #7056, #11538 ) ) ;
#6537=DIRECTION ( 'NONE',  ( 1.000000000000000000, 0.000000000000000000, 0.000000000000000000 ) ) ;
#6539=ORIENTED_EDGE ( 'NONE', *, *, #13137, .F. ) ;
#6545=EDGE_CURVE ( 'NONE', #252, #9928, #9854, .T. ) ;
#6546=DIRECTION ( 'NONE',  ( 0.000000000000000000, 0.000000000000000000, -1.000000000000000000 ) ) ;
#6548=FACE_OUTER_BOUND ( 'NONE', #1600, .T. ) ;
#6551=CARTESIAN_POINT ( 'NONE',  ( -23.20982120895258660, 3.064530420494592899, 13.47289532992770589 ) ) ;
#6553=AXIS2_PLACEMENT_3D ( 'NONE', #19381, #17586, #13887 ) ;
#6554=CARTESIAN_POINT ( 'NONE',  ( -25.37540678000427263, -68.44634676501046044, 7.500000000000000000 ) ) ;
#6555=EDGE_CURVE ( 'NONE', #4383, #10528, #21100, .T. ) ;
#6557=ORIENTED_EDGE ( 'NONE', *, *, #16470, .F. ) ;
#6558=ORIENTED_EDGE ( 'NONE', *, *, #17962, .T. ) ;
#6559=FACE_OUTER_BOUND ( 'NONE', #2459, .T. ) ;
#6562=ORIENTED_EDGE ( 'NONE', *, *, #4846, .F. ) ;
#6563=DIRECTION ( 'NONE',  ( 1.000000000000000000, 0.000000000000000000, 0.000000000000000000 ) ) ;
#6564=VERTEX_POINT ( 'NONE', #5774 ) ;
#6565=DIRECTION ( 'NONE',  ( 1.000000000000000000, 0.000000000000000000, 0.000000000000000000 ) ) ;
#6567=CYLINDRICAL_SURFACE ( 'NONE', #16351, 0.5000000000000000000 ) ;
#6568=DIRECTION ( 'NONE',  ( 0.000000000000000000, -1.000000000000000000, 0.000000000000000000 ) ) ;
#6570=CYLINDRICAL_SURFACE ( 'NONE', #15232, 4.351418481279133665 ) ;
#6571=LINE ( 'NONE', #13362, #3911 ) ;
#6572=EDGE_CURVE ( 'NONE', #4630, #15132, #7316, .T. ) ;
#6573=ADVANCED_FACE ( 'NONE', ( #21207 ), #2501, .F. ) ;
#6574=FACE_OUTER_BOUND ( 'NONE', #18878, .T. ) ;
#6575=DIRECTION ( 'NONE',  ( -3.052134192567367925E-16, -1.000000000000000000, 0.000000000000000000 ) ) ;
#6576=VERTEX_POINT ( 'NONE', #12656 ) ;
#6577=CARTESIAN_POINT ( 'NONE',  ( -3.127054932750481964, -32.11873716947361856, 68.00000000000000000 ) ) ;
#6580=DIRECTION ( 'NONE',  ( 1.000000000000000000, 0.000000000000000000, 0.000000000000000000 ) ) ;
#6582=ORIENTED_EDGE ( 'NONE', *, *, #18700, .T. ) ;
#6585=DIRECTION ( 'NONE',  ( 1.000000000000000000, 0.000000000000000000, 0.000000000000000000 ) ) ;
#6588=DIRECTION ( 'NONE',  ( 0.000000000000000000, -0.000000000000000000, -1.000000000000000000 ) ) ;
#6589=ORIENTED_EDGE ( 'NONE', *, *, #5363, .F. ) ;
#6590=ORIENTED_EDGE ( 'NONE', *, *, #12969, .F. ) ;
#6592=TOROIDAL_SURFACE ( 'NONE', #19079, 2.299999999999993161, 0.2999999999999999889 ) ;
#6593=CARTESIAN_POINT ( 'NONE',  ( 29.50000000000002132, -2.473451120191013430, -150.0833101980363722 ) ) ;
#6594=CARTESIAN_POINT ( 'NONE',  ( -27.67540678000428400, -10.94079601157914716, 13.79999999999999893 ) ) ;
#6596=DIRECTION ( 'NONE',  ( -0.000000000000000000, 1.000000000000000000, -0.000000000000000000 ) ) ;
#6601=CARTESIAN_POINT ( 'NONE',  ( -25.37540678000429040, -36.74634676501047181, 42.50000000000000000 ) ) ;
#6604=EDGE_CURVE ( 'NONE', #20393, #14744, #13993, .T. ) ;
#6605=DIRECTION ( 'NONE',  ( 0.000000000000000000, 0.000000000000000000, -1.000000000000000000 ) ) ;
#6606=EDGE_LOOP ( 'NONE', ( #18193, #507, #22052, #15089 ) ) ;
#6607=DIRECTION ( 'NONE',  ( 0.000000000000000000, 0.000000000000000000, 1.000000000000000000 ) ) ;
#6610=ORIENTED_EDGE ( 'NONE', *, *, #4453, .F. ) ;
#6611=DIRECTION ( 'NONE',  ( 1.000000000000000000, 0.000000000000000000, 0.000000000000000000 ) ) ;
#6612=EDGE_CURVE ( 'NONE', #21055, #104, #8672, .T. ) ;
#6614=CARTESIAN_POINT ( 'NONE',  ( -25.37540678000427263, 68.44634676501046044, 7.500000000000000000 ) ) ;
#6616=ADVANCED_FACE ( 'NONE', ( #3287 ), #2954, .F. ) ;
#6617=DIRECTION ( 'NONE',  ( 1.000000000000000000, 0.000000000000000000, 0.000000000000000000 ) ) ;
#6618=EDGE_CURVE ( 'NONE', #13600, #3729, #22094, .T. ) ;
#6620=DIRECTION ( 'NONE',  ( 1.000000000000000000, -0.000000000000000000, 0.000000000000000000 ) ) ;
#6621=CARTESIAN_POINT ( 'NONE',  ( -26.61833302554978786, 9.663695060508649348, 13.79999999999999893 ) ) ;
#6623=CARTESIAN_POINT ( 'NONE',  ( -15.06704456860866870, -51.94509779313090547, 13.50000000000000000 ) ) ;
#6624=DIRECTION ( 'NONE',  ( 0.000000000000000000, 1.000000000000000000, 0.000000000000000000 ) ) ;
#6626=TOROIDAL_SURFACE ( 'NONE', #13390, 0.7000000000000000666, 0.2999999999999999889 ) ;
#6628=CYLINDRICAL_SURFACE ( 'NONE', #7759, 0.5000000000000004441 ) ;
#6633=DIRECTION ( 'NONE',  ( 1.000000000000000000, 0.000000000000000000, 0.000000000000000000 ) ) ;
#6634=ADVANCED_FACE ( 'NONE', ( #4747 ), #21648, .T. ) ;
#6635=VERTEX_POINT ( 'NONE', #4635 ) ;
#6638=TOROIDAL_SURFACE ( 'NONE', #12676, 1.000000000000000000, 0.5000000000000000000 ) ;
#6639=ORIENTED_EDGE ( 'NONE', *, *, #21873, .T. ) ;
#6640=ADVANCED_FACE ( 'NONE', ( #14907 ), #3433, .F. ) ;
#6641=ADVANCED_FACE ( 'NONE', ( #18490 ), #13571, .F. ) ;
#6642=LINE ( 'NONE', #15348, #10581 ) ;
#6643=CARTESIAN_POINT ( 'NONE',  ( -29.50000000000002132, -69.00000000000000000, 1.500000000000000000 ) ) ;
#6648=ADVANCED_FACE ( 'NONE', ( #18606 ), #15128, .T. ) ;
#6649=CARTESIAN_POINT ( 'NONE',  ( -15.95292532278785913, -50.11873716947361856, 68.00000000000000000 ) ) ;
#6650=DIRECTION ( 'NONE',  ( 0.000000000000000000, 0.000000000000000000, 1.000000000000000000 ) ) ;
#6651=DIRECTION ( 'NONE',  ( 1.000000000000000000, 0.000000000000000000, 0.000000000000000000 ) ) ;
#6652=AXIS2_PLACEMENT_3D ( 'NONE', #18224, #2664, #11395 ) ;
#6653=DIRECTION ( 'NONE',  ( 1.000000000000000000, 0.000000000000000000, 0.000000000000000000 ) ) ;
#6655=ORIENTED_EDGE ( 'NONE', *, *, #18939, .T. ) ;
#6656=VECTOR ( 'NONE', #8782, 1000.000000000000000 ) ;
#6657=AXIS2_PLACEMENT_3D ( 'NONE', #1638, #3440, #17296 ) ;
#6660=LINE ( 'NONE', #41, #6759 ) ;
#6661=EDGE_CURVE ( 'NONE', #19805, #13239, #6261, .T. ) ;
#6662=CARTESIAN_POINT ( 'NONE',  ( 15.13073201445139127, -52.10286008774955491, 13.87500000000000000 ) ) ;
#6664=DIRECTION ( 'NONE',  ( 0.000000000000000000, 0.000000000000000000, -1.000000000000000000 ) ) ;
#6666=FACE_OUTER_BOUND ( 'NONE', #15816, .T. ) ;
#6669=VECTOR ( 'NONE', #1116, 1000.000000000000000 ) ;
#6670=DIRECTION ( 'NONE',  ( 0.000000000000000000, 0.000000000000000000, 1.000000000000000000 ) ) ;
#6671=VECTOR ( 'NONE', #14240, 1000.000000000000000 ) ;
#6672=ORIENTED_EDGE ( 'NONE', *, *, #2764, .T. ) ;
#6673=LINE ( 'NONE', #10360, #9173 ) ;
#6674=EDGE_CURVE ( 'NONE', #21627, #20211, #12299, .T. ) ;
#6675=CARTESIAN_POINT ( 'NONE',  ( -27.37540678000427619, 10.94079601157914539, 42.50000000000000000 ) ) ;
#6676=CARTESIAN_POINT ( 'NONE',  ( -25.37540678000426908, 39.04634676501046187, 13.50000000000000000 ) ) ;
#6679=CARTESIAN_POINT ( 'NONE',  ( 14.66174975910705847, 42.11054587065083155, 13.50000000000000000 ) ) ;
#6681=DIRECTION ( 'NONE',  ( 0.000000000000000000, 0.000000000000000000, -1.000000000000000000 ) ) ;
#6682=DIRECTION ( 'NONE',  ( 0.000000000000000000, -0.000000000000000000, 1.000000000000000000 ) ) ;
#6683=AXIS2_PLACEMENT_3D ( 'NONE', #4416, #2862, #21449 ) ;
#6686=ORIENTED_EDGE ( 'NONE', *, *, #19934, .F. ) ;
#6689=CYLINDRICAL_SURFACE ( 'NONE', #18849, 6.500000000000002665 ) ;
#6691=ORIENTED_EDGE ( 'NONE', *, *, #5367, .T. ) ;
#6692=CARTESIAN_POINT ( 'NONE',  ( 17.45292532278785913, 0.000000000000000000, 68.00000000000000000 ) ) ;
#6694=VERTEX_POINT ( 'NONE', #1372 ) ;
#6695=EDGE_CURVE ( 'NONE', #17212, #6786, #20187, .T. ) ;
#6696=ORIENTED_EDGE ( 'NONE', *, *, #17486, .F. ) ;
#6700=AXIS2_PLACEMENT_3D ( 'NONE', #7547, #10554, #17373 ) ;
#6703=TOROIDAL_SURFACE ( 'NONE', #5995, 5.299999999999999822, 0.2999999999999999889 ) ;
#6704=AXIS2_PLACEMENT_3D ( 'NONE', #5221, #18981, #7231 ) ;
#6705=PLANE ( 'NONE',  #15354 ) ;
#6707=ORIENTED_EDGE ( 'NONE', *, *, #3244, .F. ) ;
#6708=DIRECTION ( 'NONE',  ( -0.000000000000000000, -0.000000000000000000, -1.000000000000000000 ) ) ;
#6709=ADVANCED_FACE ( 'NONE', ( #4844 ), #4966, .T. ) ;
#6710=DIRECTION ( 'NONE',  ( 0.000000000000000000, 0.000000000000000000, 1.000000000000000000 ) ) ;
#6712=DIRECTION ( 'NONE',  ( 1.000000000000000000, 0.000000000000000000, 0.000000000000000000 ) ) ;
#6713=ORIENTED_EDGE ( 'NONE', *, *, #15873, .F. ) ;
#6720=ORIENTED_EDGE ( 'NONE', *, *, #6373, .T. ) ;
#6721=AXIS2_PLACEMENT_3D ( 'NONE', #13044, #16419, #11260 ) ;
#6723=ORIENTED_EDGE ( 'NONE', *, *, #3826, .F. ) ;
#6724=DIRECTION ( 'NONE',  ( -1.000000000000000000, 0.000000000000000000, 0.000000000000000000 ) ) ;
#6725=ADVANCED_FACE ( 'NONE', ( #3618 ), #6626, .T. ) ;
#6727=ORIENTED_EDGE ( 'NONE', *, *, #22143, .F. ) ;
#6731=CARTESIAN_POINT ( 'NONE',  ( -29.13662752439705272, 0.000000000000000000, 0.000000000000000000 ) ) ;
#6732=VERTEX_POINT ( 'NONE', #134 ) ;
#6736=CARTESIAN_POINT ( 'NONE',  ( -29.37540678000427619, -4.700000000000000178, 3.799999999999999822 ) ) ;
#6738=DIRECTION ( 'NONE',  ( 0.000000000000000000, 0.000000000000000000, -1.000000000000000000 ) ) ;
#6739=DIRECTION ( 'NONE',  ( 1.000000000000000000, 0.000000000000000000, 0.000000000000000000 ) ) ;
#6740=DIRECTION ( 'NONE',  ( 0.000000000000000000, 1.000000000000000000, -0.000000000000000000 ) ) ;
#6741=VECTOR ( 'NONE', #12067, 1000.000000000000000 ) ;
#6743=DIRECTION ( 'NONE',  ( 0.000000000000000000, 0.000000000000000000, 1.000000000000000000 ) ) ;
#6744=EDGE_CURVE ( 'NONE', #9810, #17039, #16929, .T. ) ;
#6746=DIRECTION ( 'NONE',  ( -1.000000000000000000, 0.000000000000000000, -0.000000000000000000 ) ) ;
#6749=EDGE_LOOP ( 'NONE', ( #5194, #11860, #12985, #10717 ) ) ;
#6750=ORIENTED_EDGE ( 'NONE', *, *, #7184, .F. ) ;
#6751=DIRECTION ( 'NONE',  ( -1.000000000000000000, 0.000000000000000000, 0.000000000000000000 ) ) ;
#6755=AXIS2_PLACEMENT_3D ( 'NONE', #14346, #19493, #7434 ) ;
#6756=TOROIDAL_SURFACE ( 'NONE', #12779, 1.300000000000000044, 0.2999999999999999889 ) ;
#6757=EDGE_LOOP ( 'NONE', ( #19651, #1391, #10195, #11154 ) ) ;
#6759=VECTOR ( 'NONE', #1595, 1000.000000000000000 ) ;
#6762=AXIS2_PLACEMENT_3D ( 'NONE', #1317, #21824, #20477 ) ;
#6764=CARTESIAN_POINT ( 'NONE',  ( -25.37540678000427263, 68.74634676501045760, 3.799999999999999822 ) ) ;
#6769=DIRECTION ( 'NONE',  ( 1.000000000000000000, 0.000000000000000000, 0.000000000000000000 ) ) ;
#6770=DIRECTION ( 'NONE',  ( -1.000000000000000000, 0.000000000000000000, 0.000000000000000000 ) ) ;
#6772=CARTESIAN_POINT ( 'NONE',  ( -23.04392555272740850, 2.268071869891183034, 13.22877247997976013 ) ) ;
#6773=CARTESIAN_POINT ( 'NONE',  ( 29.17540678000427690, 6.499884319688664647, 7.500000000000000000 ) ) ;
#6775=ORIENTED_EDGE ( 'NONE', *, *, #17405, .T. ) ;
#6776=ORIENTED_EDGE ( 'NONE', *, *, #6102, .T. ) ;
#6777=ORIENTED_EDGE ( 'NONE', *, *, #247, .F. ) ;
#6780=CIRCLE ( 'NONE', #7137, 0.2500000000000002220 ) ;
#6781=PLANE ( 'NONE',  #6408 ) ;
#6783=ORIENTED_EDGE ( 'NONE', *, *, #13703, .F. ) ;
#6785=CARTESIAN_POINT ( 'NONE',  ( 14.96174975910705918, -51.76873716947361714, 13.79999999999999716 ) ) ;
#6786=VERTEX_POINT ( 'NONE', #12104 ) ;
#6787=CARTESIAN_POINT ( 'NONE',  ( 9.141460742840918030, 33.43424481021354921, 7.321391277662001151 ) ) ;
#6788=CARTESIAN_POINT ( 'NONE',  ( 9.641460742840918030, -32.61873716947361856, 109.6002446535588319 ) ) ;
#6790=CIRCLE ( 'NONE', #18207, 0.2999999999999999334 ) ;
#6792=ORIENTED_EDGE ( 'NONE', *, *, #17545, .F. ) ;
#6793=DIRECTION ( 'NONE',  ( 0.000000000000000000, -1.000000000000000000, 0.000000000000000000 ) ) ;
#6794=CARTESIAN_POINT ( 'NONE',  ( 9.141460742840918030, -33.43424481021354921, 7.321391277662001151 ) ) ;
#6796=DIRECTION ( 'NONE',  ( 0.000000000000000000, 0.000000000000000000, 1.000000000000000000 ) ) ;
#6798=DIRECTION ( 'NONE',  ( 1.000000000000000000, 0.000000000000000000, 0.000000000000000000 ) ) ;
#6804=CARTESIAN_POINT ( 'NONE',  ( 3.127054932750481964, 32.61873716947361856, 68.00000000000000000 ) ) ;
#6806=ORIENTED_EDGE ( 'NONE', *, *, #7051, .F. ) ;
#6807=CIRCLE ( 'NONE', #20370, 0.2999999999999999334 ) ;
#6809=VERTEX_POINT ( 'NONE', #17251 ) ;
#6810=FACE_OUTER_BOUND ( 'NONE', #16901, .T. ) ;
#6811=EDGE_CURVE ( 'NONE', #22008, #19359, #1920, .T. ) ;
#6812=CARTESIAN_POINT ( 'NONE',  ( -30.37540678000427619, 6.000000000000000000, 3.799999999999999822 ) ) ;
#6814=AXIS2_PLACEMENT_3D ( 'NONE', #17079, #14951, #18876 ) ;
#6816=EDGE_LOOP ( 'NONE', ( #22144, #21213, #11399, #5402 ) ) ;
#6820=CARTESIAN_POINT ( 'NONE',  ( -9.141460742840918030, -32.11873716947361856, 68.00000000000000000 ) ) ;
#6821=ORIENTED_EDGE ( 'NONE', *, *, #16684, .F. ) ;
#6824=CARTESIAN_POINT ( 'NONE',  ( -31.50000000000002132, 71.00000000000001421, 1.500000000000000000 ) ) ;
#6826=ORIENTED_EDGE ( 'NONE', *, *, #14305, .F. ) ;
#6828=DIRECTION ( 'NONE',  ( 0.000000000000000000, 1.000000000000000000, -0.000000000000000000 ) ) ;
#6831=CARTESIAN_POINT ( 'NONE',  ( -23.02398829872513986, 2.157133568460765538, 7.500000000000000000 ) ) ;
#6833=EDGE_LOOP ( 'NONE', ( #19841, #11422, #5883, #5486 ) ) ;
#6836=ADVANCED_FACE ( 'NONE', ( #21404 ), #6190, .T. ) ;
#6838=DIRECTION ( 'NONE',  ( -0.000000000000000000, -0.000000000000000000, 1.000000000000000000 ) ) ;
#6844=VECTOR ( 'NONE', #5954, 1000.000000000000000 ) ;
#6846=CARTESIAN_POINT ( 'NONE',  ( 32.50000000000002132, -71.00000000000001421, 3.200000000000000178 ) ) ;
#6847=ORIENTED_EDGE ( 'NONE', *, *, #3348, .F. ) ;
#6853=CARTESIAN_POINT ( 'NONE',  ( 8.641460742840918030, 32.93424481021354921, 7.321391277662001151 ) ) ;
#6855=CIRCLE ( 'NONE', #20768, 1.299999999999999156 ) ;
#6856=DIRECTION ( 'NONE',  ( 0.000000000000000000, -1.000000000000000000, 0.000000000000000000 ) ) ;
#6857=ADVANCED_FACE ( 'NONE', ( #795 ), #10770, .F. ) ;
#6858=CARTESIAN_POINT ( 'NONE',  ( -15.21174975910705029, -52.10286008774955491, 13.87500000000000000 ) ) ;
#6860=ORIENTED_EDGE ( 'NONE', *, *, #18942, .T. ) ;
#6861=FACE_OUTER_BOUND ( 'NONE', #2614, .T. ) ;
#6867=AXIS2_PLACEMENT_3D ( 'NONE', #9701, #18065, #11361 ) ;
#6868=ORIENTED_EDGE ( 'NONE', *, *, #2706, .T. ) ;
#6870=EDGE_LOOP ( 'NONE', ( #9845, #21861, #10315, #10962 ) ) ;
#6871=EDGE_CURVE ( 'NONE', #5089, #2540, #8399, .T. ) ;
#6876=FACE_OUTER_BOUND ( 'NONE', #2957, .T. ) ;
#6878=EDGE_CURVE ( 'NONE', #5446, #5867, #10871, .T. ) ;
#6879=AXIS2_PLACEMENT_3D ( 'NONE', #12777, #14574, #2609 ) ;
#6881=AXIS2_PLACEMENT_3D ( 'NONE', #7059, #5268, #17122 ) ;
#6882=FACE_OUTER_BOUND ( 'NONE', #12193, .T. ) ;
#6883=( BOUNDED_CURVE ( )  B_SPLINE_CURVE ( 3, ( #16488, #21216, #14364, #14588 ),
 .UNSPECIFIED., .F., .T. ) 
 B_SPLINE_CURVE_WITH_KNOTS ( ( 4, 4 ),
 ( 4.712388980384689674, 6.283185307179586232 ),
 .UNSPECIFIED. ) 
 CURVE ( )  GEOMETRIC_REPRESENTATION_ITEM ( )  RATIONAL_B_SPLINE_CURVE ( ( 1.000000000000000000, 0.8047378541243649375, 0.8047378541243649375, 1.000000000000000000 ) ) 
 REPRESENTATION_ITEM ( '' )  );
#6884=EDGE_CURVE ( 'NONE', #15579, #13135, #2690, .T. ) ;
#6885=DIRECTION ( 'NONE',  ( 0.000000000000000000, 0.000000000000000000, -1.000000000000000000 ) ) ;
#6886=FACE_OUTER_BOUND ( 'NONE', #20772, .T. ) ;
#6887=ORIENTED_EDGE ( 'NONE', *, *, #12213, .F. ) ;
#6890=ORIENTED_EDGE ( 'NONE', *, *, #5831, .T. ) ;
#6894=DIRECTION ( 'NONE',  ( -0.000000000000000000, 0.000000000000000000, 1.000000000000000000 ) ) ;
#6895=ORIENTED_EDGE ( 'NONE', *, *, #8561, .F. ) ;
#6898=CIRCLE ( 'NONE', #12924, 0.5000000000000004441 ) ;
#6904=FACE_OUTER_BOUND ( 'NONE', #4345, .T. ) ;
#6905=CARTESIAN_POINT ( 'NONE',  ( 29.50000000000002132, 69.00000000000000000, 0.2999999999999947153 ) ) ;
#6907=DIRECTION ( 'NONE',  ( 1.000000000000000000, 0.000000000000000000, 0.000000000000000000 ) ) ;
#6910=ORIENTED_EDGE ( 'NONE', *, *, #4734, .T. ) ;
#6911=CYLINDRICAL_SURFACE ( 'NONE', #17342, 0.2999999999999999334 ) ;
#6915=CYLINDRICAL_SURFACE ( 'NONE', #887, 0.5000000000000004441 ) ;
#6916=CARTESIAN_POINT ( 'NONE',  ( 29.20000000000002061, -68.70000000000001705, 0.000000000000000000 ) ) ;
#6918=ORIENTED_EDGE ( 'NONE', *, *, #401, .T. ) ;
#6920=DIRECTION ( 'NONE',  ( 0.000000000000000000, 1.000000000000000000, 0.000000000000000000 ) ) ;
#6922=LINE ( 'NONE', #1406, #20025 ) ;
#6923=DIRECTION ( 'NONE',  ( 0.000000000000000000, 0.000000000000000000, 1.000000000000000000 ) ) ;
#6924=EDGE_CURVE ( 'NONE', #13253, #15404, #162, .T. ) ;
#6927=ORIENTED_EDGE ( 'NONE', *, *, #1494, .F. ) ;
#6928=CARTESIAN_POINT ( 'NONE',  ( -30.07540678000427548, 6.000000000000000000, 7.500000000000000000 ) ) ;
#6932=ORIENTED_EDGE ( 'NONE', *, *, #15370, .F. ) ;
#6933=CARTESIAN_POINT ( 'NONE',  ( 15.95292532278785913, 52.11873716947361856, 68.00000000000000000 ) ) ;
#6935=EDGE_CURVE ( 'NONE', #1047, #2833, #7685, .T. ) ;
#6936=EDGE_CURVE ( 'NONE', #21686, #4773, #21519, .T. ) ;
#6940=ORIENTED_EDGE ( 'NONE', *, *, #13166, .F. ) ;
#6945=CARTESIAN_POINT ( 'NONE',  ( 0.000000000000000000, -39.04634676501046187, 13.50000000000000000 ) ) ;
#6951=ORIENTED_EDGE ( 'NONE', *, *, #21583, .T. ) ;
#6956=EDGE_CURVE ( 'NONE', #18789, #8135, #9648, .T. ) ;
#6957=FACE_OUTER_BOUND ( 'NONE', #11930, .T. ) ;
#6960=CARTESIAN_POINT ( 'NONE',  ( 3.627054932750481964, -33.43424481021354921, 7.321391277662001151 ) ) ;
#6961=CARTESIAN_POINT ( 'NONE',  ( -28.57540678000427548, -6.776800961815481195, 13.50000000000000000 ) ) ;
#6962=ORIENTED_EDGE ( 'NONE', *, *, #3922, .T. ) ;
#6963=CARTESIAN_POINT ( 'NONE',  ( 29.17540678000427690, -6.499884319688664647, 7.500000000000000000 ) ) ;
#6966=CARTESIAN_POINT ( 'NONE',  ( -9.641460742840918030, -32.61873716947361856, 68.00000000000000000 ) ) ;
#6972=( NAMED_UNIT ( * ) SI_UNIT ( $, .STERADIAN. ) SOLID_ANGLE_UNIT ( ) );
#6975=ORIENTED_EDGE ( 'NONE', *, *, #8325, .T. ) ;
#6976=EDGE_CURVE ( 'NONE', #15626, #961, #12662, .T. ) ;
#6978=DIRECTION ( 'NONE',  ( 0.000000000000000000, 0.000000000000000000, 1.000000000000000000 ) ) ;
#6980=LINE ( 'NONE', #28, #20695 ) ;
#6981=AXIS2_PLACEMENT_3D ( 'NONE', #4053, #18016, #11089 ) ;
#6982=EDGE_CURVE ( 'NONE', #19753, #11635, #4659, .T. ) ;
#6983=DIRECTION ( 'NONE',  ( 1.000000000000000000, 0.000000000000000000, -0.000000000000000000 ) ) ;
#6984=DIRECTION ( 'NONE',  ( 0.000000000000000000, 0.000000000000000000, 1.000000000000000000 ) ) ;
#6986=CARTESIAN_POINT ( 'NONE',  ( 9.141460742840918030, 32.93424481021354921, 42.50000000000000000 ) ) ;
#6990=CARTESIAN_POINT ( 'NONE',  ( 9.141460742840918030, 33.43424481021354921, 42.50000000000000000 ) ) ;
#6993=VECTOR ( 'NONE', #18433, 1000.000000000000000 ) ;
#6994=EDGE_CURVE ( 'NONE', #13036, #11265, #3045, .T. ) ;
#6997=CARTESIAN_POINT ( 'NONE',  ( 28.87540678000427619, -63.74634676501045050, 13.50000000000000000 ) ) ;
#7000=VECTOR ( 'NONE', #18775, 1000.000000000000000 ) ;
#7002=DIRECTION ( 'NONE',  ( 0.000000000000000000, 0.000000000000000000, 1.000000000000000000 ) ) ;
#7005=DIRECTION ( 'NONE',  ( -0.000000000000000000, -0.000000000000000000, 1.000000000000000000 ) ) ;
#7006=CARTESIAN_POINT ( 'NONE',  ( -27.67540678000426979, 36.74634676501047181, 13.50000000000000000 ) ) ;
#7007=DIRECTION ( 'NONE',  ( 0.000000000000000000, 0.000000000000000000, 1.000000000000000000 ) ) ;
#7008=CIRCLE ( 'NONE', #13405, 0.2999999999999999334 ) ;
#7009=AXIS2_PLACEMENT_3D ( 'NONE', #15936, #19423, #12354 ) ;
#7011=CARTESIAN_POINT ( 'NONE',  ( -26.37540678000427619, 10.94079601157914539, 42.50000000000000000 ) ) ;
#7012=DIRECTION ( 'NONE',  ( 1.000000000000000000, 0.000000000000000000, 0.000000000000000000 ) ) ;
#7013=EDGE_CURVE ( 'NONE', #17752, #4113, #18028, .T. ) ;
#7015=ORIENTED_EDGE ( 'NONE', *, *, #8966, .T. ) ;
#7016=ORIENTED_EDGE ( 'NONE', *, *, #7247, .F. ) ;
#7018=CARTESIAN_POINT ( 'NONE',  ( -25.37540678000427263, 63.74634676501045050, 7.799999999999999822 ) ) ;
#7019=DIRECTION ( 'NONE',  ( 0.000000000000000000, 1.000000000000000000, 0.000000000000000000 ) ) ;
#7022=EDGE_CURVE ( 'NONE', #16813, #6358, #19834, .T. ) ;
#7024=EDGE_LOOP ( 'NONE', ( #11777, #337, #20519, #293 ) ) ;
#7025=DIRECTION ( 'NONE',  ( -2.832483164223434527E-16, -1.000000000000000000, 0.000000000000000000 ) ) ;
#7028=CARTESIAN_POINT ( 'NONE',  ( 15.95292532278785913, 51.61873716947361856, 68.00000000000000000 ) ) ;
#7033=CARTESIAN_POINT ( 'NONE',  ( 23.06502549581203709, 2.381505846144868155, 13.31536975879941131 ) ) ;
#7037=ORIENTED_EDGE ( 'NONE', *, *, #20493, .T. ) ;
#7038=AXIS2_PLACEMENT_3D ( 'NONE', #2587, #4477, #9411 ) ;
#7039=VECTOR ( 'NONE', #5811, 1000.000000000000000 ) ;
#7040=DIRECTION ( 'NONE',  ( -1.000000000000000000, 0.000000000000000000, 0.000000000000000000 ) ) ;
#7044=VERTEX_POINT ( 'NONE', #9975 ) ;
#7045=AXIS2_PLACEMENT_3D ( 'NONE', #9759, #21408, #6193 ) ;
#7047=DIRECTION ( 'NONE',  ( 1.000000000000000000, 0.000000000000000000, 0.000000000000000000 ) ) ;
#7049=EDGE_CURVE ( 'NONE', #13197, #6444, #12298, .T. ) ;
#7051=EDGE_CURVE ( 'NONE', #11610, #8448, #18400, .T. ) ;
#7055=AXIS2_PLACEMENT_3D ( 'NONE', #6381, #761, #21254 ) ;
#7056=ORIENTED_EDGE ( 'NONE', *, *, #21778, .F. ) ;
#7058=AXIS2_PLACEMENT_3D ( 'NONE', #1950, #10374, #13492 ) ;
#7059=CARTESIAN_POINT ( 'NONE',  ( 29.17540678000427690, 0.000000000000000000, 7.799999999999999822 ) ) ;
#7061=DIRECTION ( 'NONE',  ( 0.000000000000000000, 0.000000000000000000, -1.000000000000000000 ) ) ;
#7062=CARTESIAN_POINT ( 'NONE',  ( 29.37540678000427619, -6.000000000000000000, 7.200000000000000178 ) ) ;
#7063=EDGE_CURVE ( 'NONE', #15586, #19777, #3398, .T. ) ;
#7066=AXIS2_PLACEMENT_3D ( 'NONE', #999, #11739, #13307 ) ;
#7067=EDGE_LOOP ( 'NONE', ( #10641, #5295, #5371, #770, #19042, #6324, #3272, #19032 ) ) ;
#7068=LINE ( 'NONE', #22067, #15974 ) ;
#7069=FACE_OUTER_BOUND ( 'NONE', #20703, .T. ) ;
#7070=AXIS2_PLACEMENT_3D ( 'NONE', #17918, #2829, #5970 ) ;
#7076=ADVANCED_FACE ( 'NONE', ( #18133 ), #4611, .F. ) ;
#7077=ORIENTED_EDGE ( 'NONE', *, *, #6424, .F. ) ;
#7078=EDGE_CURVE ( 'NONE', #13976, #13366, #15881, .T. ) ;
#7079=ADVANCED_FACE ( 'NONE', ( #4816 ), #15103, .T. ) ;
#7080=CARTESIAN_POINT ( 'NONE',  ( 23.26560317237337117, -3.297643262788042762, 13.49417356369015586 ) ) ;
#7081=ORIENTED_EDGE ( 'NONE', *, *, #8624, .F. ) ;
#7083=VECTOR ( 'NONE', #14063, 1000.000000000000000 ) ;
#7085=CARTESIAN_POINT ( 'NONE',  ( 18.22752199202934520, 0.000000000000000000, 13.79999999999999893 ) ) ;
#7086=FACE_OUTER_BOUND ( 'NONE', #12895, .T. ) ;
#7088=CIRCLE ( 'NONE', #15996, 0.2999999999999999334 ) ;
#7089=CARTESIAN_POINT ( 'NONE',  ( 23.02398829872513986, 3.262363296411947111, 13.79999999999999716 ) ) ;
#7090=DIRECTION ( 'NONE',  ( 0.000000000000000000, -0.000000000000000000, 1.000000000000000000 ) ) ;
#7091=AXIS2_PLACEMENT_3D ( 'NONE', #21292, #19609, #1233 ) ;
#7097=CARTESIAN_POINT ( 'NONE',  ( 14.66174975910705847, -51.76873716947361714, 13.50000000000000000 ) ) ;
#7098=ADVANCED_FACE ( 'NONE', ( #3362 ), #12257, .T. ) ;
#7099=CARTESIAN_POINT ( 'NONE',  ( -26.37540678000427619, -10.94079601157914716, 13.79999999999999893 ) ) ;
#7100=CIRCLE ( 'NONE', #12778, 0.5000000000000004441 ) ;
#7102=ORIENTED_EDGE ( 'NONE', *, *, #1936, .T. ) ;
#7103=ORIENTED_EDGE ( 'NONE', *, *, #14455, .F. ) ;
#7106=ORIENTED_EDGE ( 'NONE', *, *, #18676, .F. ) ;
#7109=AXIS2_PLACEMENT_3D ( 'NONE', #12352, #724, #7351 ) ;
#7110=EDGE_CURVE ( 'NONE', #9769, #11165, #17315, .T. ) ;
#7111=CARTESIAN_POINT ( 'NONE',  ( -15.21174975910705207, 52.10286008774954780, 13.87500000000000000 ) ) ;
#7115=DIRECTION ( 'NONE',  ( 0.000000000000000000, 0.000000000000000000, 1.000000000000000000 ) ) ;
#7116=DIRECTION ( 'NONE',  ( -1.000000000000000000, -0.000000000000000000, -0.000000000000000000 ) ) ;
#7117=DIRECTION ( 'NONE',  ( 0.000000000000000000, 0.000000000000000000, -1.000000000000000000 ) ) ;
#7118=VECTOR ( 'NONE', #6828, 1000.000000000000000 ) ;
#7121=LINE ( 'NONE', #8898, #5216 ) ;
#7122=AXIS2_PLACEMENT_3D ( 'NONE', #14638, #868, #6388 ) ;
#7123=EDGE_CURVE ( 'NONE', #1401, #3263, #19433, .T. ) ;
#7125=CARTESIAN_POINT ( 'NONE',  ( 29.13662752439705272, 0.000000000000000000, -18.50000000000000000 ) ) ;
#7126=DIRECTION ( 'NONE',  ( 0.000000000000000000, 1.000000000000000000, 0.000000000000000000 ) ) ;
#7128=EDGE_LOOP ( 'NONE', ( #16768, #8711, #12536, #9434 ) ) ;
#7130=CARTESIAN_POINT ( 'NONE',  ( 15.95292532278785913, -50.11873716947361856, 13.99999999999999822 ) ) ;
#7134=AXIS2_PLACEMENT_3D ( 'NONE', #17498, #13793, #3740 ) ;
#7135=VERTEX_POINT ( 'NONE', #12368 ) ;
#7136=DIRECTION ( 'NONE',  ( 0.000000000000000000, 0.000000000000000000, 1.000000000000000000 ) ) ;
#7137=AXIS2_PLACEMENT_3D ( 'NONE', #12613, #7951, #11272 ) ;
#7138=ORIENTED_EDGE ( 'NONE', *, *, #6102, .F. ) ;
#7140=DIRECTION ( 'NONE',  ( 1.000000000000000000, 0.000000000000000000, -0.000000000000000000 ) ) ;
#7142=ADVANCED_FACE ( 'NONE', ( #5707 ), #17539, .T. ) ;
#7144=DIRECTION ( 'NONE',  ( -1.000000000000000000, 0.000000000000000000, 0.000000000000000000 ) ) ;
#7146=FACE_OUTER_BOUND ( 'NONE', #6027, .T. ) ;
#7147=CARTESIAN_POINT ( 'NONE',  ( -25.37540678000426908, 38.74634676501045760, 42.50000000000000000 ) ) ;
#7149=DIRECTION ( 'NONE',  ( -0.000000000000000000, -0.000000000000000000, -1.000000000000000000 ) ) ;
#7152=EDGE_CURVE ( 'NONE', #17715, #19005, #16228, .T. ) ;
#7154=TOROIDAL_SURFACE ( 'NONE', #11770, 1.500000000000000000, 0.5000000000000000000 ) ;
#7156=AXIS2_PLACEMENT_3D ( 'NONE', #11294, #18127, #9642 ) ;
#7158=VERTEX_POINT ( 'NONE', #19225 ) ;
#7159=ORIENTED_EDGE ( 'NONE', *, *, #12375, .F. ) ;
#7161=ORIENTED_EDGE ( 'NONE', *, *, #19688, .T. ) ;
#7165=EDGE_LOOP ( 'NONE', ( #19908, #14133, #11643, #9057 ) ) ;
#7168=DIRECTION ( 'NONE',  ( -0.000000000000000000, -0.000000000000000000, -1.000000000000000000 ) ) ;
#7169=DIRECTION ( 'NONE',  ( -1.000000000000000000, 0.000000000000000000, 0.000000000000000000 ) ) ;
#7170=DIRECTION ( 'NONE',  ( 0.000000000000000000, 0.000000000000000000, 1.000000000000000000 ) ) ;
#7175=FACE_OUTER_BOUND ( 'NONE', #6108, .T. ) ;
#7176=EDGE_CURVE ( 'NONE', #13135, #18406, #3904, .T. ) ;
#7181=ORIENTED_EDGE ( 'NONE', *, *, #13869, .T. ) ;
#7183=DIRECTION ( 'NONE',  ( 0.000000000000000000, -0.000000000000000000, -1.000000000000000000 ) ) ;
#7184=EDGE_CURVE ( 'NONE', #6576, #8378, #7589, .T. ) ;
#7188=CARTESIAN_POINT ( 'NONE',  ( -14.96174975910705207, -51.86873716947361856, 14.00000000000000000 ) ) ;
#7190=ORIENTED_EDGE ( 'NONE', *, *, #15438, .F. ) ;
#7191=CARTESIAN_POINT ( 'NONE',  ( -32.20000000000001705, -71.00000000000001421, 3.500000000000000000 ) ) ;
#7194=DIRECTION ( 'NONE',  ( -0.000000000000000000, -0.000000000000000000, -1.000000000000000000 ) ) ;
#7196=CARTESIAN_POINT ( 'NONE',  ( 15.21174975910707161, -41.81054587065082728, 68.25000000000000000 ) ) ;
#7199=EDGE_CURVE ( 'NONE', #1525, #8484, #10826, .T. ) ;
#7200=CARTESIAN_POINT ( 'NONE',  ( 15.21174975910707161, 51.86873716947361856, 68.00000000000000000 ) ) ;
#7202=DIRECTION ( 'NONE',  ( 1.000000000000000000, 0.000000000000000000, 0.000000000000000000 ) ) ;
#7203=EDGE_CURVE ( 'NONE', #2930, #1905, #5914, .T. ) ;
#7208=CARTESIAN_POINT ( 'NONE',  ( -25.37540678000429040, -36.74634676501047181, 13.79999999999999893 ) ) ;
#7211=AXIS2_PLACEMENT_3D ( 'NONE', #8360, #15170, #10382 ) ;
#7212=ORIENTED_EDGE ( 'NONE', *, *, #9646, .F. ) ;
#7215=AXIS2_PLACEMENT_3D ( 'NONE', #14120, #19297, #3741 ) ;
#7216=CIRCLE ( 'NONE', #5429, 0.2999999999999999334 ) ;
#7217=CARTESIAN_POINT ( 'NONE',  ( -31.50000000000002132, 71.70000000000001705, 1.800000000000000044 ) ) ;
#7221=CARTESIAN_POINT ( 'NONE',  ( 15.95292532278785913, 32.11873716947361856, 68.00000000000000000 ) ) ;
#7222=CARTESIAN_POINT ( 'NONE',  ( -30.07540678000427548, -63.74634676501045050, 7.200000000000000178 ) ) ;
#7224=ADVANCED_FACE ( 'NONE', ( #12484 ), #17637, .T. ) ;
#7225=CARTESIAN_POINT ( 'NONE',  ( 29.50000000000002132, 2.512390033608338236, 0.2999999999999947153 ) ) ;
#7226=CARTESIAN_POINT ( 'NONE',  ( -15.05469906388004020, 52.39333383871511529, 13.50000000000000355 ) ) ;
#7227=DIRECTION ( 'NONE',  ( -1.000000000000000000, -0.000000000000000000, 0.000000000000000000 ) ) ;
#7230=CARTESIAN_POINT ( 'NONE',  ( -29.13662752439705272, 0.000000000000000000, 7.200000000000000178 ) ) ;
#7231=DIRECTION ( 'NONE',  ( 0.000000000000000000, 0.000000000000000000, 1.000000000000000000 ) ) ;
#7232=ORIENTED_EDGE ( 'NONE', *, *, #8962, .T. ) ;
#7233=VECTOR ( 'NONE', #9029, 1000.000000000000000 ) ;
#7236=CARTESIAN_POINT ( 'NONE',  ( -15.95292532278785913, 34.11873716947361856, 42.50000000000000711 ) ) ;
#7238=PLANE ( 'NONE',  #21816 ) ;
#7245=ORIENTED_EDGE ( 'NONE', *, *, #7078, .F. ) ;
#7247=EDGE_CURVE ( 'NONE', #19749, #8671, #19118, .T. ) ;
#7248=CARTESIAN_POINT ( 'NONE',  ( 30.67540678000428045, 6.000000000000000000, 3.799999999999999822 ) ) ;
#7252=CARTESIAN_POINT ( 'NONE',  ( 29.37540678000427619, 5.000000000000000000, 3.799999999999999822 ) ) ;
#7253=DIRECTION ( 'NONE',  ( 1.000000000000000000, 0.000000000000000000, -0.000000000000000000 ) ) ;
#7254=AXIS2_PLACEMENT_3D ( 'NONE', #21259, #7843, #16435 ) ;
#7255=AXIS2_PLACEMENT_3D ( 'NONE', #1612, #8453, #6798 ) ;
#7256=LINE ( 'NONE', #17853, #21779 ) ;
#7257=VERTEX_POINT ( 'NONE', #6028 ) ;
#7259=EDGE_CURVE ( 'NONE', #20751, #16560, #8398, .T. ) ;
#7260=ORIENTED_EDGE ( 'NONE', *, *, #4116, .F. ) ;
#7261=CARTESIAN_POINT ( 'NONE',  ( 0.000000000000000000, -32.61873716947361856, 68.00000000000000000 ) ) ;
#7263=EDGE_LOOP ( 'NONE', ( #18038, #10851, #20566, #9489 ) ) ;
#7264=ORIENTED_EDGE ( 'NONE', *, *, #3785, .T. ) ;
#7265=CIRCLE ( 'NONE', #14372, 0.2999999999999999334 ) ;
#7266=CARTESIAN_POINT ( 'NONE',  ( -18.22752199202934520, 0.000000000000000000, 13.79999999999999893 ) ) ;
#7267=FACE_OUTER_BOUND ( 'NONE', #7677, .T. ) ;
#7268=ORIENTED_EDGE ( 'NONE', *, *, #16193, .F. ) ;
#7269=VERTEX_POINT ( 'NONE', #4669 ) ;
#7275=DIRECTION ( 'NONE',  ( 0.000000000000000000, 0.000000000000000000, -1.000000000000000000 ) ) ;
#7276=CARTESIAN_POINT ( 'NONE',  ( -28.57540678000427548, 63.74634676501045050, 13.19999999999999929 ) ) ;
#7280=DIRECTION ( 'NONE',  ( 0.000000000000000000, 0.000000000000000000, 1.000000000000000000 ) ) ;
#7286=ORIENTED_EDGE ( 'NONE', *, *, #4807, .T. ) ;
#7287=CARTESIAN_POINT ( 'NONE',  ( 9.641460742840918030, 33.43424481021354921, 68.00000000000000000 ) ) ;
#7288=PRODUCT_CONTEXT ( 'NONE', #3150, 'mechanical' ) ;
#7289=ORIENTED_EDGE ( 'NONE', *, *, #6811, .F. ) ;
#7290=ORIENTED_EDGE ( 'NONE', *, *, #15515, .T. ) ;
#7293=CARTESIAN_POINT ( 'NONE',  ( 23.02398829872513986, -3.528912754968635213, 13.79999999999999893 ) ) ;
#7294=ORIENTED_EDGE ( 'NONE', *, *, #8160, .F. ) ;
#7295=ORIENTED_EDGE ( 'NONE', *, *, #10767, .T. ) ;
#7301=CARTESIAN_POINT ( 'NONE',  ( 30.37540678000427619, 0.000000000000000000, 7.500000000000000000 ) ) ;
#7304=FACE_OUTER_BOUND ( 'NONE', #10010, .T. ) ;
#7307=DIRECTION ( 'NONE',  ( 1.000000000000000000, 0.000000000000000000, 0.000000000000000000 ) ) ;
#7308=EDGE_CURVE ( 'NONE', #2242, #1813, #17969, .T. ) ;
#7309=DIRECTION ( 'NONE',  ( 1.000000000000000000, -0.000000000000000000, -0.000000000000000000 ) ) ;
#7310=VERTEX_POINT ( 'NONE', #9707 ) ;
#7312=CARTESIAN_POINT ( 'NONE',  ( -26.37540678000427619, 10.94079601157914539, 13.79999999999999893 ) ) ;
#7314=CARTESIAN_POINT ( 'NONE',  ( -26.63662752439704917, -3.061616997868386099E-16, -18.50000000000000000 ) ) ;
#7315=ORIENTED_EDGE ( 'NONE', *, *, #13726, .F. ) ;
#7316=B_SPLINE_CURVE_WITH_KNOTS ( 'NONE', 3,
 ( #9221, #14576, #17707, #14354, #1042, #21429, #19737, #705, #19845, #7554 ),
 .UNSPECIFIED., .F., .F.,
 ( 4, 2, 2, 2, 4 ),
 ( 0.000000000000000000, 0.0007882085451459019303, 0.001182312817718852950, 0.001379364954005326887, 0.001576417090291801042 ),
 .UNSPECIFIED. ) ;
#7317=EDGE_LOOP ( 'NONE', ( #21156, #4801, #922, #17153 ) ) ;
#7318=ORIENTED_EDGE ( 'NONE', *, *, #9780, .T. ) ;
#7319=EDGE_CURVE ( 'NONE', #6172, #13182, #18782, .T. ) ;
#7321=VECTOR ( 'NONE', #11751, 1000.000000000000000 ) ;
#7324=ORIENTED_EDGE ( 'NONE', *, *, #12217, .T. ) ;
#7326=DIRECTION ( 'NONE',  ( 1.000000000000000000, 2.832483164223434527E-16, -0.000000000000000000 ) ) ;
#7328=CARTESIAN_POINT ( 'NONE',  ( 29.37540678000427619, 6.000000000000000000, 3.500000000000000000 ) ) ;
#7330=DIRECTION ( 'NONE',  ( 1.000000000000000000, 0.000000000000000000, 0.000000000000000000 ) ) ;
#7332=FACE_OUTER_BOUND ( 'NONE', #4804, .T. ) ;
#7334=DIRECTION ( 'NONE',  ( 1.000000000000000000, 0.000000000000000000, 0.000000000000000000 ) ) ;
#7340=CARTESIAN_POINT ( 'NONE',  ( -25.37540678000427263, 63.74634676501045050, 3.799999999999999822 ) ) ;
#7341=ORIENTED_EDGE ( 'NONE', *, *, #15873, .T. ) ;
#7345=ORIENTED_EDGE ( 'NONE', *, *, #17304, .F. ) ;
#7348=EDGE_CURVE ( 'NONE', #14892, #1748, #8022, .T. ) ;
#7349=VERTEX_POINT ( 'NONE', #16608 ) ;
#7351=DIRECTION ( 'NONE',  ( 1.000000000000000000, 0.000000000000000000, 0.000000000000000000 ) ) ;
#7352=CIRCLE ( 'NONE', #10208, 2.500000000000002220 ) ;
#7354=CIRCLE ( 'NONE', #13407, 0.2999999999999999334 ) ;
#7358=DIRECTION ( 'NONE',  ( 0.000000000000000000, 0.000000000000000000, 1.000000000000000000 ) ) ;
#7361=ORIENTED_EDGE ( 'NONE', *, *, #8723, .T. ) ;
#7364=CARTESIAN_POINT ( 'NONE',  ( -28.87540678000427619, -6.494748934539263274, 13.19999999999999929 ) ) ;
#7365=ORIENTED_EDGE ( 'NONE', *, *, #2373, .T. ) ;
#7369=ADVANCED_FACE ( 'NONE', ( #1175 ), #4434, .T. ) ;
#7372=ORIENTED_EDGE ( 'NONE', *, *, #19365, .F. ) ;
#7374=AXIS2_PLACEMENT_3D ( 'NONE', #18393, #12914, #7676 ) ;
#7377=ORIENTED_EDGE ( 'NONE', *, *, #6149, .T. ) ;
#7379=VECTOR ( 'NONE', #2020, 1000.000000000000000 ) ;
#7380=VECTOR ( 'NONE', #8377, 1000.000000000000000 ) ;
#7381=CIRCLE ( 'NONE', #17699, 0.2999999999999999334 ) ;
#7383=LINE ( 'NONE', #10622, #9939 ) ;
#7385=CARTESIAN_POINT ( 'NONE',  ( 14.71479891163412113, 52.07369784467161367, 13.50000000000000000 ) ) ;
#7388=EDGE_LOOP ( 'NONE', ( #15263, #19459, #6723, #17887 ) ) ;
#7392=ADVANCED_FACE ( 'NONE', ( #10035 ), #18865, .F. ) ;
#7398=DIRECTION ( 'NONE',  ( -0.000000000000000000, -0.000000000000000000, -1.000000000000000000 ) ) ;
#7401=VERTEX_POINT ( 'NONE', #10251 ) ;
#7403=CARTESIAN_POINT ( 'NONE',  ( 23.02398829872513986, -2.558598175897759841, 13.47089014135852914 ) ) ;
#7407=DIRECTION ( 'NONE',  ( -0.000000000000000000, -1.000000000000000000, -0.000000000000000000 ) ) ;
#7408=DIRECTION ( 'NONE',  ( 1.000000000000000000, 0.000000000000000000, -0.000000000000000000 ) ) ;
#7410=CIRCLE ( 'NONE', #10662, 3.500000000000003109 ) ;
#7411=ADVANCED_FACE ( 'NONE', ( #20110 ), #6638, .T. ) ;
#7412=TOROIDAL_SURFACE ( 'NONE', #19190, 3.800000000000002931, 0.2999999999999999889 ) ;
#7415=AXIS2_PLACEMENT_3D ( 'NONE', #4690, #18326, #3001 ) ;
#7418=DIRECTION ( 'NONE',  ( -2.832483164223434527E-16, 1.000000000000000000, 0.000000000000000000 ) ) ;
#7421=CARTESIAN_POINT ( 'NONE',  ( -17.95292532278785913, -38.74634676501046471, 42.50000000000000711 ) ) ;
#7425=CARTESIAN_POINT ( 'NONE',  ( 9.141460742840918030, -32.61873716947361856, 7.321391277662001151 ) ) ;
#7426=ORIENTED_EDGE ( 'NONE', *, *, #1844, .F. ) ;
#7430=ORIENTED_EDGE ( 'NONE', *, *, #2794, .T. ) ;
#7433=ADVANCED_FACE ( 'NONE', ( #13486 ), #6915, .T. ) ;
#7434=DIRECTION ( 'NONE',  ( 0.000000000000000000, 0.000000000000000000, -1.000000000000000000 ) ) ;
#7435=DIRECTION ( 'NONE',  ( 0.000000000000000000, 0.000000000000000000, 1.000000000000000000 ) ) ;
#7438=CARTESIAN_POINT ( 'NONE',  ( -17.45292532278785913, 0.000000000000000000, 13.99999999999999822 ) ) ;
#7440=CARTESIAN_POINT ( 'NONE',  ( 15.04770344846787822, 51.92604205163220854, 13.50000000000000000 ) ) ;
#7442=VECTOR ( 'NONE', #13639, 1000.000000000000000 ) ;
#7444=AXIS2_PLACEMENT_3D ( 'NONE', #3575, #15316, #11833 ) ;
#7445=CARTESIAN_POINT ( 'NONE',  ( 29.13662752439705272, 0.000000000000000000, 0.000000000000000000 ) ) ;
#7450=ADVANCED_FACE ( 'NONE', ( #22006 ), #21901, .T. ) ;
#7451=VECTOR ( 'NONE', #5045, 1000.000000000000000 ) ;
#7454=ORIENTED_EDGE ( 'NONE', *, *, #17246, .T. ) ;
#7455=AXIS2_PLACEMENT_3D ( 'NONE', #5529, #20852, #19059 ) ;
#7457=CARTESIAN_POINT ( 'NONE',  ( 27.65375860907908745, -2.282443358843508019, -3.134021904840910022E-17 ) ) ;
#7458=VECTOR ( 'NONE', #15934, 1000.000000000000000 ) ;
#7459=CARTESIAN_POINT ( 'NONE',  ( 17.95292532278785913, -34.11873716947361856, 68.00000000000000000 ) ) ;
#7460=ORIENTED_EDGE ( 'NONE', *, *, #20953, .T. ) ;
#7463=ORIENTED_EDGE ( 'NONE', *, *, #3831, .F. ) ;
#7464=DIRECTION ( 'NONE',  ( 1.000000000000000000, 0.000000000000000000, 0.000000000000000000 ) ) ;
#7465=AXIS2_PLACEMENT_3D ( 'NONE', #13331, #16916, #4740 ) ;
#7467=EDGE_CURVE ( 'NONE', #2970, #20337, #14458, .T. ) ;
#7469=DIRECTION ( 'NONE',  ( 0.000000000000000000, 0.000000000000000000, -1.000000000000000000 ) ) ;
#7470=CARTESIAN_POINT ( 'NONE',  ( 32.50000000000002132, 72.00000000000001421, 3.500000000000000000 ) ) ;
#7471=CIRCLE ( 'NONE', #10327, 2.000000000000001776 ) ;
#7472=CIRCLE ( 'NONE', #18847, 5.000000000000004441 ) ;
#7474=CIRCLE ( 'NONE', #14584, 1.999999999999991340 ) ;
#7476=CARTESIAN_POINT ( 'NONE',  ( -32.20000000000001705, 71.00000000000001421, 3.500000000000000000 ) ) ;
#7477=AXIS2_PLACEMENT_3D ( 'NONE', #99, #6607, #14978 ) ;
#7479=CARTESIAN_POINT ( 'NONE',  ( -8.641460742840918030, -32.93424481021354921, 68.00000000000000000 ) ) ;
#7480=CARTESIAN_POINT ( 'NONE',  ( -28.87540678000427619, -63.74634676501045050, 13.19999999999999929 ) ) ;
#7483=ADVANCED_FACE ( 'NONE', ( #8136 ), #14944, .T. ) ;
#7484=ORIENTED_EDGE ( 'NONE', *, *, #10081, .T. ) ;
#7485=DIRECTION ( 'NONE',  ( 0.000000000000000000, 0.000000000000000000, 1.000000000000000000 ) ) ;
#7486=ADVANCED_FACE ( 'NONE', ( #15056 ), #20441, .F. ) ;
#7487=LINE ( 'NONE', #512, #17697 ) ;
#7488=CIRCLE ( 'NONE', #19989, 1.000000000000000888 ) ;
#7490=ORIENTED_EDGE ( 'NONE', *, *, #2043, .F. ) ;
#7491=DIRECTION ( 'NONE',  ( 1.000000000000000000, 0.000000000000000000, 0.000000000000000000 ) ) ;
#7493=CARTESIAN_POINT ( 'NONE',  ( 25.37540678000427263, 63.74634676501045050, 7.799999999999999822 ) ) ;
#7494=AXIS2_PLACEMENT_3D ( 'NONE', #13592, #16831, #8450 ) ;
#7498=EDGE_CURVE ( 'NONE', #17454, #13749, #6285, .T. ) ;
#7499=CARTESIAN_POINT ( 'NONE',  ( 3.127054932750481964, -32.11873716947361856, 42.50000000000000711 ) ) ;
#7500=CARTESIAN_POINT ( 'NONE',  ( -9.641460742840918030, -32.61873716947361856, 42.50000000000000711 ) ) ;
#7502=DIRECTION ( 'NONE',  ( 0.000000000000000000, -1.000000000000000000, 0.000000000000000000 ) ) ;
#7503=ADVANCED_FACE ( 'NONE', ( #11691 ), #12311, .F. ) ;
#7505=DIRECTION ( 'NONE',  ( 1.000000000000000000, 0.000000000000000000, 0.000000000000000000 ) ) ;
#7509=DIRECTION ( 'NONE',  ( -0.000000000000000000, 1.000000000000000000, -0.000000000000000000 ) ) ;
#7510=ADVANCED_FACE ( 'NONE', ( #8349 ), #5931, .T. ) ;
#7511=ORIENTED_EDGE ( 'NONE', *, *, #8962, .F. ) ;
#7513=ORIENTED_EDGE ( 'NONE', *, *, #4260, .F. ) ;
#7515=ORIENTED_EDGE ( 'NONE', *, *, #16398, .T. ) ;
#7518=ORIENTED_EDGE ( 'NONE', *, *, #11039, .F. ) ;
#7519=VECTOR ( 'NONE', #16404, 1000.000000000000000 ) ;
#7520=CIRCLE ( 'NONE', #1790, 0.5000000000000000000 ) ;
#7521=EDGE_LOOP ( 'NONE', ( #21544, #7463, #21767, #4833 ) ) ;
#7524=ORIENTED_EDGE ( 'NONE', *, *, #16883, .T. ) ;
#7526=EDGE_CURVE ( 'NONE', #11236, #8930, #14110, .T. ) ;
#7530=EDGE_CURVE ( 'NONE', #17106, #6358, #17611, .T. ) ;
#7531=AXIS2_PLACEMENT_3D ( 'NONE', #6456, #1384, #6565 ) ;
#7532=CIRCLE ( 'NONE', #5380, 0.5000000000000004441 ) ;
#7533=CARTESIAN_POINT ( 'NONE',  ( 4.127054932750481520, 33.93424481021354921, 68.50000000000000000 ) ) ;
#7534=CARTESIAN_POINT ( 'NONE',  ( 0.000000000000000000, 69.00000000000000000, -150.0833101980363722 ) ) ;
#7535=DIRECTION ( 'NONE',  ( -2.832483164223434527E-16, -1.000000000000000000, -0.000000000000000000 ) ) ;
#7536=CARTESIAN_POINT ( 'NONE',  ( 25.37540678000429395, -39.04634676501046187, 13.50000000000000000 ) ) ;
#7538=ORIENTED_EDGE ( 'NONE', *, *, #17275, .F. ) ;
#7539=DIRECTION ( 'NONE',  ( 0.000000000000000000, 0.000000000000000000, 1.000000000000000000 ) ) ;
#7541=FACE_OUTER_BOUND ( 'NONE', #3319, .T. ) ;
#7542=ORIENTED_EDGE ( 'NONE', *, *, #2273, .F. ) ;
#7543=EDGE_LOOP ( 'NONE', ( #4421, #21053, #17891, #11528 ) ) ;
#7546=EDGE_CURVE ( 'NONE', #9117, #19361, #17691, .T. ) ;
#7547=CARTESIAN_POINT ( 'NONE',  ( 14.96174975910705918, 32.10873716947361345, 13.05380965755522737 ) ) ;
#7548=ADVANCED_BREP_SHAPE_REPRESENTATION ( '', ( #6179, #17493 ), #10355 ) ;
#7549=ADVANCED_FACE ( 'NONE', ( #15915 ), #13800, .F. ) ;
#7551=DIRECTION ( 'NONE',  ( -0.000000000000000000, -0.000000000000000000, -1.000000000000000000 ) ) ;
#7554=CARTESIAN_POINT ( 'NONE',  ( -23.02398829872513986, 2.157133568460765538, 13.19999999999999929 ) ) ;
#7555=ORIENTED_EDGE ( 'NONE', *, *, #7530, .F. ) ;
#7556=DIRECTION ( 'NONE',  ( 1.000000000000000000, 0.000000000000000000, 0.000000000000000000 ) ) ;
#7557=AXIS2_PLACEMENT_3D ( 'NONE', #6621, #6519, #20150 ) ;
#7560=ORIENTED_EDGE ( 'NONE', *, *, #11231, .F. ) ;
#7562=CARTESIAN_POINT ( 'NONE',  ( 27.61238352468048518, -2.348761424523157615, 0.000000000000000000 ) ) ;
#7566=ADVANCED_FACE ( 'NONE', ( #20873 ), #3056, .T. ) ;
#7573=DIRECTION ( 'NONE',  ( 0.000000000000000000, 1.000000000000000000, 0.000000000000000000 ) ) ;
#7575=ADVANCED_FACE ( 'NONE', ( #5777 ), #17386, .F. ) ;
#7576=FACE_OUTER_BOUND ( 'NONE', #11450, .T. ) ;
#7578=DIRECTION ( 'NONE',  ( -1.000000000000000000, 0.000000000000000000, 0.000000000000000000 ) ) ;
#7580=VERTEX_POINT ( 'NONE', #3980 ) ;
#7582=DIRECTION ( 'NONE',  ( 1.000000000000000000, 0.000000000000000000, 0.000000000000000000 ) ) ;
#7585=EDGE_LOOP ( 'NONE', ( #13621, #21794, #6275, #9048 ) ) ;
#7586=SURFACE_STYLE_FILL_AREA ( #6132 ) ;
#7588=VECTOR ( 'NONE', #17339, 1000.000000000000000 ) ;
#7589=LINE ( 'NONE', #1676, #8770 ) ;
#7591=DIRECTION ( 'NONE',  ( 1.000000000000000000, 0.000000000000000000, -0.000000000000000000 ) ) ;
#7592=EDGE_LOOP ( 'NONE', ( #2156, #21608, #672, #3318 ) ) ;
#7593=AXIS2_PLACEMENT_3D ( 'NONE', #11792, #6907, #18738 ) ;
#7598=VERTEX_POINT ( 'NONE', #20980 ) ;
#7600=CIRCLE ( 'NONE', #14737, 0.3000000000000016542 ) ;
#7602=ORIENTED_EDGE ( 'NONE', *, *, #4591, .F. ) ;
#7604=VECTOR ( 'NONE', #3108, 1000.000000000000000 ) ;
#7607=FACE_OUTER_BOUND ( 'NONE', #16707, .T. ) ;
#7608=EDGE_CURVE ( 'NONE', #17937, #16679, #7008, .T. ) ;
#7609=DIRECTION ( 'NONE',  ( 0.000000000000000000, 0.000000000000000000, -1.000000000000000000 ) ) ;
#7610=CARTESIAN_POINT ( 'NONE',  ( -29.37573593128808369, -68.87573593128806237, -5.214931150217776400E-15 ) ) ;
#7611=FACE_OUTER_BOUND ( 'NONE', #7024, .T. ) ;
#7612=ORIENTED_EDGE ( 'NONE', *, *, #3218, .F. ) ;
#7613=CARTESIAN_POINT ( 'NONE',  ( 3.127054932750481964, 32.61873716947361856, 42.50000000000000711 ) ) ;
#7615=CARTESIAN_POINT ( 'NONE',  ( 23.02398829872514341, -5.683640910026986681, 42.50000000000000000 ) ) ;
#7617=DIRECTION ( 'NONE',  ( -1.000000000000000000, 0.000000000000000000, 0.000000000000000000 ) ) ;
#7618=EDGE_CURVE ( 'NONE', #10680, #15986, #7352, .T. ) ;
#7620=EDGE_LOOP ( 'NONE', ( #5742, #9628, #8690, #2431 ) ) ;
#7621=ORIENTED_EDGE ( 'NONE', *, *, #16147, .F. ) ;
#7622=LINE ( 'NONE', #9741, #7828 ) ;
#7625=ORIENTED_EDGE ( 'NONE', *, *, #13336, .F. ) ;
#7626=DIRECTION ( 'NONE',  ( 1.000000000000000000, 0.000000000000000000, 0.000000000000000000 ) ) ;
#7631=CARTESIAN_POINT ( 'NONE',  ( 27.37540678000427619, 7.754037881813018962E-15, 42.50000000000000000 ) ) ;
#7632=CARTESIAN_POINT ( 'NONE',  ( -30.07540678000427548, 0.000000000000000000, 7.500000000000000000 ) ) ;
#7633=CARTESIAN_POINT ( 'NONE',  ( 9.641460742840918030, -32.93424481021354921, 68.00000000000000000 ) ) ;
#7639=DIRECTION ( 'NONE',  ( -3.052134192567367925E-16, 1.000000000000000000, 0.000000000000000000 ) ) ;
#7641=CARTESIAN_POINT ( 'NONE',  ( 15.21174975910705918, -51.86873716947361856, 14.00000000000000000 ) ) ;
#7642=ORIENTED_EDGE ( 'NONE', *, *, #4694, .F. ) ;
#7645=EDGE_CURVE ( 'NONE', #6172, #22137, #6212, .T. ) ;
#7646=ORIENTED_EDGE ( 'NONE', *, *, #15828, .F. ) ;
#7651=ORIENTED_EDGE ( 'NONE', *, *, #1039, .F. ) ;
#7652=DIRECTION ( 'NONE',  ( 0.000000000000000000, 0.000000000000000000, 1.000000000000000000 ) ) ;
#7653=LINE ( 'NONE', #14447, #20793 ) ;
#7654=CARTESIAN_POINT ( 'NONE',  ( -28.87540678000428329, 6.494748934539265051, 13.24746166461178554 ) ) ;
#7656=CARTESIAN_POINT ( 'NONE',  ( -23.07462249345254435, 2.431574673422040700, 13.33584746657813902 ) ) ;
#7657=ORIENTED_EDGE ( 'NONE', *, *, #13340, .T. ) ;
#7658=DIRECTION ( 'NONE',  ( 0.000000000000000000, 0.000000000000000000, 1.000000000000000000 ) ) ;
#7659=DIRECTION ( 'NONE',  ( -0.000000000000000000, 1.000000000000000000, -0.000000000000000000 ) ) ;
#7660=CARTESIAN_POINT ( 'NONE',  ( -32.20000000000001705, -71.00000000000001421, 3.500000000000000000 ) ) ;
#7661=ORIENTED_EDGE ( 'NONE', *, *, #9309, .T. ) ;
#7662=ORIENTED_EDGE ( 'NONE', *, *, #21972, .F. ) ;
#7664=CARTESIAN_POINT ( 'NONE',  ( 25.37540678000427263, -63.74634676501045050, 7.799999999999999822 ) ) ;
#7665=LINE ( 'NONE', #4518, #15318 ) ;
#7666=EDGE_CURVE ( 'NONE', #2722, #21585, #9495, .T. ) ;
#7667=ORIENTED_EDGE ( 'NONE', *, *, #8477, .F. ) ;
#7668=EDGE_CURVE ( 'NONE', #16560, #7135, #5949, .T. ) ;
#7669=DIRECTION ( 'NONE',  ( 0.000000000000000000, -0.000000000000000000, -1.000000000000000000 ) ) ;
#7670=ORIENTED_EDGE ( 'NONE', *, *, #14368, .T. ) ;
#7676=DIRECTION ( 'NONE',  ( 0.000000000000000000, 0.000000000000000000, -1.000000000000000000 ) ) ;
#7677=EDGE_LOOP ( 'NONE', ( #5000, #20905, #4444, #4797 ) ) ;
#7678=DIRECTION ( 'NONE',  ( 0.000000000000000000, 0.000000000000000000, 1.000000000000000000 ) ) ;
#7680=CARTESIAN_POINT ( 'NONE',  ( -14.97529860451076189, 51.91950568661982857, 13.84831215707030339 ) ) ;
#7681=CARTESIAN_POINT ( 'NONE',  ( 23.32398829872514057, 5.683640910026983128, 13.79999999999999893 ) ) ;
#7682=EDGE_LOOP ( 'NONE', ( #18474, #13262, #5966, #20809 ) ) ;
#7683=EDGE_CURVE ( 'NONE', #13748, #17214, #9441, .T. ) ;
#7684=AXIS2_PLACEMENT_3D ( 'NONE', #7971, #18461, #22063 ) ;
#7685=CIRCLE ( 'NONE', #12647, 0.2999999999999999334 ) ;
#7686=VERTEX_POINT ( 'NONE', #17826 ) ;
#7688=DIRECTION ( 'NONE',  ( -0.000000000000000000, 0.000000000000000000, 1.000000000000000000 ) ) ;
#7690=ORIENTED_EDGE ( 'NONE', *, *, #9055, .F. ) ;
#7695=CARTESIAN_POINT ( 'NONE',  ( 8.641460742840918030, 33.93424481021354921, 68.50000000000000000 ) ) ;
#7697=ORIENTED_EDGE ( 'NONE', *, *, #16364, .F. ) ;
#7699=AXIS2_PLACEMENT_3D ( 'NONE', #3870, #15814, #158 ) ;
#7700=ORIENTED_EDGE ( 'NONE', *, *, #3725, .T. ) ;
#7701=DIRECTION ( 'NONE',  ( 1.000000000000000000, 0.000000000000000000, 0.000000000000000000 ) ) ;
#7702=DIRECTION ( 'NONE',  ( 0.000000000000000000, -0.000000000000000000, -1.000000000000000000 ) ) ;
#7703=CARTESIAN_POINT ( 'NONE',  ( 29.17540678000427690, 6.499884319688664647, 7.500000000000000000 ) ) ;
#7704=CARTESIAN_POINT ( 'NONE',  ( 23.02398829872513986, -2.157133568460768647, 13.19999999999999929 ) ) ;
#7708=( BOUNDED_CURVE ( )  B_SPLINE_CURVE ( 3, ( #4336, #18312, #2986, #19890 ),
 .UNSPECIFIED., .F., .T. ) 
 B_SPLINE_CURVE_WITH_KNOTS ( ( 4, 4 ),
 ( 1.570796326794896558, 3.141592653589793116 ),
 .UNSPECIFIED. ) 
 CURVE ( )  GEOMETRIC_REPRESENTATION_ITEM ( )  RATIONAL_B_SPLINE_CURVE ( ( 1.000000000000000000, 0.8047378541243649375, 0.8047378541243649375, 1.000000000000000000 ) ) 
 REPRESENTATION_ITEM ( '' )  );
#7711=CYLINDRICAL_SURFACE ( 'NONE', #11872, 0.5000000000000004441 ) ;
#7714=AXIS2_PLACEMENT_3D ( 'NONE', #726, #14047, #13142 ) ;
#7715=CYLINDRICAL_SURFACE ( 'NONE', #15671, 1.000000000000000888 ) ;
#7719=ORIENTED_EDGE ( 'NONE', *, *, #15415, .F. ) ;
#7723=CARTESIAN_POINT ( 'NONE',  ( -25.37540678000427263, 63.74634676501045050, 7.799999999999999822 ) ) ;
#7728=EDGE_CURVE ( 'NONE', #4820, #6037, #9332, .T. ) ;
#7729=AXIS2_PLACEMENT_3D ( 'NONE', #16913, #11233, #18055 ) ;
#7732=AXIS2_PLACEMENT_3D ( 'NONE', #14423, #2682, #6405 ) ;
#7734=CARTESIAN_POINT ( 'NONE',  ( -14.96174975910705207, 41.81054587065082728, 13.79999999999999893 ) ) ;
#7736=EDGE_CURVE ( 'NONE', #14744, #21160, #18437, .T. ) ;
#7738=DIRECTION ( 'NONE',  ( -0.000000000000000000, -0.000000000000000000, -1.000000000000000000 ) ) ;
#7739=CARTESIAN_POINT ( 'NONE',  ( 32.20000000000001705, -71.00000000000001421, 1.800000000000000044 ) ) ;
#7740=DIRECTION ( 'NONE',  ( 0.000000000000000000, 0.000000000000000000, -1.000000000000000000 ) ) ;
#7743=VECTOR ( 'NONE', #17849, 1000.000000000000000 ) ;
#7744=CARTESIAN_POINT ( 'NONE',  ( 29.20000000000002061, 50.00000000000000000, 0.000000000000000000 ) ) ;
#7745=AXIS2_PLACEMENT_3D ( 'NONE', #6736, #8065, #19937 ) ;
#7748=LINE ( 'NONE', #18018, #8105 ) ;
#7750=CARTESIAN_POINT ( 'NONE',  ( -17.95292532278785913, -50.11873716947361856, 13.49999999999999822 ) ) ;
#7752=ORIENTED_EDGE ( 'NONE', *, *, #9281, .T. ) ;
#7753=DIRECTION ( 'NONE',  ( 0.000000000000000000, 0.000000000000000000, 1.000000000000000000 ) ) ;
#7755=LINE ( 'NONE', #14556, #20283 ) ;
#7757=VECTOR ( 'NONE', #3301, 1000.000000000000000 ) ;
#7758=CIRCLE ( 'NONE', #9540, 0.5000000000000004441 ) ;
#7759=AXIS2_PLACEMENT_3D ( 'NONE', #9, #11752, #15106 ) ;
#7760=VECTOR ( 'NONE', #12834, 1000.000000000000000 ) ;
#7761=EDGE_CURVE ( 'NONE', #20854, #13945, #19269, .T. ) ;
#7765=ORIENTED_EDGE ( 'NONE', *, *, #62, .T. ) ;
#7766=CARTESIAN_POINT ( 'NONE',  ( -8.641460742840918030, 32.93424481021354921, 42.50000000000000000 ) ) ;
#7767=EDGE_CURVE ( 'NONE', #19811, #11511, #5405, .T. ) ;
#7768=DIRECTION ( 'NONE',  ( 0.000000000000000000, -0.000000000000000000, 1.000000000000000000 ) ) ;
#7769=CARTESIAN_POINT ( 'NONE',  ( 14.96174975910705740, 51.76873716947361004, 13.50000000000000000 ) ) ;
#7770=LINE ( 'NONE', #5985, #1480 ) ;
#7774=CARTESIAN_POINT ( 'NONE',  ( 15.21174975910705918, 51.86873716947361856, 14.00000000000000000 ) ) ;
#7775=AXIS2_PLACEMENT_3D ( 'NONE', #15995, #10534, #451 ) ;
#7779=ORIENTED_EDGE ( 'NONE', *, *, #16341, .T. ) ;
#7781=LINE ( 'NONE', #13241, #15620 ) ;
#7782=EDGE_CURVE ( 'NONE', #2691, #20345, #1269, .T. ) ;
#7783=DIRECTION ( 'NONE',  ( 0.000000000000000000, -1.000000000000000000, 0.000000000000000000 ) ) ;
#7784=ORIENTED_EDGE ( 'NONE', *, *, #10675, .F. ) ;
#7787=VECTOR ( 'NONE', #12666, 1000.000000000000000 ) ;
#7789=ORIENTED_EDGE ( 'NONE', *, *, #4358, .T. ) ;
#7790=CARTESIAN_POINT ( 'NONE',  ( 14.66174975910705847, -42.11054587065083155, 13.50000000000000000 ) ) ;
#7791=CARTESIAN_POINT ( 'NONE',  ( 15.21174975910707161, -51.86873716947361856, 68.00000000000000000 ) ) ;
#7792=LINE ( 'NONE', #20098, #8877 ) ;
#7793=LINE ( 'NONE', #13560, #20236 ) ;
#7795=VECTOR ( 'NONE', #6226, 1000.000000000000000 ) ;
#7796=AXIS2_PLACEMENT_3D ( 'NONE', #11485, #9600, #19781 ) ;
#7798=PLANE ( 'NONE',  #13759 ) ;
#7799=EDGE_LOOP ( 'NONE', ( #13379, #20676, #1130, #10150 ) ) ;
#7801=CYLINDRICAL_SURFACE ( 'NONE', #2471, 0.2999999999999999334 ) ;
#7802=ADVANCED_FACE ( 'NONE', ( #2244 ), #8865, .F. ) ;
#7805=AXIS2_PLACEMENT_3D ( 'NONE', #10513, #20916, #9054 ) ;
#7808=EDGE_LOOP ( 'NONE', ( #17180, #7993, #19921, #6713 ) ) ;
#7809=EDGE_CURVE ( 'NONE', #4893, #17752, #16257, .T. ) ;
#7810=DIRECTION ( 'NONE',  ( 0.000000000000000000, 0.000000000000000000, -1.000000000000000000 ) ) ;
#7813=AXIS2_PLACEMENT_3D ( 'NONE', #7470, #19527, #17625 ) ;
#7816=DIRECTION ( 'NONE',  ( 0.000000000000000000, 1.000000000000000000, 0.000000000000000000 ) ) ;
#7817=ORIENTED_EDGE ( 'NONE', *, *, #9994, .T. ) ;
#7818=EDGE_LOOP ( 'NONE', ( #3688, #14483, #1492, #6940 ) ) ;
#7820=CARTESIAN_POINT ( 'NONE',  ( 26.56227312273159313, 9.958410664601840878, 42.50000000000000000 ) ) ;
#7822=AXIS2_PLACEMENT_3D ( 'NONE', #9125, #14149, #15933 ) ;
#7823=VECTOR ( 'NONE', #1582, 1000.000000000000000 ) ;
#7824=VERTEX_POINT ( 'NONE', #17471 ) ;
#7828=VECTOR ( 'NONE', #16441, 1000.000000000000000 ) ;
#7830=CARTESIAN_POINT ( 'NONE',  ( -23.32398829872514057, -2.157133568460768647, 13.50000000000000000 ) ) ;
#7831=CARTESIAN_POINT ( 'NONE',  ( 32.20000000000001705, 0.000000000000000000, 1.500000000000000000 ) ) ;
#7833=DIRECTION ( 'NONE',  ( 0.000000000000000000, -0.000000000000000000, 1.000000000000000000 ) ) ;
#7834=DIRECTION ( 'NONE',  ( 0.000000000000000000, 0.000000000000000000, 1.000000000000000000 ) ) ;
#7838=ORIENTED_EDGE ( 'NONE', *, *, #308, .F. ) ;
#7839=AXIS2_PLACEMENT_3D ( 'NONE', #5365, #1534, #1969 ) ;
#7840=CARTESIAN_POINT ( 'NONE',  ( -9.641460742840918030, -32.61873716947361856, 109.6002446535588319 ) ) ;
#7842=AXIS2_PLACEMENT_3D ( 'NONE', #14118, #154, #12008 ) ;
#7843=DIRECTION ( 'NONE',  ( 0.000000000000000000, 0.000000000000000000, 1.000000000000000000 ) ) ;
#7844=CIRCLE ( 'NONE', #3913, 0.5000000000000004441 ) ;
#7847=ORIENTED_EDGE ( 'NONE', *, *, #5661, .F. ) ;
#7848=ORIENTED_EDGE ( 'NONE', *, *, #14869, .F. ) ;
#7849=DIRECTION ( 'NONE',  ( 1.000000000000000000, 0.000000000000000000, 0.000000000000000000 ) ) ;
#7856=EDGE_CURVE ( 'NONE', #9562, #12188, #12526, .T. ) ;
#7857=DIRECTION ( 'NONE',  ( -0.000000000000000000, -1.000000000000000000, -0.000000000000000000 ) ) ;
#7858=LINE ( 'NONE', #11186, #13055 ) ;
#7861=FACE_OUTER_BOUND ( 'NONE', #9298, .T. ) ;
#7862=CARTESIAN_POINT ( 'NONE',  ( 28.87540678000427619, 0.000000000000000000, 13.50000000000000000 ) ) ;
#7864=CARTESIAN_POINT ( 'NONE',  ( 23.32398829872514412, -5.683640910026986681, 13.50000000000000000 ) ) ;
#7865=CARTESIAN_POINT ( 'NONE',  ( 30.67540678000428045, 63.74634676501045050, 3.799999999999999822 ) ) ;
#7866=AXIS2_PLACEMENT_3D ( 'NONE', #19182, #19075, #12123 ) ;
#7870=AXIS2_PLACEMENT_3D ( 'NONE', #7340, #10699, #10806 ) ;
#7872=ORIENTED_EDGE ( 'NONE', *, *, #637, .F. ) ;
#7873=ORIENTED_EDGE ( 'NONE', *, *, #16006, .F. ) ;
#7878=EDGE_LOOP ( 'NONE', ( #7289, #11021, #12337, #4994 ) ) ;
#7879=ORIENTED_EDGE ( 'NONE', *, *, #1039, .T. ) ;
#7882=EDGE_CURVE ( 'NONE', #21191, #8611, #2354, .T. ) ;
#7884=CARTESIAN_POINT ( 'NONE',  ( 15.05577974591271051, -52.39333374568191459, 13.50000000000000000 ) ) ;
#7888=VERTEX_POINT ( 'NONE', #2474 ) ;
#7889=DIRECTION ( 'NONE',  ( -0.000000000000000000, -0.000000000000000000, 1.000000000000000000 ) ) ;
#7890=ADVANCED_FACE ( 'NONE', ( #15776 ), #227, .F. ) ;
#7891=CARTESIAN_POINT ( 'NONE',  ( 3.627054932750481964, -32.61873716947361856, 7.321391277662001151 ) ) ;
#7892=DIRECTION ( 'NONE',  ( 0.000000000000000000, 1.000000000000000000, -0.000000000000000000 ) ) ;
#7893=DIRECTION ( 'NONE',  ( 0.000000000000000000, -0.000000000000000000, -1.000000000000000000 ) ) ;
#7894=ORIENTED_EDGE ( 'NONE', *, *, #16324, .T. ) ;
#7900=CARTESIAN_POINT ( 'NONE',  ( 14.97552947837228032, 51.92046840034491595, 13.84856038353110463 ) ) ;
#7902=DIRECTION ( 'NONE',  ( 1.000000000000000000, 0.000000000000000000, 0.000000000000000000 ) ) ;
#7907=CARTESIAN_POINT ( 'NONE',  ( -28.57540678000427548, -63.74634676501045050, 13.50000000000000000 ) ) ;
#7908=EDGE_CURVE ( 'NONE', #15670, #5317, #11990, .T. ) ;
#7909=CARTESIAN_POINT ( 'NONE',  ( -3.127054932750481964, -32.11873716947361856, 42.50000000000000711 ) ) ;
#7910=DIRECTION ( 'NONE',  ( 1.000000000000000000, 0.000000000000000000, 0.000000000000000000 ) ) ;
#7911=EDGE_LOOP ( 'NONE', ( #9322, #1438, #17055, #17038 ) ) ;
#7912=CARTESIAN_POINT ( 'NONE',  ( -9.641460742840918030, -33.43424481021354921, 68.00000000000000000 ) ) ;
#7916=CARTESIAN_POINT ( 'NONE',  ( -14.96174975910705207, 51.76873716947361714, 13.79999999999999716 ) ) ;
#7919=FACE_OUTER_BOUND ( 'NONE', #15344, .T. ) ;
#7921=ORIENTED_EDGE ( 'NONE', *, *, #8563, .T. ) ;
#7922=DIRECTION ( 'NONE',  ( 0.000000000000000000, 0.000000000000000000, -1.000000000000000000 ) ) ;
#7923=DIRECTION ( 'NONE',  ( 1.000000000000000000, 0.000000000000000000, 0.000000000000000000 ) ) ;
#7927=DIRECTION ( 'NONE',  ( 0.000000000000000000, 0.000000000000000000, 1.000000000000000000 ) ) ;
#7928=CARTESIAN_POINT ( 'NONE',  ( 17.95292532278785913, 34.11873716947361856, 68.00000000000000000 ) ) ;
#7929=DIRECTION ( 'NONE',  ( -1.000000000000000000, 0.000000000000000000, 0.000000000000000000 ) ) ;
#7930=VECTOR ( 'NONE', #19301, 1000.000000000000000 ) ;
#7932=ADVANCED_FACE ( 'NONE', ( #11412 ), #8428, .T. ) ;
#7933=EDGE_CURVE ( 'NONE', #4677, #10096, #11275, .T. ) ;
#7935=CARTESIAN_POINT ( 'NONE',  ( -29.50000000000002132, 0.000000000000000000, 1.500000000000000000 ) ) ;
#7936=DIRECTION ( 'NONE',  ( -1.000000000000000000, 0.000000000000000000, -0.000000000000000000 ) ) ;
#7937=CARTESIAN_POINT ( 'NONE',  ( 17.45292532278785913, 34.11873716947361856, 68.00000000000000000 ) ) ;
#7938=CIRCLE ( 'NONE', #10783, 0.5000000000000000000 ) ;
#7940=FACE_OUTER_BOUND ( 'NONE', #3290, .T. ) ;
#7943=EDGE_CURVE ( 'NONE', #12460, #225, #14124, .T. ) ;
#7944=CYLINDRICAL_SURFACE ( 'NONE', #14935, 0.2999999999999999334 ) ;
#7951=DIRECTION ( 'NONE',  ( 1.000000000000000000, -0.000000000000000000, -0.000000000000000000 ) ) ;
#7952=ORIENTED_EDGE ( 'NONE', *, *, #16173, .T. ) ;
#7956=CARTESIAN_POINT ( 'NONE',  ( -1.836970198721029934E-16, -71.70000000000001705, 3.200000000000000178 ) ) ;
#7958=VECTOR ( 'NONE', #15856, 1000.000000000000000 ) ;
#7959=ORIENTED_EDGE ( 'NONE', *, *, #6924, .F. ) ;
#7963=DIRECTION ( 'NONE',  ( 0.000000000000000000, 0.000000000000000000, 1.000000000000000000 ) ) ;
#7964=DIRECTION ( 'NONE',  ( -0.000000000000000000, -1.000000000000000000, 0.000000000000000000 ) ) ;
#7965=CARTESIAN_POINT ( 'NONE',  ( -29.13662752439705272, 0.000000000000000000, 3.500000000000000000 ) ) ;
#7967=FACE_OUTER_BOUND ( 'NONE', #21175, .T. ) ;
#7968=CIRCLE ( 'NONE', #7254, 0.3000000000000016542 ) ;
#7970=FACE_OUTER_BOUND ( 'NONE', #1079, .T. ) ;
#7971=CARTESIAN_POINT ( 'NONE',  ( -29.13662752439705272, 0.000000000000000000, 3.799999999999999822 ) ) ;
#7974=CARTESIAN_POINT ( 'NONE',  ( 9.641460742840918030, 32.61873716947361856, 68.00000000000000000 ) ) ;
#7976=ORIENTED_EDGE ( 'NONE', *, *, #18558, .F. ) ;
#7977=VERTEX_POINT ( 'NONE', #7734 ) ;
#7979=ADVANCED_FACE ( 'NONE', ( #5951 ), #4849, .T. ) ;
#7981=EDGE_CURVE ( 'NONE', #1455, #17364, #4475, .T. ) ;
#7985=DIRECTION ( 'NONE',  ( -1.000000000000000000, 0.000000000000000000, 0.000000000000000000 ) ) ;
#7986=CARTESIAN_POINT ( 'NONE',  ( 26.63662752439704917, 3.061616997868386099E-16, 1.500000000000001332 ) ) ;
#7989=EDGE_CURVE ( 'NONE', #2179, #12457, #12348, .T. ) ;
#7990=CARTESIAN_POINT ( 'NONE',  ( -3.127054932750481964, 32.11873716947361856, 42.50000000000000711 ) ) ;
#7991=LINE ( 'NONE', #4746, #20076 ) ;
#7992=CARTESIAN_POINT ( 'NONE',  ( -29.13662752439705272, 0.000000000000000000, -18.50000000000000000 ) ) ;
#7993=ORIENTED_EDGE ( 'NONE', *, *, #406, .F. ) ;
#7995=EDGE_LOOP ( 'NONE', ( #19437, #2398, #17684, #16980 ) ) ;
#7998=CARTESIAN_POINT ( 'NONE',  ( 23.04273156199908357, -2.261510999192740901, 13.19999999999999929 ) ) ;
#7999=DIRECTION ( 'NONE',  ( 0.000000000000000000, 0.000000000000000000, 1.000000000000000000 ) ) ;
#8000=EDGE_CURVE ( 'NONE', #9706, #19294, #22040, .T. ) ;
#8002=EDGE_CURVE ( 'NONE', #2490, #3783, #20045, .T. ) ;
#8006=CARTESIAN_POINT ( 'NONE',  ( -32.50000000000002132, 71.00000000000001421, 1.800000000000000044 ) ) ;
#8008=LINE ( 'NONE', #4763, #17428 ) ;
#8011=DIRECTION ( 'NONE',  ( -1.000000000000000000, 0.000000000000000000, 0.000000000000000000 ) ) ;
#8013=ADVANCED_FACE ( 'NONE', ( #16445 ), #19162, .T. ) ;
#8019=DIRECTION ( 'NONE',  ( 0.000000000000000000, 0.000000000000000000, -1.000000000000000000 ) ) ;
#8021=VERTEX_POINT ( 'NONE', #18009 ) ;
#8022=LINE ( 'NONE', #1283, #21297 ) ;
#8023=CARTESIAN_POINT ( 'NONE',  ( 15.21174975910707161, 52.11873716947361856, 68.00000000000000000 ) ) ;
#8026=AXIS2_PLACEMENT_3D ( 'NONE', #20763, #12449, #20866 ) ;
#8027=ORIENTED_EDGE ( 'NONE', *, *, #6982, .F. ) ;
#8028=ORIENTED_EDGE ( 'NONE', *, *, #149, .T. ) ;
#8036=ORIENTED_EDGE ( 'NONE', *, *, #13104, .F. ) ;
#8038=CARTESIAN_POINT ( 'NONE',  ( 23.02398829872513986, 2.157133568460765538, 7.500000000000000000 ) ) ;
#8039=DIRECTION ( 'NONE',  ( 1.000000000000000000, 0.000000000000000000, 0.000000000000000000 ) ) ;
#8040=FACE_OUTER_BOUND ( 'NONE', #220, .T. ) ;
#8044=CARTESIAN_POINT ( 'NONE',  ( -23.02398829872514341, -5.683640910026986681, 42.50000000000000000 ) ) ;
#8046=DIRECTION ( 'NONE',  ( -1.000000000000000000, 0.000000000000000000, 0.000000000000000000 ) ) ;
#8047=VERTEX_POINT ( 'NONE', #1551 ) ;
#8049=EDGE_CURVE ( 'NONE', #11393, #20783, #9966, .T. ) ;
#8051=ORIENTED_EDGE ( 'NONE', *, *, #11793, .F. ) ;
#8052=CARTESIAN_POINT ( 'NONE',  ( -26.56227312273159313, 9.958410664601840878, 42.50000000000000000 ) ) ;
#8056=ORIENTED_EDGE ( 'NONE', *, *, #12900, .T. ) ;
#8057=AXIS2_PLACEMENT_3D ( 'NONE', #1536, #14972, #5251 ) ;
#8059=ADVANCED_FACE ( 'NONE', ( #18684 ), #13861, .T. ) ;
#8061=DIRECTION ( 'NONE',  ( 0.000000000000000000, 0.000000000000000000, -1.000000000000000000 ) ) ;
#8063=VECTOR ( 'NONE', #21373, 1000.000000000000000 ) ;
#8064=CARTESIAN_POINT ( 'NONE',  ( -9.641460742840918030, 32.61873716947361856, 68.00000000000000000 ) ) ;
#8065=DIRECTION ( 'NONE',  ( -1.000000000000000000, -0.000000000000000000, -0.000000000000000000 ) ) ;
#8066=CARTESIAN_POINT ( 'NONE',  ( 23.02398829872513986, 3.395978615688218571, 13.79999998357615532 ) ) ;
#8070=AXIS2_PLACEMENT_3D ( 'NONE', #9906, #9695, #2742 ) ;
#8072=EDGE_CURVE ( 'NONE', #17208, #18524, #2795, .T. ) ;
#8074=ADVANCED_FACE ( 'NONE', ( #13309 ), #18885, .F. ) ;
#8075=DIRECTION ( 'NONE',  ( -0.000000000000000000, -1.000000000000000000, -0.000000000000000000 ) ) ;
#8079=DIRECTION ( 'NONE',  ( 0.000000000000000000, 1.000000000000000000, -0.000000000000000000 ) ) ;
#8081=DIRECTION ( 'NONE',  ( 1.000000000000000000, 0.000000000000000000, 0.000000000000000000 ) ) ;
#8084=VERTEX_POINT ( 'NONE', #15436 ) ;
#8085=LINE ( 'NONE', #14890, #13151 ) ;
#8088=CARTESIAN_POINT ( 'NONE',  ( -4.127054932750482408, -33.43424481021354921, 68.00000000000000000 ) ) ;
#8094=ORIENTED_EDGE ( 'NONE', *, *, #12972, .F. ) ;
#8095=CARTESIAN_POINT ( 'NONE',  ( 14.71479891986436606, -52.07369784111803312, 13.50000000000000000 ) ) ;
#8096=AXIS2_PLACEMENT_3D ( 'NONE', #2247, #7194, #20842 ) ;
#8097=AXIS2_PLACEMENT_3D ( 'NONE', #19334, #14058, #5370 ) ;
#8099=ORIENTED_EDGE ( 'NONE', *, *, #7933, .F. ) ;
#8100=CARTESIAN_POINT ( 'NONE',  ( 0.000000000000000000, 51.61873716947361856, 68.00000000000000000 ) ) ;
#8101=EDGE_CURVE ( 'NONE', #20941, #7686, #1668, .T. ) ;
#8102=CARTESIAN_POINT ( 'NONE',  ( 30.67540678000428045, 63.74634676501045050, 3.500000000000000000 ) ) ;
#8104=CARTESIAN_POINT ( 'NONE',  ( -29.09616827897941249, 6.500357068115323322, 7.499999999998635758 ) ) ;
#8105=VECTOR ( 'NONE', #10982, 1000.000000000000000 ) ;
#8110=CARTESIAN_POINT ( 'NONE',  ( 0.000000000000000000, -51.61873716947361856, 68.00000000000000000 ) ) ;
#8111=DIRECTION ( 'NONE',  ( 1.000000000000000000, 0.000000000000000000, 0.000000000000000000 ) ) ;
#8115=VECTOR ( 'NONE', #4333, 1000.000000000000000 ) ;
#8117=VECTOR ( 'NONE', #8364, 1000.000000000000000 ) ;
#8119=VERTEX_POINT ( 'NONE', #109 ) ;
#8122=DIRECTION ( 'NONE',  ( -1.000000000000000000, 0.000000000000000000, 0.000000000000000000 ) ) ;
#8124=FACE_OUTER_BOUND ( 'NONE', #20855, .T. ) ;
#8127=EDGE_CURVE ( 'NONE', #8176, #8431, #19575, .T. ) ;
#8129=EDGE_CURVE ( 'NONE', #13945, #11867, #12073, .T. ) ;
#8130=CARTESIAN_POINT ( 'NONE',  ( 29.37540678000427619, -6.000000000000000000, 7.200000000000000178 ) ) ;
#8133=CIRCLE ( 'NONE', #21345, 4.351418481279133665 ) ;
#8134=LINE ( 'NONE', #21898, #10914 ) ;
#8135=VERTEX_POINT ( 'NONE', #15200 ) ;
#8136=FACE_OUTER_BOUND ( 'NONE', #3291, .T. ) ;
#8138=CARTESIAN_POINT ( 'NONE',  ( 29.13662752439705272, 0.000000000000000000, 7.200000000000000178 ) ) ;
#8139=ORIENTED_EDGE ( 'NONE', *, *, #17435, .T. ) ;
#8144=CARTESIAN_POINT ( 'NONE',  ( -29.50000000000002132, 69.00000000000000000, 1.500000000000000000 ) ) ;
#8146=EDGE_CURVE ( 'NONE', #11890, #19753, #15098, .T. ) ;
#8147=ORIENTED_EDGE ( 'NONE', *, *, #8536, .F. ) ;
#8149=CARTESIAN_POINT ( 'NONE',  ( 29.20000000000002061, 68.70000000000001705, 0.000000000000000000 ) ) ;
#8150=CIRCLE ( 'NONE', #14192, 0.5000000000000004441 ) ;
#8151=AXIS2_PLACEMENT_3D ( 'NONE', #8959, #21054, #5732 ) ;
#8153=DIRECTION ( 'NONE',  ( -0.000000000000000000, -0.000000000000000000, 1.000000000000000000 ) ) ;
#8156=CIRCLE ( 'NONE', #975, 0.5000000000000004441 ) ;
#8159=CARTESIAN_POINT ( 'NONE',  ( 30.37540678000427619, 0.000000000000000000, 7.200000000000000178 ) ) ;
#8160=EDGE_CURVE ( 'NONE', #5001, #4119, #21380, .T. ) ;
#8163=CARTESIAN_POINT ( 'NONE',  ( -9.641460742840918030, 32.61873716947361856, 68.00000000000000000 ) ) ;
#8165=CYLINDRICAL_SURFACE ( 'NONE', #15535, 0.2999999999999999334 ) ;
#8167=CARTESIAN_POINT ( 'NONE',  ( 0.000000000000000000, 67.24634676501045760, 7.799999999999999822 ) ) ;
#8172=CARTESIAN_POINT ( 'NONE',  ( 15.21174975910707161, 42.31054587065082728, 68.50000000000000000 ) ) ;
#8174=ORIENTED_EDGE ( 'NONE', *, *, #473, .T. ) ;
#8175=VECTOR ( 'NONE', #14844, 1000.000000000000000 ) ;
#8176=VERTEX_POINT ( 'NONE', #18571 ) ;
#8177=CIRCLE ( 'NONE', #14217, 0.2999999999999999334 ) ;
#8178=CARTESIAN_POINT ( 'NONE',  ( 25.37540678000427263, 67.24634676501045760, 13.19999999999999929 ) ) ;
#8179=AXIS2_PLACEMENT_3D ( 'NONE', #19319, #2299, #20891 ) ;
#8182=CYLINDRICAL_SURFACE ( 'NONE', #3137, 0.2999999999999999334 ) ;
#8184=AXIS2_PLACEMENT_3D ( 'NONE', #12932, #16690, #10107 ) ;
#8186=CARTESIAN_POINT ( 'NONE',  ( 29.13662752439705272, 0.000000000000000000, 0.3000000000000016542 ) ) ;
#8188=AXIS2_PLACEMENT_3D ( 'NONE', #20687, #20792, #17198 ) ;
#8189=ADVANCED_FACE ( 'NONE', ( #5495 ), #3801, .T. ) ;
#8192=EDGE_CURVE ( 'NONE', #19749, #712, #14299, .T. ) ;
#8194=CARTESIAN_POINT ( 'NONE',  ( 15.21174975910707161, 52.11873716947361856, 68.00000000000000000 ) ) ;
#8195=DIRECTION ( 'NONE',  ( 0.000000000000000000, 0.000000000000000000, 1.000000000000000000 ) ) ;
#8196=EDGE_LOOP ( 'NONE', ( #19542, #18337, #21643, #8554 ) ) ;
#8197=FACE_OUTER_BOUND ( 'NONE', #15423, .T. ) ;
#8198=VERTEX_POINT ( 'NONE', #12504 ) ;
#8199=CARTESIAN_POINT ( 'NONE',  ( -29.50000000000002132, -2.473451120191013430, -150.0833101980363722 ) ) ;
#8201=EDGE_LOOP ( 'NONE', ( #20417, #18208, #13522, #14404 ) ) ;
#8203=CIRCLE ( 'NONE', #6054, 0.2999999999999999334 ) ;
#8207=EDGE_CURVE ( 'NONE', #18926, #11864, #17797, .T. ) ;
#8209=EDGE_CURVE ( 'NONE', #8021, #1401, #7088, .T. ) ;
#8210=ORIENTED_EDGE ( 'NONE', *, *, #18754, .F. ) ;
#8211=CARTESIAN_POINT ( 'NONE',  ( 14.98281217233416562, -51.83338592095527275, 13.50000000000000000 ) ) ;
#8212=DIRECTION ( 'NONE',  ( -0.000000000000000000, -1.000000000000000000, -0.000000000000000000 ) ) ;
#8213=ORIENTED_EDGE ( 'NONE', *, *, #2256, .F. ) ;
#8215=AXIS2_PLACEMENT_3D ( 'NONE', #21250, #17982, #18092 ) ;
#8216=VECTOR ( 'NONE', #6024, 1000.000000000000000 ) ;
#8217=CARTESIAN_POINT ( 'NONE',  ( -23.26560317237337117, 3.297643262788010787, 13.49417356369015231 ) ) ;
#8218=CARTESIAN_POINT ( 'NONE',  ( -17.95292532278785913, -34.11873716947361856, 42.50000000000000711 ) ) ;
#8219=DIRECTION ( 'NONE',  ( -1.000000000000000000, 0.000000000000000000, 0.000000000000000000 ) ) ;
#8221=ORIENTED_EDGE ( 'NONE', *, *, #12398, .F. ) ;
#8222=ORIENTED_EDGE ( 'NONE', *, *, #22026, .T. ) ;
#8223=ORIENTED_EDGE ( 'NONE', *, *, #7856, .F. ) ;
#8227=DIRECTION ( 'NONE',  ( 0.000000000000000000, -1.000000000000000000, 0.000000000000000000 ) ) ;
#8229=CIRCLE ( 'NONE', #18584, 0.5000000000000004441 ) ;
#8230=ORIENTED_EDGE ( 'NONE', *, *, #386, .F. ) ;
#8232=EDGE_CURVE ( 'NONE', #14977, #4119, #8949, .T. ) ;
#8233=DIRECTION ( 'NONE',  ( 1.000000000000000000, 0.000000000000000000, 0.000000000000000000 ) ) ;
#8234=DIRECTION ( 'NONE',  ( -0.000000000000000000, 1.000000000000000000, 0.000000000000000000 ) ) ;
#8239=CARTESIAN_POINT ( 'NONE',  ( -28.87540678000427619, -63.74634676501045050, 7.799999999999999822 ) ) ;
#8240=ORIENTED_EDGE ( 'NONE', *, *, #19691, .T. ) ;
#8244=AXIS2_PLACEMENT_3D ( 'NONE', #13333, #16918, #10109 ) ;
#8245=DIRECTION ( 'NONE',  ( 0.000000000000000000, 0.000000000000000000, -1.000000000000000000 ) ) ;
#8246=LINE ( 'NONE', #4670, #11647 ) ;
#8247=EDGE_CURVE ( 'NONE', #6694, #6444, #17431, .T. ) ;
#8248=VERTEX_POINT ( 'NONE', #15751 ) ;
#8254=EDGE_CURVE ( 'NONE', #4674, #7580, #16355, .T. ) ;
#8255=ORIENTED_EDGE ( 'NONE', *, *, #5256, .T. ) ;
#8257=ORIENTED_EDGE ( 'NONE', *, *, #11258, .F. ) ;
#8258=CARTESIAN_POINT ( 'NONE',  ( 15.21174975910705918, -52.11873716947361856, 14.00000000000000000 ) ) ;
#8259=DIRECTION ( 'NONE',  ( 0.000000000000000000, -0.000000000000000000, -1.000000000000000000 ) ) ;
#8260=CYLINDRICAL_SURFACE ( 'NONE', #8498, 0.2999999999999999334 ) ;
#8261=VECTOR ( 'NONE', #3357, 1000.000000000000000 ) ;
#8263=DIRECTION ( 'NONE',  ( 0.000000000000000000, 1.000000000000000000, 0.000000000000000000 ) ) ;
#8264=CARTESIAN_POINT ( 'NONE',  ( -23.02398829872513986, 5.683640910026983128, 13.79999999999999893 ) ) ;
#8266=LINE ( 'NONE', #8159, #17110 ) ;
#8267=CARTESIAN_POINT ( 'NONE',  ( -17.92752199202934094, -38.74634676501045760, 13.79999999999999893 ) ) ;
#8268=FACE_OUTER_BOUND ( 'NONE', #13875, .T. ) ;
#8269=B_SPLINE_CURVE_WITH_KNOTS ( 'NONE', 3,
 ( #15682, #20954, #3841, #8983, #19161, #5642, #458, #20849 ),
 .UNSPECIFIED., .F., .F.,
 ( 4, 2, 2, 4 ),
 ( 0.000000000000000000, 0.0002421094859592866821, 0.0003631642289389202518, 0.0004842189719185537944 ),
 .UNSPECIFIED. ) ;
#8270=ORIENTED_EDGE ( 'NONE', *, *, #15, .F. ) ;
#8272=ADVANCED_FACE ( 'NONE', ( #1891 ), #20817, .T. ) ;
#8273=VECTOR ( 'NONE', #7658, 1000.000000000000000 ) ;
#8274=CARTESIAN_POINT ( 'NONE',  ( 27.37540678000427974, -10.94079601157914716, 42.50000000000000000 ) ) ;
#8276=CYLINDRICAL_SURFACE ( 'NONE', #16718, 0.5000000000000004441 ) ;
#8278=EDGE_LOOP ( 'NONE', ( #10896, #20061, #19850, #16225 ) ) ;
#8280=DIRECTION ( 'NONE',  ( 0.000000000000000000, 0.000000000000000000, 1.000000000000000000 ) ) ;
#8283=AXIS2_PLACEMENT_3D ( 'NONE', #21646, #18155, #9435 ) ;
#8284=ADVANCED_FACE ( 'NONE', ( #3923 ), #22105, .F. ) ;
#8286=EDGE_CURVE ( 'NONE', #5550, #2970, #7383, .T. ) ;
#8290=AXIS2_PLACEMENT_3D ( 'NONE', #3728, #7309, #12207 ) ;
#8292=CARTESIAN_POINT ( 'NONE',  ( 0.000000000000000000, -68.70000000000001705, 0.000000000000000000 ) ) ;
#8294=FACE_OUTER_BOUND ( 'NONE', #2847, .T. ) ;
#8298=CARTESIAN_POINT ( 'NONE',  ( -15.00250675241655429, -51.98442790175712247, 13.86082508289638149 ) ) ;
#8299=DIRECTION ( 'NONE',  ( 0.000000000000000000, 1.000000000000000000, 0.000000000000000000 ) ) ;
#8302=DIRECTION ( 'NONE',  ( -0.000000000000000000, -1.000000000000000000, -0.000000000000000000 ) ) ;
#8307=ORIENTED_EDGE ( 'NONE', *, *, #4762, .T. ) ;
#8310=ORIENTED_EDGE ( 'NONE', *, *, #34, .F. ) ;
#8311=EDGE_CURVE ( 'NONE', #8671, #17214, #13146, .T. ) ;
#8312=ADVANCED_FACE ( 'NONE', ( #16424 ), #21701, .T. ) ;
#8319=ORIENTED_EDGE ( 'NONE', *, *, #1561, .F. ) ;
#8321=CARTESIAN_POINT ( 'NONE',  ( -23.02398829872513986, 3.418849134688105362, 13.52821124852824397 ) ) ;
#8323=DIRECTION ( 'NONE',  ( 0.000000000000000000, 0.000000000000000000, 1.000000000000000000 ) ) ;
#8325=EDGE_CURVE ( 'NONE', #10005, #8815, #21369, .T. ) ;
#8328=ORIENTED_EDGE ( 'NONE', *, *, #3509, .F. ) ;
#8329=VERTEX_POINT ( 'NONE', #14630 ) ;
#8330=DIRECTION ( 'NONE',  ( -0.000000000000000000, -0.000000000000000000, -1.000000000000000000 ) ) ;
#8331=CARTESIAN_POINT ( 'NONE',  ( -29.50000000000002842, -2.473451120191013874, 0.2503166595423103602 ) ) ;
#8334=ORIENTED_EDGE ( 'NONE', *, *, #10937, .F. ) ;
#8335=DIRECTION ( 'NONE',  ( 1.000000000000000000, -0.000000000000000000, 0.000000000000000000 ) ) ;
#8336=DIRECTION ( 'NONE',  ( -0.000000000000000000, -0.000000000000000000, 1.000000000000000000 ) ) ;
#8342=PLANE ( 'NONE',  #7593 ) ;
#8346=DIRECTION ( 'NONE',  ( 1.000000000000000000, -0.000000000000000000, 0.000000000000000000 ) ) ;
#8348=EDGE_LOOP ( 'NONE', ( #12721, #11125, #17615, #18645 ) ) ;
#8349=FACE_OUTER_BOUND ( 'NONE', #2366, .T. ) ;
#8353=ORIENTED_EDGE ( 'NONE', *, *, #18893, .T. ) ;
#8355=DIRECTION ( 'NONE',  ( 0.000000000000000000, 1.000000000000000000, 0.000000000000000000 ) ) ;
#8358=EDGE_LOOP ( 'NONE', ( #11540, #22010, #9702, #5368 ) ) ;
#8360=CARTESIAN_POINT ( 'NONE',  ( -25.37540678000427263, 67.54634676501045476, 7.799999999999999822 ) ) ;
#8363=CARTESIAN_POINT ( 'NONE',  ( 0.000000000000000000, 0.000000000000000000, 13.50000000000000000 ) ) ;
#8364=DIRECTION ( 'NONE',  ( 1.000000000000000000, 0.000000000000000000, -0.000000000000000000 ) ) ;
#8368=CARTESIAN_POINT ( 'NONE',  ( 0.000000000000000000, -67.24634676501045760, 7.799999999999999822 ) ) ;
#8373=ORIENTED_EDGE ( 'NONE', *, *, #7761, .F. ) ;
#8375=AXIS2_PLACEMENT_3D ( 'NONE', #8576, #8452, #20104 ) ;
#8376=ADVANCED_FACE ( 'NONE', ( #18095 ), #7944, .T. ) ;
#8377=DIRECTION ( 'NONE',  ( -0.000000000000000000, -0.000000000000000000, 1.000000000000000000 ) ) ;
#8378=VERTEX_POINT ( 'NONE', #11057 ) ;
#8380=LINE ( 'NONE', #20478, #13858 ) ;
#8381=VERTEX_POINT ( 'NONE', #2449 ) ;
#8382=ORIENTED_EDGE ( 'NONE', *, *, #3776, .F. ) ;
#8385=EDGE_CURVE ( 'NONE', #9771, #4245, #19449, .T. ) ;
#8387=CARTESIAN_POINT ( 'NONE',  ( -29.33570773061603276, 2.657594995084290979, 0.02220324760240992637 ) ) ;
#8389=DIRECTION ( 'NONE',  ( 0.000000000000000000, 0.000000000000000000, 1.000000000000000000 ) ) ;
#8390=DIRECTION ( 'NONE',  ( 0.000000000000000000, -1.000000000000000000, 0.000000000000000000 ) ) ;
#8395=CARTESIAN_POINT ( 'NONE',  ( 27.37540678000427619, 5.683640910026986681, 13.79999999999999893 ) ) ;
#8396=EDGE_CURVE ( 'NONE', #21935, #4820, #4249, .T. ) ;
#8398=CIRCLE ( 'NONE', #11242, 0.2999999999999999334 ) ;
#8399=CIRCLE ( 'NONE', #6981, 0.2999999999999999334 ) ;
#8402=DIRECTION ( 'NONE',  ( 0.000000000000000000, 0.000000000000000000, 1.000000000000000000 ) ) ;
#8403=LINE ( 'NONE', #15215, #8521 ) ;
#8407=ORIENTED_EDGE ( 'NONE', *, *, #6811, .T. ) ;
#8409=VERTEX_POINT ( 'NONE', #7704 ) ;
#8413=ORIENTED_EDGE ( 'NONE', *, *, #20857, .F. ) ;
#8414=DIRECTION ( 'NONE',  ( -1.000000000000000000, 0.000000000000000000, 0.000000000000000000 ) ) ;
#8415=CARTESIAN_POINT ( 'NONE',  ( 28.57540678000427548, -6.776800961815481195, 13.50000000000000000 ) ) ;
#8416=PLANE ( 'NONE',  #19970 ) ;
#8418=CARTESIAN_POINT ( 'NONE',  ( 15.95292532278785913, -50.11873716947361856, 13.79999999999999893 ) ) ;
#8420=CARTESIAN_POINT ( 'NONE',  ( -23.29441641503749949, 3.413540866333673485, 13.50000000000000000 ) ) ;
#8423=CARTESIAN_POINT ( 'NONE',  ( -23.04273156199908357, 2.261510999192738680, 13.19999999999999929 ) ) ;
#8428=TOROIDAL_SURFACE ( 'NONE', #20938, 3.200000000000003286, 0.2999999999999999889 ) ;
#8429=VERTEX_POINT ( 'NONE', #5132 ) ;
#8431=VERTEX_POINT ( 'NONE', #20352 ) ;
#8432=CARTESIAN_POINT ( 'NONE',  ( 29.13662752439705272, 0.000000000000000000, 1.500000000000001332 ) ) ;
#8435=CARTESIAN_POINT ( 'NONE',  ( 15.05356361075494576, -52.05881965543596834, 13.87239990309209325 ) ) ;
#8439=ORIENTED_EDGE ( 'NONE', *, *, #21949, .F. ) ;
#8440=LINE ( 'NONE', #8565, #3966 ) ;
#8441=AXIS2_PLACEMENT_3D ( 'NONE', #5799, #9032, #12681 ) ;
#8442=AXIS2_PLACEMENT_3D ( 'NONE', #10351, #4977, #6563 ) ;
#8444=CYLINDRICAL_SURFACE ( 'NONE', #13566, 0.5000000000000004441 ) ;
#8446=CARTESIAN_POINT ( 'NONE',  ( -15.95292532278785913, -52.11873716947361856, 68.00000000000000000 ) ) ;
#8448=VERTEX_POINT ( 'NONE', #22155 ) ;
#8450=DIRECTION ( 'NONE',  ( 0.000000000000000000, 0.000000000000000000, -1.000000000000000000 ) ) ;
#8452=DIRECTION ( 'NONE',  ( 0.000000000000000000, 0.000000000000000000, 1.000000000000000000 ) ) ;
#8453=DIRECTION ( 'NONE',  ( 0.000000000000000000, 0.000000000000000000, 1.000000000000000000 ) ) ;
#8458=DIRECTION ( 'NONE',  ( 0.000000000000000000, 0.000000000000000000, -1.000000000000000000 ) ) ;
#8459=CIRCLE ( 'NONE', #13462, 0.2999999999999999334 ) ;
#8460=ORIENTED_EDGE ( 'NONE', *, *, #11793, .T. ) ;
#8462=VECTOR ( 'NONE', #1974, 1000.000000000000000 ) ;
#8463=ORIENTED_EDGE ( 'NONE', *, *, #17932, .F. ) ;
#8464=CIRCLE ( 'NONE', #578, 0.5000000000000004441 ) ;
#8468=DIRECTION ( 'NONE',  ( 1.000000000000000000, -0.000000000000000000, -0.000000000000000000 ) ) ;
#8471=VERTEX_POINT ( 'NONE', #3226 ) ;
#8472=CARTESIAN_POINT ( 'NONE',  ( 29.13662752439705272, 0.000000000000000000, 3.500000000000000000 ) ) ;
#8474=ORIENTED_EDGE ( 'NONE', *, *, #16946, .T. ) ;
#8475=DIRECTION ( 'NONE',  ( 0.000000000000000000, 0.000000000000000000, -1.000000000000000000 ) ) ;
#8476=VECTOR ( 'NONE', #14900, 1000.000000000000000 ) ;
#8477=EDGE_CURVE ( 'NONE', #9810, #13749, #13393, .T. ) ;
#8479=EDGE_CURVE ( 'NONE', #6786, #14923, #8266, .T. ) ;
#8481=VECTOR ( 'NONE', #15589, 1000.000000000000000 ) ;
#8484=VERTEX_POINT ( 'NONE', #15179 ) ;
#8485=CARTESIAN_POINT ( 'NONE',  ( 23.02398829872513986, 2.877181859310994572, 13.71509684061243561 ) ) ;
#8486=LINE ( 'NONE', #15305, #7118 ) ;
#8487=AXIS2_PLACEMENT_3D ( 'NONE', #5601, #7170, #10514 ) ;
#8490=FACE_OUTER_BOUND ( 'NONE', #59, .T. ) ;
#8493=AXIS2_PLACEMENT_3D ( 'NONE', #9814, #1291, #7927 ) ;
#8495=ORIENTED_EDGE ( 'NONE', *, *, #14486, .F. ) ;
#8498=AXIS2_PLACEMENT_3D ( 'NONE', #20124, #9610, #20018 ) ;
#8501=VERTEX_POINT ( 'NONE', #8606 ) ;
#8502=LINE ( 'NONE', #6395, #9189 ) ;
#8504=ORIENTED_EDGE ( 'NONE', *, *, #7608, .F. ) ;
#8507=ORIENTED_EDGE ( 'NONE', *, *, #1844, .T. ) ;
#8508=CARTESIAN_POINT ( 'NONE',  ( -29.26826100586361079, 2.729427995260352624, 5.717472393966525748E-18 ) ) ;
#8509=EDGE_CURVE ( 'NONE', #11265, #15626, #3336, .T. ) ;
#8510=DIRECTION ( 'NONE',  ( -2.832483164223434527E-16, -1.000000000000000000, 0.000000000000000000 ) ) ;
#8511=DIRECTION ( 'NONE',  ( 1.000000000000000000, 0.000000000000000000, 0.000000000000000000 ) ) ;
#8512=CARTESIAN_POINT ( 'NONE',  ( -14.96174975910705207, -51.61873716947361856, 68.25000000000000000 ) ) ;
#8513=AXIS2_PLACEMENT_3D ( 'NONE', #8917, #393, #7469 ) ;
#8515=LINE ( 'NONE', #5048, #14619 ) ;
#8516=LINE ( 'NONE', #4933, #20421 ) ;
#8518=CARTESIAN_POINT ( 'NONE',  ( -14.71432566477614579, -52.07267295633236870, 13.50000000000000000 ) ) ;
#8520=CIRCLE ( 'NONE', #13507, 0.5000000000000004441 ) ;
#8521=VECTOR ( 'NONE', #10198, 1000.000000000000000 ) ;
#8523=LINE ( 'NONE', #21953, #6349 ) ;
#8527=ORIENTED_EDGE ( 'NONE', *, *, #7110, .T. ) ;
#8531=AXIS2_PLACEMENT_3D ( 'NONE', #2708, #19730, #16571 ) ;
#8532=AXIS2_PLACEMENT_3D ( 'NONE', #22087, #8212, #3048 ) ;
#8533=ORIENTED_EDGE ( 'NONE', *, *, #20142, .F. ) ;
#8535=ORIENTED_EDGE ( 'NONE', *, *, #21945, .F. ) ;
#8536=EDGE_CURVE ( 'NONE', #5223, #2108, #20022, .T. ) ;
#8537=CIRCLE ( 'NONE', #8188, 0.2500000000000002220 ) ;
#8542=FACE_OUTER_BOUND ( 'NONE', #8201, .T. ) ;
#8543=DIRECTION ( 'NONE',  ( -1.000000000000000000, 0.000000000000000000, 0.000000000000000000 ) ) ;
#8544=CARTESIAN_POINT ( 'NONE',  ( 23.02398829872513986, 3.002822642624742855, 13.75715867294163886 ) ) ;
#8545=CARTESIAN_POINT ( 'NONE',  ( 23.02398829872513986, -2.157133568460768647, 42.50000000000000000 ) ) ;
#8547=CARTESIAN_POINT ( 'NONE',  ( 0.000000000000000000, 67.54634676501045476, 7.500000000000000000 ) ) ;
#8549=AXIS2_PLACEMENT_3D ( 'NONE', #1194, #9946, #16868 ) ;
#8550=CARTESIAN_POINT ( 'NONE',  ( -29.50000000000002132, -69.00000000000000000, -150.0833101980363722 ) ) ;
#8551=CARTESIAN_POINT ( 'NONE',  ( 14.71479891163412468, -52.07369784467163498, 13.50000000000000178 ) ) ;
#8552=EDGE_CURVE ( 'NONE', #18926, #17256, #11496, .T. ) ;
#8553=CARTESIAN_POINT ( 'NONE',  ( 29.13662752439705272, 0.000000000000000000, 3.799999999999999822 ) ) ;
#8554=ORIENTED_EDGE ( 'NONE', *, *, #700, .T. ) ;
#8557=AXIS2_PLACEMENT_3D ( 'NONE', #655, #5499, #3808 ) ;
#8558=CARTESIAN_POINT ( 'NONE',  ( -29.26826100586361079, -2.729427995260352624, 5.717472393966525748E-18 ) ) ;
#8559=ORIENTED_EDGE ( 'NONE', *, *, #1162, .F. ) ;
#8560=LINE ( 'NONE', #5198, #5596 ) ;
#8561=EDGE_CURVE ( 'NONE', #2467, #21435, #16744, .T. ) ;
#8563=EDGE_CURVE ( 'NONE', #21160, #11864, #8486, .T. ) ;
#8565=CARTESIAN_POINT ( 'NONE',  ( 9.141460742840918030, -33.93424481021354921, 68.50000000000000000 ) ) ;
#8569=CIRCLE ( 'NONE', #4633, 0.2999999999999999334 ) ;
#8570=( BOUNDED_SURFACE ( )  B_SPLINE_SURFACE ( 3, 2, ( 
 ( #17705, #12555, #16366 ),
 ( #19400, #2715, #6099 ),
 ( #5872, #4072, #2608 ),
 ( #21309, #18035, #10889 ),
 ( #1040, #7440, #11002 ),
 ( #12654, #2385, #12776 ),
 ( #21427, #14248, #19735 ),
 ( #16024, #7769, #9436 ) ),
 .UNSPECIFIED., .F., .F., .F. ) 
 B_SPLINE_SURFACE_WITH_KNOTS ( ( 4, 2, 2, 4 ),
 ( 3, 3 ),
 ( -1.707618421664669484E-18, 0.0004639257417130348096, 0.0006958886125695531088, 0.0009278514834260713539 ),
 ( 0.000000000000000000, 1.000000000000000000 ),
 .UNSPECIFIED. ) 
 GEOMETRIC_REPRESENTATION_ITEM ( )  RATIONAL_B_SPLINE_SURFACE ( (
 ( 1.000000000000000000, 0.6123724356957929160, 1.000000000000000000),
 ( 1.000000000000000000, 0.6127303078017206639, 1.000000000000000000),
 ( 1.000000000000000000, 0.6153173443167760936, 1.000000000000000000),
 ( 1.000000000000000000, 0.6312737947278392880, 1.000000000000000000),
 ( 1.000000000000000000, 0.6386439821288609764, 1.000000000000000000),
 ( 1.000000000000000000, 0.6635434878155272997, 1.000000000000000000),
 ( 1.000000000000000000, 0.6820474757551056033, 1.000000000000000000),
 ( 1.000000000000000000, 0.7071067811865495711, 1.000000000000000000) ) ) 
 REPRESENTATION_ITEM ( '' )  SURFACE ( )  );
#8571=DIRECTION ( 'NONE',  ( -1.000000000000000000, 0.000000000000000000, 0.000000000000000000 ) ) ;
#8572=ORIENTED_EDGE ( 'NONE', *, *, #2347, .F. ) ;
#8573=CARTESIAN_POINT ( 'NONE',  ( -15.95292532278785913, 34.11873716947361856, 68.50000000000000000 ) ) ;
#8574=FACE_OUTER_BOUND ( 'NONE', #5560, .T. ) ;
#8575=LINE ( 'NONE', #20433, #21775 ) ;
#8576=CARTESIAN_POINT ( 'NONE',  ( -3.127054932750481964, 32.61873716947361856, 68.00000000000000000 ) ) ;
#8578=ORIENTED_EDGE ( 'NONE', *, *, #4846, .T. ) ;
#8579=DIRECTION ( 'NONE',  ( -1.000000000000000000, 0.000000000000000000, -0.000000000000000000 ) ) ;
#8580=ADVANCED_FACE ( 'NONE', ( #4904 ), #13939, .F. ) ;
#8581=ORIENTED_EDGE ( 'NONE', *, *, #15428, .T. ) ;
#8582=CARTESIAN_POINT ( 'NONE',  ( -23.32398829872514057, -3.528912754968629439, 13.79999999999999893 ) ) ;
#8588=DIRECTION ( 'NONE',  ( 0.000000000000000000, -0.000000000000000000, -1.000000000000000000 ) ) ;
#8590=DIRECTION ( 'NONE',  ( -0.000000000000000000, -0.000000000000000000, 1.000000000000000000 ) ) ;
#8592=ORIENTED_EDGE ( 'NONE', *, *, #18143, .T. ) ;
#8596=DIRECTION ( 'NONE',  ( 1.000000000000000000, 0.000000000000000000, 0.000000000000000000 ) ) ;
#8597=EDGE_CURVE ( 'NONE', #7888, #16845, #7471, .T. ) ;
#8601=CARTESIAN_POINT ( 'NONE',  ( -9.641460742840918030, 32.61873716947361856, 68.50000000000000000 ) ) ;
#8605=CARTESIAN_POINT ( 'NONE',  ( 23.02398829872513986, 2.624244922594596741, 13.63058196926744792 ) ) ;
#8606=CARTESIAN_POINT ( 'NONE',  ( -23.32398829872514057, -5.683640910026986681, 13.50000000000000000 ) ) ;
#8607=AXIS2_PLACEMENT_3D ( 'NONE', #2678, #15990, #14422 ) ;
#8608=AXIS2_PLACEMENT_3D ( 'NONE', #8100, #1245, #9548 ) ;
#8611=VERTEX_POINT ( 'NONE', #9135 ) ;
#8613=FACE_OUTER_BOUND ( 'NONE', #15012, .T. ) ;
#8614=ORIENTED_EDGE ( 'NONE', *, *, #3826, .T. ) ;
#8616=EDGE_CURVE ( 'NONE', #7158, #17039, #88, .T. ) ;
#8618=EDGE_CURVE ( 'NONE', #21526, #14178, #14155, .T. ) ;
#8619=ORIENTED_EDGE ( 'NONE', *, *, #13873, .T. ) ;
#8620=CARTESIAN_POINT ( 'NONE',  ( -26.61833302554978786, -9.663695060508651125, 13.50000000000000000 ) ) ;
#8623=ORIENTED_EDGE ( 'NONE', *, *, #7683, .F. ) ;
#8624=EDGE_CURVE ( 'NONE', #17966, #16219, #21047, .T. ) ;
#8625=LINE ( 'NONE', #16151, #10253 ) ;
#8629=DIRECTION ( 'NONE',  ( 0.000000000000000000, 0.000000000000000000, -1.000000000000000000 ) ) ;
#8631=PLANE ( 'NONE',  #12271 ) ;
#8632=CARTESIAN_POINT ( 'NONE',  ( -15.21174975910705385, -52.00603550409435627, 13.50000000000000000 ) ) ;
#8633=VERTEX_POINT ( 'NONE', #7147 ) ;
#8634=EDGE_CURVE ( 'NONE', #1458, #5468, #8537, .T. ) ;
#8637=CIRCLE ( 'NONE', #752, 1.000000000000000888 ) ;
#8638=DIRECTION ( 'NONE',  ( -0.000000000000000000, -0.000000000000000000, -1.000000000000000000 ) ) ;
#8642=ORIENTED_EDGE ( 'NONE', *, *, #5619, .T. ) ;
#8643=FACE_OUTER_BOUND ( 'NONE', #5968, .T. ) ;
#8646=EDGE_LOOP ( 'NONE', ( #13023, #17334, #20722, #15523 ) ) ;
#8648=FILL_AREA_STYLE_COLOUR ( '', #20375 ) ;
#8649=VERTEX_POINT ( 'NONE', #2088 ) ;
#8650=ORIENTED_EDGE ( 'NONE', *, *, #6241, .T. ) ;
#8655=PLANE ( 'NONE',  #13164 ) ;
#8657=AXIS2_PLACEMENT_3D ( 'NONE', #2145, #4155, #7418 ) ;
#8658=DIRECTION ( 'NONE',  ( 0.000000000000000000, 0.000000000000000000, 1.000000000000000000 ) ) ;
#8659=AXIS2_PLACEMENT_3D ( 'NONE', #1991, #12274, #10411 ) ;
#8660=DIRECTION ( 'NONE',  ( 0.000000000000000000, 1.000000000000000000, 0.000000000000000000 ) ) ;
#8661=CARTESIAN_POINT ( 'NONE',  ( 23.08512718742729319, -2.485300415563061360, 13.35387015137019873 ) ) ;
#8662=DIRECTION ( 'NONE',  ( -1.000000000000000000, 0.000000000000000000, -0.000000000000000000 ) ) ;
#8670=DIRECTION ( 'NONE',  ( -0.000000000000000000, -1.000000000000000000, -0.000000000000000000 ) ) ;
#8671=VERTEX_POINT ( 'NONE', #13828 ) ;
#8672=B_SPLINE_CURVE_WITH_KNOTS ( 'NONE', 3,
 ( #6440, #11880, #20080, #1248, #8104, #16697 ),
 .UNSPECIFIED., .F., .F.,
 ( 4, 2, 4 ),
 ( 0.000000000000000000, 0.0002343433793794306779, 0.0004686867587588613559 ),
 .UNSPECIFIED. ) ;
#8673=VECTOR ( 'NONE', #1197, 1000.000000000000000 ) ;
#8679=ORIENTED_EDGE ( 'NONE', *, *, #16015, .F. ) ;
#8681=CIRCLE ( 'NONE', #9045, 0.2999999999999999334 ) ;
#8682=DIRECTION ( 'NONE',  ( 0.000000000000000000, 0.000000000000000000, 1.000000000000000000 ) ) ;
#8683=CYLINDRICAL_SURFACE ( 'NONE', #21171, 0.5000000000000004441 ) ;
#8685=DIRECTION ( 'NONE',  ( -0.000000000000000000, 1.000000000000000000, -0.000000000000000000 ) ) ;
#8687=DIRECTION ( 'NONE',  ( -0.000000000000000000, 0.000000000000000000, -1.000000000000000000 ) ) ;
#8690=ORIENTED_EDGE ( 'NONE', *, *, #11376, .F. ) ;
#8691=DIRECTION ( 'NONE',  ( 0.000000000000000000, -0.000000000000000000, -1.000000000000000000 ) ) ;
#8692=CARTESIAN_POINT ( 'NONE',  ( 0.000000000000000000, -38.74634676501045760, 42.50000000000000000 ) ) ;
#8695=VERTEX_POINT ( 'NONE', #505 ) ;
#8698=FACE_OUTER_BOUND ( 'NONE', #10695, .T. ) ;
#8700=ADVANCED_FACE ( 'NONE', ( #16396 ), #10668, .F. ) ;
#8702=B_SPLINE_CURVE_WITH_KNOTS ( 'NONE', 3,
 ( #14860, #16646, #18338, #13528, #13301, #3014, #9844, #1325 ),
 .UNSPECIFIED., .F., .F.,
 ( 4, 2, 2, 4 ),
 ( 3.388890645555526065E-18, 0.0001462888802157341281, 0.0002925777604314648951, 0.0005851555208629193820 ),
 .UNSPECIFIED. ) ;
#8704=FACE_OUTER_BOUND ( 'NONE', #15762, .T. ) ;
#8707=DIRECTION ( 'NONE',  ( -0.000000000000000000, -0.000000000000000000, -1.000000000000000000 ) ) ;
#8708=DIRECTION ( 'NONE',  ( 0.000000000000000000, -1.000000000000000000, 0.000000000000000000 ) ) ;
#8711=ORIENTED_EDGE ( 'NONE', *, *, #10865, .T. ) ;
#8712=CARTESIAN_POINT ( 'NONE',  ( 25.37540678000427263, -63.74634676501045050, 7.500000000000000000 ) ) ;
#8718=EDGE_CURVE ( 'NONE', #12023, #21932, #15652, .T. ) ;
#8720=CARTESIAN_POINT ( 'NONE',  ( 29.37540678000427619, 5.000000000000000000, 7.200000000000000178 ) ) ;
#8722=CARTESIAN_POINT ( 'NONE',  ( 32.20000000000001705, 71.00000000000001421, 1.800000000000000044 ) ) ;
#8723=EDGE_CURVE ( 'NONE', #13403, #16971, #1005, .T. ) ;
#8726=EDGE_CURVE ( 'NONE', #15395, #11905, #12434, .T. ) ;
#8727=EDGE_LOOP ( 'NONE', ( #13446, #1941, #13352, #19804 ) ) ;
#8728=CARTESIAN_POINT ( 'NONE',  ( -29.20000000000002061, 2.799282752659324025, 0.000000000000000000 ) ) ;
#8735=DIRECTION ( 'NONE',  ( 0.000000000000000000, 1.000000000000000000, 0.000000000000000000 ) ) ;
#8737=CARTESIAN_POINT ( 'NONE',  ( -31.50000000000002132, -72.00000000000001421, 3.200000000000000178 ) ) ;
#8738=EDGE_CURVE ( 'NONE', #22039, #21353, #2527, .T. ) ;
#8739=ORIENTED_EDGE ( 'NONE', *, *, #1344, .F. ) ;
#8740=CARTESIAN_POINT ( 'NONE',  ( 15.95292532278785913, -50.11873716947361856, 13.50000000000000000 ) ) ;
#8742=DIRECTION ( 'NONE',  ( -1.000000000000000000, -0.000000000000000000, -0.000000000000000000 ) ) ;
#8744=ORIENTED_EDGE ( 'NONE', *, *, #12875, .F. ) ;
#8747=VERTEX_POINT ( 'NONE', #18063 ) ;
#8748=CARTESIAN_POINT ( 'NONE',  ( 23.02398829872514341, -2.279831973701432535, 13.43058255391203382 ) ) ;
#8749=EDGE_LOOP ( 'NONE', ( #7181, #1226, #14833, #12544 ) ) ;
#8750=ORIENTED_EDGE ( 'NONE', *, *, #7022, .F. ) ;
#8752=FACE_OUTER_BOUND ( 'NONE', #20877, .T. ) ;
#8753=FACE_OUTER_BOUND ( 'NONE', #3427, .T. ) ;
#8754=EDGE_CURVE ( 'NONE', #7977, #7598, #10002, .T. ) ;
#8757=DIRECTION ( 'NONE',  ( 0.000000000000000000, -1.000000000000000000, 0.000000000000000000 ) ) ;
#8760=DIRECTION ( 'NONE',  ( -0.000000000000000000, -0.000000000000000000, 1.000000000000000000 ) ) ;
#8761=CARTESIAN_POINT ( 'NONE',  ( 15.95292532278785913, 50.11873716947361856, 13.99999999999999822 ) ) ;
#8762=CARTESIAN_POINT ( 'NONE',  ( 0.000000000000000000, -32.11873716947361856, 42.50000000000000711 ) ) ;
#8763=ORIENTED_EDGE ( 'NONE', *, *, #16402, .F. ) ;
#8770=VECTOR ( 'NONE', #10723, 1000.000000000000000 ) ;
#8772=EDGE_CURVE ( 'NONE', #14847, #17942, #8203, .T. ) ;
#8773=DIRECTION ( 'NONE',  ( 0.000000000000000000, 0.000000000000000000, 1.000000000000000000 ) ) ;
#8778=DIRECTION ( 'NONE',  ( 0.000000000000000000, 0.000000000000000000, 1.000000000000000000 ) ) ;
#8782=DIRECTION ( 'NONE',  ( -0.000000000000000000, -0.000000000000000000, 1.000000000000000000 ) ) ;
#8783=VECTOR ( 'NONE', #17713, 1000.000000000000000 ) ;
#8786=ORIENTED_EDGE ( 'NONE', *, *, #17275, .T. ) ;
#8789=CARTESIAN_POINT ( 'NONE',  ( 9.641460742840918030, 32.93424481021354921, 68.50000000000000000 ) ) ;
#8790=VERTEX_POINT ( 'NONE', #2633 ) ;
#8792=ORIENTED_EDGE ( 'NONE', *, *, #1405, .F. ) ;
#8793=CARTESIAN_POINT ( 'NONE',  ( 17.95292532278785913, -34.11873716947361856, 42.50000000000000711 ) ) ;
#8796=CIRCLE ( 'NONE', #8441, 5.000000000000004441 ) ;
#8798=DIRECTION ( 'NONE',  ( -0.000000000000000000, 0.000000000000000000, 1.000000000000000000 ) ) ;
#8801=CARTESIAN_POINT ( 'NONE',  ( -28.87540678000427619, 63.74634676501045050, 7.799999999999999822 ) ) ;
#8802=VECTOR ( 'NONE', #10532, 1000.000000000000000 ) ;
#8804=ORIENTED_EDGE ( 'NONE', *, *, #8616, .T. ) ;
#8805=CARTESIAN_POINT ( 'NONE',  ( -23.29450335057350330, -3.413880037201929341, 13.50000000000000178 ) ) ;
#8806=ADVANCED_FACE ( 'NONE', ( #1067 ), #7801, .T. ) ;
#8808=CARTESIAN_POINT ( 'NONE',  ( 15.21174975910707161, 41.81054587065082728, 68.50000000000000000 ) ) ;
#8810=ORIENTED_EDGE ( 'NONE', *, *, #2502, .T. ) ;
#8811=CARTESIAN_POINT ( 'NONE',  ( 23.02398829872513986, 2.279872152331596347, 13.43073953831959066 ) ) ;
#8813=FACE_OUTER_BOUND ( 'NONE', #5144, .T. ) ;
#8815=VERTEX_POINT ( 'NONE', #21458 ) ;
#8816=CIRCLE ( 'NONE', #1659, 0.3000000000000016542 ) ;
#8817=CIRCLE ( 'NONE', #12363, 0.2999999999999999334 ) ;
#8819=CIRCLE ( 'NONE', #16292, 4.700000000000002842 ) ;
#8821=CYLINDRICAL_SURFACE ( 'NONE', #21325, 0.2999999999999999334 ) ;
#8823=VECTOR ( 'NONE', #3261, 1000.000000000000000 ) ;
#8824=ORIENTED_EDGE ( 'NONE', *, *, #18932, .T. ) ;
#8825=DIRECTION ( 'NONE',  ( 0.000000000000000000, 0.000000000000000000, -1.000000000000000000 ) ) ;
#8827=LINE ( 'NONE', #19229, #7083 ) ;
#8829=ORIENTED_EDGE ( 'NONE', *, *, #4834, .T. ) ;
#8830=AXIS2_PLACEMENT_3D ( 'NONE', #9347, #10706, #19524 ) ;
#8832=VECTOR ( 'NONE', #19564, 1000.000000000000000 ) ;
#8834=CARTESIAN_POINT ( 'NONE',  ( 15.95292532278785913, 34.11873716947361856, 68.00000000000000000 ) ) ;
#8836=AXIS2_PLACEMENT_3D ( 'NONE', #11806, #20668, #72 ) ;
#8837=CYLINDRICAL_SURFACE ( 'NONE', #12202, 0.3000000000000016542 ) ;
#8841=CARTESIAN_POINT ( 'NONE',  ( 15.21174975910705918, 52.39333383871510108, 13.50000000000000000 ) ) ;
#8842=DIRECTION ( 'NONE',  ( 1.000000000000000000, 0.000000000000000000, 0.000000000000000000 ) ) ;
#8843=CARTESIAN_POINT ( 'NONE',  ( 23.32398829872514057, 2.157133568460765538, 7.500000000000000000 ) ) ;
#8845=AXIS2_PLACEMENT_3D ( 'NONE', #10952, #12400, #15763 ) ;
#8846=VERTEX_POINT ( 'NONE', #13255 ) ;
#8851=VECTOR ( 'NONE', #2511, 1000.000000000000000 ) ;
#8863=ORIENTED_EDGE ( 'NONE', *, *, #11828, .T. ) ;
#8865=CYLINDRICAL_SURFACE ( 'NONE', #15910, 0.2999999999999999334 ) ;
#8868=AXIS2_PLACEMENT_3D ( 'NONE', #4927, #16777, #5154 ) ;
#8874=CARTESIAN_POINT ( 'NONE',  ( 23.04709339880124475, -2.285361808764056590, 13.25160309052396279 ) ) ;
#8875=DIRECTION ( 'NONE',  ( 0.000000000000000000, 0.000000000000000000, 1.000000000000000000 ) ) ;
#8876=LINE ( 'NONE', #5526, #410 ) ;
#8877=VECTOR ( 'NONE', #12911, 1000.000000000000000 ) ;
#8880=EDGE_LOOP ( 'NONE', ( #21856, #21960, #3733 ) ) ;
#8883=ADVANCED_FACE ( 'NONE', ( #1505 ), #21996, .F. ) ;
#8884=ORIENTED_EDGE ( 'NONE', *, *, #8477, .T. ) ;
#8885=ADVANCED_FACE ( 'NONE', ( #10025 ), #2973, .F. ) ;
#8886=AXIS2_PLACEMENT_3D ( 'NONE', #7287, #10752, #19039 ) ;
#8888=FACE_OUTER_BOUND ( 'NONE', #11254, .T. ) ;
#8891=VERTEX_POINT ( 'NONE', #16598 ) ;
#8892=DIRECTION ( 'NONE',  ( 0.000000000000000000, 0.000000000000000000, 1.000000000000000000 ) ) ;
#8893=CARTESIAN_POINT ( 'NONE',  ( -15.95292532278785913, -32.61873716947361856, 68.00000000000000000 ) ) ;
#8894=LINE ( 'NONE', #2272, #5426 ) ;
#8896=PLANE ( 'NONE',  #15692 ) ;
#8898=CARTESIAN_POINT ( 'NONE',  ( -30.07540678000427548, 0.000000000000000000, 7.500000000000000000 ) ) ;
#8899=VECTOR ( 'NONE', #4463, 1000.000000000000000 ) ;
#8901=CARTESIAN_POINT ( 'NONE',  ( 28.82574430125643516, -6.542305536751587880, 13.37088755551135932 ) ) ;
#8902=DIRECTION ( 'NONE',  ( 0.000000000000000000, 1.000000000000000000, 0.000000000000000000 ) ) ;
#8904=VERTEX_POINT ( 'NONE', #15266 ) ;
#8905=B_SPLINE_CURVE_WITH_KNOTS ( 'NONE', 3,
 ( #2864, #15935, #618, #12097, #20732, #3614, #18943, #8544, #7089, #13886 ),
 .UNSPECIFIED., .F., .F.,
 ( 4, 2, 2, 2, 4 ),
 ( 0.000000000000000000, 0.0001998921237118762633, 0.0003997842474237525267, 0.0007995684948475050534, 0.001599136989695010540 ),
 .UNSPECIFIED. ) ;
#8908=CARTESIAN_POINT ( 'NONE',  ( -25.37540678000429395, -38.74634676501045760, 42.50000000000000000 ) ) ;
#8911=DIRECTION ( 'NONE',  ( -0.000000000000000000, 1.000000000000000000, 0.000000000000000000 ) ) ;
#8912=CIRCLE ( 'NONE', #2114, 0.2999999999999999334 ) ;
#8913=ORIENTED_EDGE ( 'NONE', *, *, #18318, .T. ) ;
#8915=AXIS2_PLACEMENT_3D ( 'NONE', #19355, #429, #5388 ) ;
#8917=CARTESIAN_POINT ( 'NONE',  ( -15.95292532278785913, 52.39333383871510108, 13.79999999999999893 ) ) ;
#8924=CARTESIAN_POINT ( 'NONE',  ( 28.87540678000427619, 6.494748934539263274, 13.19999999999999929 ) ) ;
#8926=ORIENTED_EDGE ( 'NONE', *, *, #973, .T. ) ;
#8927=ADVANCED_FACE ( 'NONE', ( #15149 ), #16722, .T. ) ;
#8928=CARTESIAN_POINT ( 'NONE',  ( -30.37540678000427619, -6.000000000000000000, 7.200000000000000178 ) ) ;
#8930=VERTEX_POINT ( 'NONE', #6675 ) ;
#8932=CIRCLE ( 'NONE', #1408, 0.2999999999999999334 ) ;
#8934=CIRCLE ( 'NONE', #6814, 0.5000000000000004441 ) ;
#8935=FACE_OUTER_BOUND ( 'NONE', #6341, .T. ) ;
#8936=ORIENTED_EDGE ( 'NONE', *, *, #13166, .T. ) ;
#8938=EDGE_CURVE ( 'NONE', #9117, #16813, #20315, .T. ) ;
#8940=LINE ( 'NONE', #414, #20675 ) ;
#8942=VERTEX_POINT ( 'NONE', #1274 ) ;
#8946=CARTESIAN_POINT ( 'NONE',  ( -25.37540678000429040, -36.74634676501047181, 13.50000000000000000 ) ) ;
#8948=DIRECTION ( 'NONE',  ( 0.000000000000000000, 1.000000000000000000, 0.000000000000000000 ) ) ;
#8949=LINE ( 'NONE', #15528, #4935 ) ;
#8950=EDGE_CURVE ( 'NONE', #18406, #3824, #5714, .T. ) ;
#8951=CARTESIAN_POINT ( 'NONE',  ( 4.127054932750481520, -32.93424481021354921, 7.321391277662001151 ) ) ;
#8952=ORIENTED_EDGE ( 'NONE', *, *, #11402, .T. ) ;
#8956=CIRCLE ( 'NONE', #11797, 0.3000000000000016542 ) ;
#8959=CARTESIAN_POINT ( 'NONE',  ( 29.13662752439705272, 0.000000000000000000, 13.50000000000000000 ) ) ;
#8961=VERTEX_POINT ( 'NONE', #21894 ) ;
#8962=EDGE_CURVE ( 'NONE', #4728, #18442, #6571, .T. ) ;
#8964=ORIENTED_EDGE ( 'NONE', *, *, #17962, .F. ) ;
#8965=CARTESIAN_POINT ( 'NONE',  ( -15.21174975910705207, -52.11873716947361856, 14.00000000000000000 ) ) ;
#8966=EDGE_CURVE ( 'NONE', #4986, #5889, #1025, .T. ) ;
#8967=SHAPE_DEFINITION_REPRESENTATION ( #18772, #9407 ) ;
#8968=ORIENTED_EDGE ( 'NONE', *, *, #10134, .T. ) ;
#8969=CARTESIAN_POINT ( 'NONE',  ( 23.02398829872513630, -2.681487294389184761, 13.50129116665758389 ) ) ;
#8970=ORIENTED_EDGE ( 'NONE', *, *, #11921, .F. ) ;
#8971=ORIENTED_EDGE ( 'NONE', *, *, #14020, .F. ) ;
#8972=CARTESIAN_POINT ( 'NONE',  ( 15.21174975910707161, -52.11873716947361856, 68.00000000000000000 ) ) ;
#8974=EDGE_CURVE ( 'NONE', #4820, #17759, #19992, .T. ) ;
#8975=CARTESIAN_POINT ( 'NONE',  ( -29.13662752439705272, 0.000000000000000000, 1.500000000000001332 ) ) ;
#8976=AXIS2_PLACEMENT_3D ( 'NONE', #19897, #12937, #1297 ) ;
#8982=TOROIDAL_SURFACE ( 'NONE', #7255, 1.000000000000000000, 0.5000000000000000000 ) ;
#8983=CARTESIAN_POINT ( 'NONE',  ( -14.98825539710680488, -51.95771298364783775, 13.85621828746129225 ) ) ;
#8986=ORIENTED_EDGE ( 'NONE', *, *, #17904, .F. ) ;
#8988=CARTESIAN_POINT ( 'NONE',  ( -9.141460742840918030, 32.93424481021354921, 68.50000000000000000 ) ) ;
#8989=ADVANCED_FACE ( 'NONE', ( #18855 ), #3530, .T. ) ;
#8992=ORIENTED_EDGE ( 'NONE', *, *, #2405, .F. ) ;
#8993=AXIS2_PLACEMENT_3D ( 'NONE', #3662, #5462, #15606 ) ;
#8995=ORIENTED_EDGE ( 'NONE', *, *, #10693, .F. ) ;
#8996=AXIS2_PLACEMENT_3D ( 'NONE', #10561, #9776, #16576 ) ;
#8997=AXIS2_PLACEMENT_3D ( 'NONE', #5894, #13012, #19867 ) ;
#8998=AXIS2_PLACEMENT_3D ( 'NONE', #18949, #11984, #133 ) ;
#9003=CARTESIAN_POINT ( 'NONE',  ( 27.37540678000427619, 7.754037881813018962E-15, 42.50000000000000000 ) ) ;
#9005=CARTESIAN_POINT ( 'NONE',  ( 8.641460742840918030, -32.93424481021354921, 68.50000000000000000 ) ) ;
#9007=CARTESIAN_POINT ( 'NONE',  ( -14.75141514895149442, 52.14252005765843734, 13.49999999999999822 ) ) ;
#9008=DIRECTION ( 'NONE',  ( -0.000000000000000000, -0.000000000000000000, -1.000000000000000000 ) ) ;
#9010=CARTESIAN_POINT ( 'NONE',  ( -27.67540678000428400, -10.94079601157914716, 13.50000000000000000 ) ) ;
#9012=CARTESIAN_POINT ( 'NONE',  ( -25.37540678000427263, -67.24634676501045760, 7.799999999999999822 ) ) ;
#9014=ORIENTED_EDGE ( 'NONE', *, *, #2620, .T. ) ;
#9015=ORIENTED_EDGE ( 'NONE', *, *, #14502, .T. ) ;
#9017=DIRECTION ( 'NONE',  ( -0.000000000000000000, -0.000000000000000000, 1.000000000000000000 ) ) ;
#9026=ORIENTED_EDGE ( 'NONE', *, *, #16477, .F. ) ;
#9028=CARTESIAN_POINT ( 'NONE',  ( 17.45292532278785913, 38.74634676501045760, 14.00000000000000000 ) ) ;
#9029=DIRECTION ( 'NONE',  ( -0.000000000000000000, 1.000000000000000000, -0.000000000000000000 ) ) ;
#9031=EDGE_LOOP ( 'NONE', ( #8642, #1206, #21966, #9145 ) ) ;
#9032=DIRECTION ( 'NONE',  ( -0.000000000000000000, -0.000000000000000000, -1.000000000000000000 ) ) ;
#9035=CARTESIAN_POINT ( 'NONE',  ( 23.32398829872514057, -3.528912754968634768, 13.79999999999999893 ) ) ;
#9038=EDGE_CURVE ( 'NONE', #5864, #17139, #21416, .T. ) ;
#9039=CARTESIAN_POINT ( 'NONE',  ( 3.627054932750481964, -32.61873716947361856, 42.50000000000000000 ) ) ;
#9040=EDGE_LOOP ( 'NONE', ( #5103, #665, #1224, #13743 ) ) ;
#9045=AXIS2_PLACEMENT_3D ( 'NONE', #9885, #16365, #21541 ) ;
#9047=CYLINDRICAL_SURFACE ( 'NONE', #2056, 5.000000000000000888 ) ;
#9048=ORIENTED_EDGE ( 'NONE', *, *, #6572, .F. ) ;
#9050=ADVANCED_FACE ( 'NONE', ( #8574 ), #5207, .T. ) ;
#9053=CYLINDRICAL_SURFACE ( 'NONE', #16866, 0.5000000000000004441 ) ;
#9054=DIRECTION ( 'NONE',  ( 1.000000000000000000, 0.000000000000000000, 0.000000000000000000 ) ) ;
#9055=EDGE_CURVE ( 'NONE', #1152, #13238, #3552, .T. ) ;
#9057=ORIENTED_EDGE ( 'NONE', *, *, #15335, .F. ) ;
#9058=FACE_OUTER_BOUND ( 'NONE', #16197, .T. ) ;
#9061=ORIENTED_EDGE ( 'NONE', *, *, #10429, .F. ) ;
#9064=ORIENTED_EDGE ( 'NONE', *, *, #21659, .F. ) ;
#9067=ADVANCED_FACE ( 'NONE', ( #55 ), #15805, .F. ) ;
#9069=VERTEX_POINT ( 'NONE', #6905 ) ;
#9070=CARTESIAN_POINT ( 'NONE',  ( 17.95292532278785913, 34.11873716947361856, 13.49999999999999822 ) ) ;
#9071=EDGE_LOOP ( 'NONE', ( #1605, #18149, #17747, #9064, #2316 ) ) ;
#9072=CARTESIAN_POINT ( 'NONE',  ( -15.21174975910705207, 51.61873716947361856, 68.50000000000000000 ) ) ;
#9076=EDGE_CURVE ( 'NONE', #21509, #12543, #16023, .T. ) ;
#9077=CARTESIAN_POINT ( 'NONE',  ( -4.127054932750482408, 33.43424481021354921, 68.00000000000000000 ) ) ;
#9081=ADVANCED_FACE ( 'NONE', ( #10241 ), #2164, .T. ) ;
#9083=CARTESIAN_POINT ( 'NONE',  ( 28.82574430125643516, 6.542305536751587880, 13.37088755551135932 ) ) ;
#9084=CIRCLE ( 'NONE', #21956, 0.2999999999999999334 ) ;
#9085=DIRECTION ( 'NONE',  ( 1.000000000000000000, 0.000000000000000000, 0.000000000000000000 ) ) ;
#9089=CARTESIAN_POINT ( 'NONE',  ( -28.57540678000427548, 6.776800961815481195, 13.50000000000000000 ) ) ;
#9092=ADVANCED_FACE ( 'NONE', ( #13689 ), #3640, .F. ) ;
#9098=EDGE_CURVE ( 'NONE', #16245, #13276, #21514, .T. ) ;
#9099=CARTESIAN_POINT ( 'NONE',  ( -15.95292532278785913, -52.39333383871510108, 13.50000000000000000 ) ) ;
#9102=EDGE_CURVE ( 'NONE', #15132, #14744, #9985, .T. ) ;
#9104=DIRECTION ( 'NONE',  ( 1.000000000000000000, 0.000000000000000000, 0.000000000000000000 ) ) ;
#9106=CARTESIAN_POINT ( 'NONE',  ( 31.50000000000002132, 72.00000000000001421, 1.800000000000000044 ) ) ;
#9109=DIRECTION ( 'NONE',  ( -1.000000000000000000, 0.000000000000000000, 0.000000000000000000 ) ) ;
#9110=DIRECTION ( 'NONE',  ( -0.000000000000000000, -0.000000000000000000, -1.000000000000000000 ) ) ;
#9111=ORIENTED_EDGE ( 'NONE', *, *, #21821, .F. ) ;
#9113=ORIENTED_EDGE ( 'NONE', *, *, #6329, .F. ) ;
#9114=CARTESIAN_POINT ( 'NONE',  ( 25.37540678000427263, 63.74634676501045050, 3.500000000000000000 ) ) ;
#9115=DIRECTION ( 'NONE',  ( 0.000000000000000000, 0.000000000000000000, 1.000000000000000000 ) ) ;
#9116=ADVANCED_FACE ( 'NONE', ( #7861 ), #1217, .T. ) ;
#9117=VERTEX_POINT ( 'NONE', #585 ) ;
#9119=ADVANCED_FACE ( 'NONE', ( #12553 ), #17703, .T. ) ;
#9120=ORIENTED_EDGE ( 'NONE', *, *, #17066, .T. ) ;
#9122=AXIS2_PLACEMENT_3D ( 'NONE', #7613, #6267, #14405 ) ;
#9123=CARTESIAN_POINT ( 'NONE',  ( 0.000000000000000000, 68.74634676501045760, 7.500000000000000000 ) ) ;
#9125=CARTESIAN_POINT ( 'NONE',  ( -29.13662752439705272, 0.000000000000000000, 0.3000000000000016542 ) ) ;
#9126=CARTESIAN_POINT ( 'NONE',  ( 0.000000000000000000, -52.11873716947361856, 68.00000000000000000 ) ) ;
#9128=DIRECTION ( 'NONE',  ( -0.000000000000000000, -0.000000000000000000, -1.000000000000000000 ) ) ;
#9130=DIRECTION ( 'NONE',  ( -1.000000000000000000, -0.000000000000000000, -0.000000000000000000 ) ) ;
#9135=CARTESIAN_POINT ( 'NONE',  ( 15.21174975910707161, -52.11873716947361856, 68.00000000000000000 ) ) ;
#9137=CARTESIAN_POINT ( 'NONE',  ( -23.05525514579169410, -2.329474921856953706, 13.28656140283153952 ) ) ;
#9138=ORIENTED_EDGE ( 'NONE', *, *, #4293, .F. ) ;
#9139=CARTESIAN_POINT ( 'NONE',  ( -15.21174975910705207, 52.39333383871510108, 13.50000000000000000 ) ) ;
#9140=CARTESIAN_POINT ( 'NONE',  ( 14.96174975910705918, -32.10873716947361345, 13.79999999999999893 ) ) ;
#9145=ORIENTED_EDGE ( 'NONE', *, *, #7308, .T. ) ;
#9146=DIRECTION ( 'NONE',  ( 1.000000000000000000, 0.000000000000000000, 0.000000000000000000 ) ) ;
#9148=ORIENTED_EDGE ( 'NONE', *, *, #16153, .F. ) ;
#9149=AXIS2_PLACEMENT_3D ( 'NONE', #7445, #12995, #14250 ) ;
#9150=TOROIDAL_SURFACE ( 'NONE', #11289, 1.000000000000000000, 0.5000000000000000000 ) ;
#9152=EDGE_CURVE ( 'NONE', #8329, #7598, #16549, .T. ) ;
#9161=LINE ( 'NONE', #17983, #7604 ) ;
#9164=ORIENTED_EDGE ( 'NONE', *, *, #11363, .F. ) ;
#9165=CARTESIAN_POINT ( 'NONE',  ( 14.66174975910705847, 51.76873716947361714, 13.50000000000000000 ) ) ;
#9166=AXIS2_PLACEMENT_3D ( 'NONE', #10127, #6568, #22117 ) ;
#9169=ORIENTED_EDGE ( 'NONE', *, *, #22079, .F. ) ;
#9171=ORIENTED_EDGE ( 'NONE', *, *, #6871, .T. ) ;
#9173=VECTOR ( 'NONE', #10462, 1000.000000000000000 ) ;
#9174=ORIENTED_EDGE ( 'NONE', *, *, #13350, .T. ) ;
#9175=VECTOR ( 'NONE', #14546, 1000.000000000000000 ) ;
#9176=DIRECTION ( 'NONE',  ( 1.000000000000000000, 0.000000000000000000, 0.000000000000000000 ) ) ;
#9180=EDGE_CURVE ( 'NONE', #170, #7349, #4261, .T. ) ;
#9183=VERTEX_POINT ( 'NONE', #3973 ) ;
#9185=CARTESIAN_POINT ( 'NONE',  ( 0.000000000000000000, 52.39333383871510108, 13.79999999999999893 ) ) ;
#9188=VECTOR ( 'NONE', #4288, 1000.000000000000000 ) ;
#9189=VECTOR ( 'NONE', #11945, 1000.000000000000000 ) ;
#9191=PLANE ( 'NONE',  #20051 ) ;
#9192=CARTESIAN_POINT ( 'NONE',  ( 28.87540678000427619, 6.494748934539263274, 13.19999999999999929 ) ) ;
#9195=DIRECTION ( 'NONE',  ( -2.546383084002652634E-16, -0.000000000000000000, -1.000000000000000000 ) ) ;
#9196=EDGE_CURVE ( 'NONE', #13259, #15133, #6438, .T. ) ;
#9198=AXIS2_PLACEMENT_3D ( 'NONE', #13868, #213, #3813 ) ;
#9200=CARTESIAN_POINT ( 'NONE',  ( 17.93704824106378837, 38.74634676501045760, 13.87500000000000000 ) ) ;
#9201=EDGE_CURVE ( 'NONE', #15111, #13985, #6184, .T. ) ;
#9202=ORIENTED_EDGE ( 'NONE', *, *, #11546, .F. ) ;
#9203=AXIS2_PLACEMENT_3D ( 'NONE', #11259, #7936, #2994 ) ;
#9204=AXIS2_PLACEMENT_3D ( 'NONE', #2446, #14071, #12385 ) ;
#9210=CARTESIAN_POINT ( 'NONE',  ( -15.21174975910705207, 51.86873716947361856, 13.05380965755523448 ) ) ;
#9211=CARTESIAN_POINT ( 'NONE',  ( 0.000000000000000000, 38.74634676501045760, 42.50000000000000000 ) ) ;
#9212=ORIENTED_EDGE ( 'NONE', *, *, #18939, .F. ) ;
#9214=CARTESIAN_POINT ( 'NONE',  ( 23.05525514579170121, 2.329474921856955039, 13.28656140283153420 ) ) ;
#9215=EDGE_CURVE ( 'NONE', #19777, #961, #21079, .T. ) ;
#9217=DIRECTION ( 'NONE',  ( 1.000000000000000000, 0.000000000000000000, 0.000000000000000000 ) ) ;
#9219=CIRCLE ( 'NONE', #9951, 1.499999999999999556 ) ;
#9221=CARTESIAN_POINT ( 'NONE',  ( -23.02398829872513986, 3.528912754968630328, 13.79999999999999893 ) ) ;
#9228=VERTEX_POINT ( 'NONE', #16449 ) ;
#9230=ORIENTED_EDGE ( 'NONE', *, *, #805, .T. ) ;
#9231=DIRECTION ( 'NONE',  ( -0.000000000000000000, -0.000000000000000000, -1.000000000000000000 ) ) ;
#9234=EDGE_CURVE ( 'NONE', #16676, #15319, #13739, .T. ) ;
#9235=EDGE_LOOP ( 'NONE', ( #10372, #5175, #6777, #1430 ) ) ;
#9238=ADVANCED_FACE ( 'NONE', ( #4932 ), #339, .T. ) ;
#9243=CARTESIAN_POINT ( 'NONE',  ( -29.50000000000002132, 69.00000000000000000, -150.0833101980363722 ) ) ;
#9247=CARTESIAN_POINT ( 'NONE',  ( 27.37540678000427974, -5.683640910026986681, 42.50000000000000000 ) ) ;
#9248=FACE_OUTER_BOUND ( 'NONE', #19168, .T. ) ;
#9249=ORIENTED_EDGE ( 'NONE', *, *, #20063, .F. ) ;
#9251=EDGE_CURVE ( 'NONE', #20337, #9771, #5724, .T. ) ;
#9254=ORIENTED_EDGE ( 'NONE', *, *, #2853, .F. ) ;
#9258=CARTESIAN_POINT ( 'NONE',  ( -15.21174975910705207, 52.11873716947361856, 14.00000000000000000 ) ) ;
#9259=AXIS2_PLACEMENT_3D ( 'NONE', #10130, #3641, #17269 ) ;
#9260=ORIENTED_EDGE ( 'NONE', *, *, #9520, .T. ) ;
#9262=CARTESIAN_POINT ( 'NONE',  ( 17.93704824106378837, 50.11873716947361856, 13.87499999999999822 ) ) ;
#9266=EDGE_CURVE ( 'NONE', #20894, #6809, #6790, .T. ) ;
#9267=VERTEX_POINT ( 'NONE', #5271 ) ;
#9268=ADVANCED_FACE ( 'NONE', ( #16995 ), #20379, .T. ) ;
#9270=ORIENTED_EDGE ( 'NONE', *, *, #5557, .T. ) ;
#9274=DIRECTION ( 'NONE',  ( 0.000000000000000000, -1.000000000000000000, 0.000000000000000000 ) ) ;
#9276=AXIS2_PLACEMENT_3D ( 'NONE', #5416, #12303, #8875 ) ;
#9277=CIRCLE ( 'NONE', #6069, 1.000000000000000888 ) ;
#9278=FACE_OUTER_BOUND ( 'NONE', #14148, .T. ) ;
#9279=ORIENTED_EDGE ( 'NONE', *, *, #4365, .F. ) ;
#9280=CARTESIAN_POINT ( 'NONE',  ( -17.92752199202934094, 38.74634676501045760, 13.79999999999999893 ) ) ;
#9281=EDGE_CURVE ( 'NONE', #1657, #18203, #1038, .T. ) ;
#9283=DIRECTION ( 'NONE',  ( -0.000000000000000000, 0.000000000000000000, 1.000000000000000000 ) ) ;
#9284=DIRECTION ( 'NONE',  ( 0.000000000000000000, 0.000000000000000000, -1.000000000000000000 ) ) ;
#9286=DIRECTION ( 'NONE',  ( -0.000000000000000000, 1.000000000000000000, 0.000000000000000000 ) ) ;
#9287=ORIENTED_EDGE ( 'NONE', *, *, #328, .F. ) ;
#9292=B_SPLINE_CURVE_WITH_KNOTS ( 'NONE', 3,
 ( #13859, #15970, #20708, #12278, #17324, #1996, #19127, #428 ),
 .UNSPECIFIED., .F., .F.,
 ( 4, 2, 2, 4 ),
 ( 0.000000000000000000, 0.0001479575850294295161, 0.0002959151700588590322, 0.0005918303401177112339 ),
 .UNSPECIFIED. ) ;
#9298=EDGE_LOOP ( 'NONE', ( #16319, #21133, #12445, #16013 ) ) ;
#9299=LINE ( 'NONE', #9072, #9304 ) ;
#9300=DIRECTION ( 'NONE',  ( 0.000000000000000000, -1.000000000000000000, 0.000000000000000000 ) ) ;
#9301=CARTESIAN_POINT ( 'NONE',  ( 25.37540678000427263, 63.74634676501045050, 3.799999999999999822 ) ) ;
#9302=CARTESIAN_POINT ( 'NONE',  ( -28.87540678000427619, -63.74634676501045050, 13.50000000000000000 ) ) ;
#9303=CARTESIAN_POINT ( 'NONE',  ( -31.50000000000002132, 71.70000000000001705, 3.500000000000000000 ) ) ;
#9304=VECTOR ( 'NONE', #18007, 1000.000000000000000 ) ;
#9308=DIRECTION ( 'NONE',  ( -0.000000000000000000, 1.000000000000000000, -0.000000000000000000 ) ) ;
#9309=EDGE_CURVE ( 'NONE', #16076, #21435, #8569, .T. ) ;
#9314=CARTESIAN_POINT ( 'NONE',  ( 23.02398829872514341, -5.683640910026986681, 13.79999999999999893 ) ) ;
#9316=ORIENTED_EDGE ( 'NONE', *, *, #10937, .T. ) ;
#9317=CIRCLE ( 'NONE', #21127, 0.5000000000000004441 ) ;
#9320=CARTESIAN_POINT ( 'NONE',  ( 14.75227361498200551, -52.14371094787964722, 13.50000000000000000 ) ) ;
#9322=ORIENTED_EDGE ( 'NONE', *, *, #5591, .T. ) ;
#9323=FACE_BOUND ( 'NONE', #2292, .T. ) ;
#9324=EDGE_CURVE ( 'NONE', #21509, #16219, #18456, .T. ) ;
#9325=CARTESIAN_POINT ( 'NONE',  ( -32.50000000000002132, 72.00000000000001421, 1.800000000000000044 ) ) ;
#9327=CARTESIAN_POINT ( 'NONE',  ( -28.79994065384636315, 6.566898051583388352, 13.40260211333369256 ) ) ;
#9328=CARTESIAN_POINT ( 'NONE',  ( -23.08512718742728964, 2.485300415563057808, 13.35387015137020050 ) ) ;
#9329=ORIENTED_EDGE ( 'NONE', *, *, #15109, .T. ) ;
#9331=CIRCLE ( 'NONE', #7557, 0.3000000000000004885 ) ;
#9332=LINE ( 'NONE', #14692, #3072 ) ;
#9333=DIRECTION ( 'NONE',  ( 1.000000000000000000, 0.000000000000000000, 0.000000000000000000 ) ) ;
#9337=CARTESIAN_POINT ( 'NONE',  ( -23.02398829872513986, -2.157133568460768647, 13.19999999999999929 ) ) ;
#9341=CYLINDRICAL_SURFACE ( 'NONE', #2363, 5.000000000000004441 ) ;
#9343=VECTOR ( 'NONE', #11879, 1000.000000000000000 ) ;
#9345=ORIENTED_EDGE ( 'NONE', *, *, #1473, .T. ) ;
#9346=DIRECTION ( 'NONE',  ( 0.000000000000000000, 0.000000000000000000, 1.000000000000000000 ) ) ;
#9347=CARTESIAN_POINT ( 'NONE',  ( -9.641460742840918030, -32.61873716947361856, 68.00000000000000000 ) ) ;
#9349=DIRECTION ( 'NONE',  ( 3.052134192567367925E-16, 1.000000000000000000, 0.000000000000000000 ) ) ;
#9350=FACE_OUTER_BOUND ( 'NONE', #362, .T. ) ;
#9352=ORIENTED_EDGE ( 'NONE', *, *, #15368, .F. ) ;
#9353=CARTESIAN_POINT ( 'NONE',  ( 17.45292532278785913, 0.000000000000000000, 14.00000000000000000 ) ) ;
#9354=CARTESIAN_POINT ( 'NONE',  ( 25.37540678000427263, 66.94634676501046044, 13.19999999999999929 ) ) ;
#9355=ADVANCED_FACE ( 'NONE', ( #8294 ), #11744, .T. ) ;
#9356=EDGE_CURVE ( 'NONE', #15579, #6378, #8515, .T. ) ;
#9358=DIRECTION ( 'NONE',  ( 2.832483164223434527E-16, 1.000000000000000000, 0.000000000000000000 ) ) ;
#9359=CARTESIAN_POINT ( 'NONE',  ( -23.08502376492393182, -2.484776121502528134, 13.35369709827396534 ) ) ;
#9363=AXIS2_PLACEMENT_3D ( 'NONE', #7534, #2359, #12203 ) ;
#9370=EDGE_LOOP ( 'NONE', ( #13428, #13212, #8139, #3349 ) ) ;
#9374=ORIENTED_EDGE ( 'NONE', *, *, #21721, .T. ) ;
#9375=ADVANCED_FACE ( 'NONE', ( #6957 ), #18935, .F. ) ;
#9377=DIRECTION ( 'NONE',  ( -1.000000000000000000, 0.000000000000000000, 0.000000000000000000 ) ) ;
#9379=ORIENTED_EDGE ( 'NONE', *, *, #19863, .T. ) ;
#9381=AXIS2_PLACEMENT_3D ( 'NONE', #14353, #21099, #10890 ) ;
#9383=LINE ( 'NONE', #16184, #2947 ) ;
#9384=CARTESIAN_POINT ( 'NONE',  ( -25.37540678000427263, -63.74634676501045050, 7.200000000000000178 ) ) ;
#9385=EDGE_CURVE ( 'NONE', #13366, #14054, #20556, .T. ) ;
#9388=ORIENTED_EDGE ( 'NONE', *, *, #1699, .F. ) ;
#9389=DIRECTION ( 'NONE',  ( -0.000000000000000000, 0.000000000000000000, 1.000000000000000000 ) ) ;
#9392=DIRECTION ( 'NONE',  ( -0.000000000000000000, -0.000000000000000000, 1.000000000000000000 ) ) ;
#9393=DIRECTION ( 'NONE',  ( 0.000000000000000000, 0.000000000000000000, -1.000000000000000000 ) ) ;
#9397=CARTESIAN_POINT ( 'NONE',  ( 26.63662752439704917, 3.061616997868386099E-16, -18.50000000000000000 ) ) ;
#9399=EDGE_CURVE ( 'NONE', #1748, #1165, #8912, .T. ) ;
#9403=ADVANCED_FACE ( 'NONE', ( #9058 ), #17447, .T. ) ;
#9406=DIRECTION ( 'NONE',  ( 1.000000000000000000, 0.000000000000000000, 0.000000000000000000 ) ) ;
#9407=SHAPE_REPRESENTATION ( 'Main Body', ( #17493 ), #10355 ) ;
#9411=DIRECTION ( 'NONE',  ( 0.000000000000000000, 0.000000000000000000, -1.000000000000000000 ) ) ;
#9413=EDGE_CURVE ( 'NONE', #17690, #6786, #20360, .T. ) ;
#9418=LINE ( 'NONE', #7744, #9175 ) ;
#9420=CARTESIAN_POINT ( 'NONE',  ( -15.95292532278785913, -50.11873716947361856, 109.6002446535588319 ) ) ;
#9422=ORIENTED_EDGE ( 'NONE', *, *, #11828, .F. ) ;
#9425=VERTEX_POINT ( 'NONE', #14186 ) ;
#9431=LINE ( 'NONE', #6309, #9188 ) ;
#9432=AXIS2_PLACEMENT_3D ( 'NONE', #18130, #13315, #13648 ) ;
#9434=ORIENTED_EDGE ( 'NONE', *, *, #15259, .T. ) ;
#9435=DIRECTION ( 'NONE',  ( 1.000000000000000000, 0.000000000000000000, 0.000000000000000000 ) ) ;
#9436=CARTESIAN_POINT ( 'NONE',  ( 14.66174975910705847, 51.76873716947361004, 13.50000000000000000 ) ) ;
#9438=DIRECTION ( 'NONE',  ( 0.000000000000000000, -0.000000000000000000, -1.000000000000000000 ) ) ;
#9441=LINE ( 'NONE', #21433, #903 ) ;
#9442=EDGE_CURVE ( 'NONE', #8119, #16676, #16851, .T. ) ;
#9443=ORIENTED_EDGE ( 'NONE', *, *, #13350, .F. ) ;
#9446=DIRECTION ( 'NONE',  ( -1.000000000000000000, 0.000000000000000000, 0.000000000000000000 ) ) ;
#9447=VERTEX_POINT ( 'NONE', #17771 ) ;
#9448=CARTESIAN_POINT ( 'NONE',  ( -31.63662752439705272, 0.000000000000000000, 3.500000000000000000 ) ) ;
#9449=EDGE_CURVE ( 'NONE', #3013, #19588, #10841, .T. ) ;
#9454=CARTESIAN_POINT ( 'NONE',  ( -26.37540678000427619, 10.94079601157914539, 42.50000000000000000 ) ) ;
#9456=ORIENTED_EDGE ( 'NONE', *, *, #17977, .T. ) ;
#9458=CARTESIAN_POINT ( 'NONE',  ( 15.95292532278785913, -50.11873716947361856, 68.50000000000000000 ) ) ;
#9463=AXIS2_PLACEMENT_3D ( 'NONE', #16921, #21872, #1587 ) ;
#9464=CARTESIAN_POINT ( 'NONE',  ( -14.96174975910705207, -51.86873716947361856, 68.00000000000000000 ) ) ;
#9465=ORIENTED_EDGE ( 'NONE', *, *, #2295, .T. ) ;
#9466=CARTESIAN_POINT ( 'NONE',  ( -15.95292532278785913, -51.61873716947361856, 14.00000000000000000 ) ) ;
#9467=DIRECTION ( 'NONE',  ( -0.000000000000000000, -0.000000000000000000, -1.000000000000000000 ) ) ;
#9468=VERTEX_POINT ( 'NONE', #10517 ) ;
#9470=DIRECTION ( 'NONE',  ( 0.000000000000000000, 0.000000000000000000, -1.000000000000000000 ) ) ;
#9471=DIRECTION ( 'NONE',  ( 1.000000000000000000, -0.000000000000000000, -0.000000000000000000 ) ) ;
#9474=EDGE_CURVE ( 'NONE', #2212, #2211, #9292, .T. ) ;
#9475=EDGE_CURVE ( 'NONE', #12787, #9842, #9277, .T. ) ;
#9477=CARTESIAN_POINT ( 'NONE',  ( 29.37573593128808369, 68.87573593128806237, -5.214931150217776400E-15 ) ) ;
#9478=AXIS2_PLACEMENT_3D ( 'NONE', #21795, #6473, #5109 ) ;
#9480=CARTESIAN_POINT ( 'NONE',  ( 23.32398829872514057, 3.528912754968628551, 13.50000000000000000 ) ) ;
#9483=CARTESIAN_POINT ( 'NONE',  ( 28.57540678000427548, 6.776800961815481195, 13.50000000000000000 ) ) ;
#9485=EDGE_CURVE ( 'NONE', #1455, #2212, #15683, .T. ) ;
#9489=ORIENTED_EDGE ( 'NONE', *, *, #8232, .T. ) ;
#9492=ADVANCED_FACE ( 'NONE', ( #20213 ), #12117, .T. ) ;
#9495=CIRCLE ( 'NONE', #17361, 0.2500000000000002220 ) ;
#9496=AXIS2_PLACEMENT_3D ( 'NONE', #10469, #9008, #3866 ) ;
#9500=ORIENTED_EDGE ( 'NONE', *, *, #20132, .T. ) ;
#9502=DIRECTION ( 'NONE',  ( -0.000000000000000000, -0.000000000000000000, 1.000000000000000000 ) ) ;
#9503=ADVANCED_FACE ( 'NONE', ( #16957 ), #1409, .T. ) ;
#9505=EDGE_CURVE ( 'NONE', #5446, #8176, #11807, .T. ) ;
#9508=AXIS2_PLACEMENT_3D ( 'NONE', #15227, #11763, #18182 ) ;
#9510=ADVANCED_FACE ( 'NONE', ( #21909 ), #2859, .T. ) ;
#9512=ORIENTED_EDGE ( 'NONE', *, *, #7782, .T. ) ;
#9515=EDGE_LOOP ( 'NONE', ( #16574, #3546, #21446, #6610 ) ) ;
#9517=PLANE ( 'NONE',  #15946 ) ;
#9518=CARTESIAN_POINT ( 'NONE',  ( -9.141460742840918030, -32.93424481021354921, 68.50000000000000000 ) ) ;
#9520=EDGE_CURVE ( 'NONE', #17, #6058, #7520, .T. ) ;
#9522=CARTESIAN_POINT ( 'NONE',  ( 26.37540678000427619, 10.94079601157914539, 42.50000000000000000 ) ) ;
#9524=DIRECTION ( 'NONE',  ( -0.000000000000000000, -0.000000000000000000, -1.000000000000000000 ) ) ;
#9527=AXIS2_PLACEMENT_3D ( 'NONE', #1301, #2774, #9611 ) ;
#9528=ORIENTED_EDGE ( 'NONE', *, *, #16182, .T. ) ;
#9529=DIRECTION ( 'NONE',  ( -0.000000000000000000, -0.000000000000000000, -1.000000000000000000 ) ) ;
#9531=ORIENTED_EDGE ( 'NONE', *, *, #14394, .F. ) ;
#9532=AXIS2_PLACEMENT_3D ( 'NONE', #13112, #11209, #1032 ) ;
#9534=FACE_OUTER_BOUND ( 'NONE', #4223, .T. ) ;
#9536=EDGE_CURVE ( 'NONE', #12188, #2755, #18641, .T. ) ;
#9538=EDGE_CURVE ( 'NONE', #6564, #11436, #6922, .T. ) ;
#9539=AXIS2_PLACEMENT_3D ( 'NONE', #10354, #12003, #8233 ) ;
#9540=AXIS2_PLACEMENT_3D ( 'NONE', #18672, #11733, #9960 ) ;
#9541=AXIS2_PLACEMENT_3D ( 'NONE', #2929, #18466, #9757 ) ;
#9542=EDGE_LOOP ( 'NONE', ( #3709, #17786, #574, #19424 ) ) ;
#9543=CIRCLE ( 'NONE', #7055, 0.3000000000000003775 ) ;
#9544=CARTESIAN_POINT ( 'NONE',  ( 15.21174975910705918, -52.39333383871510108, 13.50000000000000000 ) ) ;
#9545=DIRECTION ( 'NONE',  ( -0.000000000000000000, -0.000000000000000000, -1.000000000000000000 ) ) ;
#9548=DIRECTION ( 'NONE',  ( 0.000000000000000000, 0.000000000000000000, -1.000000000000000000 ) ) ;
#9550=DIRECTION ( 'NONE',  ( 0.000000000000000000, 0.000000000000000000, 1.000000000000000000 ) ) ;
#9554=VERTEX_POINT ( 'NONE', #21802 ) ;
#9555=CARTESIAN_POINT ( 'NONE',  ( -28.87540678000427619, 63.74634676501045050, 13.50000000000000000 ) ) ;
#9557=EDGE_CURVE ( 'NONE', #225, #15133, #10261, .T. ) ;
#9558=ORIENTED_EDGE ( 'NONE', *, *, #8072, .T. ) ;
#9559=AXIS2_PLACEMENT_3D ( 'NONE', #7500, #2110, #7701 ) ;
#9561=VERTEX_POINT ( 'NONE', #8144 ) ;
#9562=VERTEX_POINT ( 'NONE', #4780 ) ;
#9563=DIRECTION ( 'NONE',  ( -0.000000000000000000, -0.000000000000000000, 1.000000000000000000 ) ) ;
#9564=DIRECTION ( 'NONE',  ( 0.000000000000000000, 0.000000000000000000, -1.000000000000000000 ) ) ;
#9568=AXIS2_PLACEMENT_3D ( 'NONE', #20086, #12898, #2725 ) ;
#9569=EDGE_CURVE ( 'NONE', #13326, #20437, #8934, .T. ) ;
#9573=FACE_OUTER_BOUND ( 'NONE', #10282, .T. ) ;
#9574=CYLINDRICAL_SURFACE ( 'NONE', #10236, 1.000000000000000888 ) ;
#9576=AXIS2_PLACEMENT_3D ( 'NONE', #12579, #19318, #723 ) ;
#9577=AXIS2_PLACEMENT_3D ( 'NONE', #10288, #4914, #1778 ) ;
#9578=DIRECTION ( 'NONE',  ( 0.000000000000000000, 0.000000000000000000, -1.000000000000000000 ) ) ;
#9579=DIRECTION ( 'NONE',  ( 0.000000000000000000, -0.000000000000000000, 1.000000000000000000 ) ) ;
#9586=CARTESIAN_POINT ( 'NONE',  ( 32.50000000000002132, -71.00000000000001421, 3.200000000000000178 ) ) ;
#9589=AXIS2_PLACEMENT_3D ( 'NONE', #11865, #6751, #11968 ) ;
#9591=AXIS2_PLACEMENT_3D ( 'NONE', #13618, #7140, #3560 ) ;
#9595=CARTESIAN_POINT ( 'NONE',  ( -23.02398829872513275, -3.262363296411949332, 13.79999999999999361 ) ) ;
#9596=ADVANCED_FACE ( 'NONE', ( #3211 ), #15165, .T. ) ;
#9597=ORIENTED_EDGE ( 'NONE', *, *, #9356, .F. ) ;
#9598=ORIENTED_EDGE ( 'NONE', *, *, #16448, .F. ) ;
#9600=DIRECTION ( 'NONE',  ( 0.000000000000000000, 1.000000000000000000, 0.000000000000000000 ) ) ;
#9602=AXIS2_PLACEMENT_3D ( 'NONE', #18709, #1817, #3382 ) ;
#9603=VERTEX_POINT ( 'NONE', #11701 ) ;
#9604=AXIS2_PLACEMENT_3D ( 'NONE', #2199, #10391, #4004 ) ;
#9606=VECTOR ( 'NONE', #13578, 1000.000000000000000 ) ;
#9607=CIRCLE ( 'NONE', #1360, 0.2999999999999999334 ) ;
#9608=AXIS2_PLACEMENT_3D ( 'NONE', #7266, #12262, #2213 ) ;
#9609=CARTESIAN_POINT ( 'NONE',  ( -15.21174975910705207, 51.86873716947361856, 68.00000000000000000 ) ) ;
#9610=DIRECTION ( 'NONE',  ( 0.000000000000000000, -1.000000000000000000, 0.000000000000000000 ) ) ;
#9611=DIRECTION ( 'NONE',  ( 0.000000000000000000, 0.000000000000000000, 1.000000000000000000 ) ) ;
#9613=DIRECTION ( 'NONE',  ( -0.000000000000000000, -0.000000000000000000, -1.000000000000000000 ) ) ;
#9619=CIRCLE ( 'NONE', #21061, 0.2999999999999999334 ) ;
#9621=ADVANCED_FACE ( 'NONE', ( #13927 ), #9654, .F. ) ;
#9623=CARTESIAN_POINT ( 'NONE',  ( -3.627054932750481964, 32.61873716947361856, 7.321391277662001151 ) ) ;
#9624=DIRECTION ( 'NONE',  ( 0.000000000000000000, -0.000000000000000000, -1.000000000000000000 ) ) ;
#9626=CIRCLE ( 'NONE', #21067, 5.000000000000004441 ) ;
#9628=ORIENTED_EDGE ( 'NONE', *, *, #1456, .F. ) ;
#9630=DIRECTION ( 'NONE',  ( 0.000000000000000000, 0.000000000000000000, -1.000000000000000000 ) ) ;
#9633=ADVANCED_FACE ( 'NONE', ( #2182 ), #15717, .T. ) ;
#9634=DIRECTION ( 'NONE',  ( -1.000000000000000000, -0.000000000000000000, -0.000000000000000000 ) ) ;
#9638=ORIENTED_EDGE ( 'NONE', *, *, #2118, .F. ) ;
#9639=CARTESIAN_POINT ( 'NONE',  ( -18.22752199202934520, -38.74634676501045760, 13.79999999999999893 ) ) ;
#9640=CARTESIAN_POINT ( 'NONE',  ( -25.37540678000427263, -68.74634676501045760, 7.200000000000000178 ) ) ;
#9642=DIRECTION ( 'NONE',  ( 1.000000000000000000, 0.000000000000000000, 0.000000000000000000 ) ) ;
#9643=PLANE ( 'NONE',  #17885 ) ;
#9645=DIRECTION ( 'NONE',  ( 0.000000000000000000, 1.000000000000000000, 0.000000000000000000 ) ) ;
#9646=EDGE_CURVE ( 'NONE', #15986, #10680, #5006, .T. ) ;
#9647=DIRECTION ( 'NONE',  ( 1.000000000000000000, 0.000000000000000000, 0.000000000000000000 ) ) ;
#9648=LINE ( 'NONE', #14772, #7321 ) ;
#9649=CIRCLE ( 'NONE', #7866, 0.6999999999999992895 ) ;
#9650=ORIENTED_EDGE ( 'NONE', *, *, #16045, .F. ) ;
#9651=DIRECTION ( 'NONE',  ( 1.000000000000000000, 0.000000000000000000, 0.000000000000000000 ) ) ;
#9652=AXIS2_PLACEMENT_3D ( 'NONE', #15641, #316, #10835 ) ;
#9653=AXIS2_PLACEMENT_3D ( 'NONE', #3840, #17478, #11881 ) ;
#9654=TOROIDAL_SURFACE ( 'NONE', #7870, 5.300000000000004263, 0.2999999999999999889 ) ;
#9662=ORIENTED_EDGE ( 'NONE', *, *, #21556, .T. ) ;
#9664=ORIENTED_EDGE ( 'NONE', *, *, #21217, .T. ) ;
#9665=ORIENTED_EDGE ( 'NONE', *, *, #2699, .T. ) ;
#9667=CIRCLE ( 'NONE', #1425, 2.000000000000000000 ) ;
#9668=LINE ( 'NONE', #19964, #8476 ) ;
#9669=AXIS2_PLACEMENT_3D ( 'NONE', #14242, #7551, #5769 ) ;
#9670=CARTESIAN_POINT ( 'NONE',  ( -25.37540678000427263, 63.74634676501045050, 3.500000000000000000 ) ) ;
#9673=EDGE_CURVE ( 'NONE', #8135, #21878, #6453, .T. ) ;
#9674=DIRECTION ( 'NONE',  ( 3.052134192567367925E-16, -1.000000000000000000, 0.000000000000000000 ) ) ;
#9675=EDGE_CURVE ( 'NONE', #17208, #15395, #17395, .T. ) ;
#9676=DIRECTION ( 'NONE',  ( 0.000000000000000000, 0.000000000000000000, 1.000000000000000000 ) ) ;
#9680=DIRECTION ( 'NONE',  ( 1.000000000000000000, -0.000000000000000000, -0.000000000000000000 ) ) ;
#9682=EDGE_LOOP ( 'NONE', ( #10450, #17835, #11306, #1565 ) ) ;
#9684=CYLINDRICAL_SURFACE ( 'NONE', #14921, 0.5000000000000004441 ) ;
#9686=LINE ( 'NONE', #17719, #2402 ) ;
#9687=VERTEX_POINT ( 'NONE', #13811 ) ;
#9693=ADVANCED_FACE ( 'NONE', ( #3757 ), #7238, .F. ) ;
#9694=CARTESIAN_POINT ( 'NONE',  ( 23.02398829872513986, -3.528912754968634768, 13.79999999999999893 ) ) ;
#9695=DIRECTION ( 'NONE',  ( 0.000000000000000000, -0.000000000000000000, -1.000000000000000000 ) ) ;
#9697=DIRECTION ( 'NONE',  ( -1.000000000000000000, -0.000000000000000000, -0.000000000000000000 ) ) ;
#9700=DIRECTION ( 'NONE',  ( 0.000000000000000000, 0.000000000000000000, 1.000000000000000000 ) ) ;
#9701=CARTESIAN_POINT ( 'NONE',  ( 0.000000000000000000, 71.70000000000001705, 1.800000000000000044 ) ) ;
#9702=ORIENTED_EDGE ( 'NONE', *, *, #6225, .T. ) ;
#9705=ADVANCED_FACE ( 'NONE', ( #3549 ), #3586, .F. ) ;
#9706=VERTEX_POINT ( 'NONE', #14135 ) ;
#9707=CARTESIAN_POINT ( 'NONE',  ( 26.61833302554978786, 9.663695060508649348, 13.50000000000000000 ) ) ;
#9708=CARTESIAN_POINT ( 'NONE',  ( -23.02398829872514696, -2.191346223869593768, 13.32987162994455232 ) ) ;
#9709=ORIENTED_EDGE ( 'NONE', *, *, #307, .F. ) ;
#9711=ORIENTED_EDGE ( 'NONE', *, *, #5367, .F. ) ;
#9713=CARTESIAN_POINT ( 'NONE',  ( 9.141460742840918030, 32.61873716947361856, 7.321391277662001151 ) ) ;
#9715=CYLINDRICAL_SURFACE ( 'NONE', #2452, 1.000000000000000888 ) ;
#9718=ORIENTED_EDGE ( 'NONE', *, *, #21673, .F. ) ;
#9719=CARTESIAN_POINT ( 'NONE',  ( 27.67540678000426269, 36.74634676501047181, 13.79999999999999893 ) ) ;
#9721=LINE ( 'NONE', #21809, #10987 ) ;
#9722=CARTESIAN_POINT ( 'NONE',  ( -23.02398829872513986, -2.279872152331584356, 13.43073953831958889 ) ) ;
#9724=EDGE_CURVE ( 'NONE', #2805, #9117, #11772, .T. ) ;
#9726=FACE_OUTER_BOUND ( 'NONE', #7799, .T. ) ;
#9729=AXIS2_PLACEMENT_3D ( 'NONE', #10004, #18834, #3510 ) ;
#9730=DIRECTION ( 'NONE',  ( -0.000000000000000000, 1.000000000000000000, 0.000000000000000000 ) ) ;
#9731=DIRECTION ( 'NONE',  ( 1.000000000000000000, 0.000000000000000000, 0.000000000000000000 ) ) ;
#9732=ORIENTED_EDGE ( 'NONE', *, *, #10048, .F. ) ;
#9734=CARTESIAN_POINT ( 'NONE',  ( 29.50000000000002132, 0.000000000000000000, -150.0833101980363722 ) ) ;
#9735=VERTEX_POINT ( 'NONE', #7459 ) ;
#9736=CARTESIAN_POINT ( 'NONE',  ( -17.45292532278785913, 34.11873716947361856, 68.50000000000000000 ) ) ;
#9741=CARTESIAN_POINT ( 'NONE',  ( 0.000000000000000000, 52.10286008774954780, 13.87500000000000000 ) ) ;
#9744=ORIENTED_EDGE ( 'NONE', *, *, #1136, .T. ) ;
#9753=DIRECTION ( 'NONE',  ( 1.000000000000000000, 0.000000000000000000, 0.000000000000000000 ) ) ;
#9754=CARTESIAN_POINT ( 'NONE',  ( 29.01849620351543280, -6.499161877189502334, 7.532606289305298297 ) ) ;
#9755=EDGE_CURVE ( 'NONE', #1923, #8135, #10577, .T. ) ;
#9756=ORIENTED_EDGE ( 'NONE', *, *, #9234, .T. ) ;
#9757=DIRECTION ( 'NONE',  ( 0.000000000000000000, 0.000000000000000000, -1.000000000000000000 ) ) ;
#9758=EDGE_LOOP ( 'NONE', ( #18360, #20796, #7106, #10265 ) ) ;
#9759=CARTESIAN_POINT ( 'NONE',  ( -26.37540678000427619, 10.94079601157914539, 13.50000000000000000 ) ) ;
#9761=ORIENTED_EDGE ( 'NONE', *, *, #10627, .F. ) ;
#9762=ORIENTED_EDGE ( 'NONE', *, *, #21477, .T. ) ;
#9767=CARTESIAN_POINT ( 'NONE',  ( 0.000000000000000000, 0.000000000000000000, 0.000000000000000000 ) ) ;
#9769=VERTEX_POINT ( 'NONE', #21552 ) ;
#9770=EDGE_CURVE ( 'NONE', #11756, #3327, #6883, .T. ) ;
#9771=VERTEX_POINT ( 'NONE', #6111 ) ;
#9772=CARTESIAN_POINT ( 'NONE',  ( -15.05469906388002777, -52.39333383871510108, 13.49999999999999822 ) ) ;
#9774=ORIENTED_EDGE ( 'NONE', *, *, #4070, .T. ) ;
#9776=DIRECTION ( 'NONE',  ( 0.000000000000000000, -1.000000000000000000, 0.000000000000000000 ) ) ;
#9779=CARTESIAN_POINT ( 'NONE',  ( -23.05541308335691042, 2.330322924046646538, 13.28711303755810214 ) ) ;
#9780=EDGE_CURVE ( 'NONE', #1350, #20894, #7665, .T. ) ;
#9784=ORIENTED_EDGE ( 'NONE', *, *, #15854, .F. ) ;
#9785=FACE_OUTER_BOUND ( 'NONE', #18379, .T. ) ;
#9787=ORIENTED_EDGE ( 'NONE', *, *, #20246, .F. ) ;
#9789=EDGE_CURVE ( 'NONE', #20854, #17559, #12668, .T. ) ;
#9791=VERTEX_POINT ( 'NONE', #930 ) ;
#9793=CARTESIAN_POINT ( 'NONE',  ( -30.37540678000427619, 6.000000000000000000, 7.200000000000000178 ) ) ;
#9797=ORIENTED_EDGE ( 'NONE', *, *, #13247, .T. ) ;
#9803=VERTEX_POINT ( 'NONE', #14697 ) ;
#9804=CARTESIAN_POINT ( 'NONE',  ( -25.37540678000427263, -67.54634676501045476, 7.799999999999999822 ) ) ;
#9805=CARTESIAN_POINT ( 'NONE',  ( 15.95292532278785913, -51.61873716947361856, 68.50000000000000000 ) ) ;
#9810=VERTEX_POINT ( 'NONE', #2726 ) ;
#9813=EDGE_LOOP ( 'NONE', ( #6860, #13066, #6776, #7077 ) ) ;
#9814=CARTESIAN_POINT ( 'NONE',  ( -9.641460742840918030, 32.93424481021354921, 68.00000000000000000 ) ) ;
#9815=EDGE_CURVE ( 'NONE', #22135, #13238, #9686, .T. ) ;
#9817=ORIENTED_EDGE ( 'NONE', *, *, #17467, .T. ) ;
#9818=EDGE_CURVE ( 'NONE', #18311, #14054, #16375, .T. ) ;
#9819=ORIENTED_EDGE ( 'NONE', *, *, #8311, .T. ) ;
#9821=EDGE_CURVE ( 'NONE', #4856, #12853, #4550, .T. ) ;
#9822=CARTESIAN_POINT ( 'NONE',  ( 0.000000000000000000, -32.11873716947361856, 42.50000000000000711 ) ) ;
#9824=DIRECTION ( 'NONE',  ( -2.388292521039847891E-16, 0.000000000000000000, -1.000000000000000000 ) ) ;
#9833=CYLINDRICAL_SURFACE ( 'NONE', #4127, 0.5000000000000004441 ) ;
#9834=CARTESIAN_POINT ( 'NONE',  ( -27.37540678000427619, 10.94079601157914539, 42.50000000000000000 ) ) ;
#9840=ADVANCED_FACE ( 'NONE', ( #19854 ), #16037, .T. ) ;
#9841=AXIS2_PLACEMENT_3D ( 'NONE', #21625, #16665, #20261 ) ;
#9842=VERTEX_POINT ( 'NONE', #1154 ) ;
#9844=CARTESIAN_POINT ( 'NONE',  ( 29.26816121220499411, -2.729530118891906110, -6.211574946531427711E-18 ) ) ;
#9845=ORIENTED_EDGE ( 'NONE', *, *, #3244, .T. ) ;
#9846=DIRECTION ( 'NONE',  ( 1.000000000000000000, 0.000000000000000000, 0.000000000000000000 ) ) ;
#9847=CARTESIAN_POINT ( 'NONE',  ( -9.141460742840918030, -32.61873716947361856, 42.50000000000000000 ) ) ;
#9850=CARTESIAN_POINT ( 'NONE',  ( -31.50000000000002132, -71.00000000000001421, 3.200000000000000178 ) ) ;
#9851=EDGE_CURVE ( 'NONE', #12877, #4893, #7472, .T. ) ;
#9852=DIRECTION ( 'NONE',  ( -0.000000000000000000, -0.000000000000000000, 1.000000000000000000 ) ) ;
#9854=CIRCLE ( 'NONE', #9149, 2.800000000000003819 ) ;
#9855=TOROIDAL_SURFACE ( 'NONE', #14837, 6.800000000000001599, 0.2999999999999999889 ) ;
#9857=PLANE ( 'NONE',  #3719 ) ;
#9858=CARTESIAN_POINT ( 'NONE',  ( 9.641460742840918030, -32.61873716947361856, 42.50000000000000711 ) ) ;
#9859=DIRECTION ( 'NONE',  ( 1.000000000000000000, 0.000000000000000000, 0.000000000000000000 ) ) ;
#9861=ORIENTED_EDGE ( 'NONE', *, *, #198, .F. ) ;
#9864=CIRCLE ( 'NONE', #8442, 2.000000000000000000 ) ;
#9865=FACE_OUTER_BOUND ( 'NONE', #20549, .T. ) ;
#9867=ORIENTED_EDGE ( 'NONE', *, *, #20739, .F. ) ;
#9874=ORIENTED_EDGE ( 'NONE', *, *, #7908, .F. ) ;
#9875=ORIENTED_EDGE ( 'NONE', *, *, #15109, .F. ) ;
#9876=ORIENTED_EDGE ( 'NONE', *, *, #8209, .T. ) ;
#9880=VECTOR ( 'NONE', #7816, 1000.000000000000000 ) ;
#9883=VERTEX_POINT ( 'NONE', #19635 ) ;
#9884=CARTESIAN_POINT ( 'NONE',  ( -17.95292532278785913, -34.11873716947361856, 109.6002446535588319 ) ) ;
#9885=CARTESIAN_POINT ( 'NONE',  ( 25.37540678000427263, -68.44634676501046044, 7.200000000000000178 ) ) ;
#9886=DIRECTION ( 'NONE',  ( 1.000000000000000000, 0.000000000000000000, 0.000000000000000000 ) ) ;
#9887=CARTESIAN_POINT ( 'NONE',  ( 0.000000000000000000, 4.700000000000000178, 3.799999999999999822 ) ) ;
#9890=CARTESIAN_POINT ( 'NONE',  ( -9.641460742840918030, 33.43424481021354921, 68.00000000000000000 ) ) ;
#9892=EDGE_LOOP ( 'NONE', ( #19138, #9113, #13695, #20128 ) ) ;
#9893=ORIENTED_EDGE ( 'NONE', *, *, #21936, .T. ) ;
#9894=LINE ( 'NONE', #4754, #2426 ) ;
#9896=ORIENTED_EDGE ( 'NONE', *, *, #21899, .F. ) ;
#9897=AXIS2_PLACEMENT_3D ( 'NONE', #13250, #4865, #18390 ) ;
#9901=FACE_OUTER_BOUND ( 'NONE', #14666, .T. ) ;
#9902=AXIS2_PLACEMENT_3D ( 'NONE', #11698, #10575, #600 ) ;
#9903=CARTESIAN_POINT ( 'NONE',  ( -17.45292532278785913, -50.11873716947361856, 68.50000000000000000 ) ) ;
#9906=CARTESIAN_POINT ( 'NONE',  ( -15.95292532278785913, 34.11873716947361856, 68.00000000000000000 ) ) ;
#9907=ORIENTED_EDGE ( 'NONE', *, *, #19646, .T. ) ;
#9909=DIRECTION ( 'NONE',  ( 0.000000000000000000, 0.000000000000000000, -1.000000000000000000 ) ) ;
#9912=AXIS2_PLACEMENT_3D ( 'NONE', #20704, #20590, #1664 ) ;
#9917=CARTESIAN_POINT ( 'NONE',  ( 9.141460742840918030, 33.93424481021354921, 68.00000000000000000 ) ) ;
#9918=EDGE_CURVE ( 'NONE', #1621, #15404, #12751, .T. ) ;
#9919=AXIS2_PLACEMENT_3D ( 'NONE', #10263, #6588, #17081 ) ;
#9920=LINE ( 'NONE', #3206, #10957 ) ;
#9922=ORIENTED_EDGE ( 'NONE', *, *, #17016, .F. ) ;
#9923=CIRCLE ( 'NONE', #1701, 0.2999999999999999334 ) ;
#9927=DIRECTION ( 'NONE',  ( -0.000000000000000000, -0.000000000000000000, -1.000000000000000000 ) ) ;
#9928=VERTEX_POINT ( 'NONE', #20088 ) ;
#9932=DIRECTION ( 'NONE',  ( -0.000000000000000000, -0.000000000000000000, -1.000000000000000000 ) ) ;
#9934=VECTOR ( 'NONE', #18314, 1000.000000000000000 ) ;
#9935=EDGE_CURVE ( 'NONE', #8084, #2490, #2811, .T. ) ;
#9936=FACE_OUTER_BOUND ( 'NONE', #382, .T. ) ;
#9938=DIRECTION ( 'NONE',  ( 1.000000000000000000, 0.000000000000000000, -2.388292521039847891E-16 ) ) ;
#9939=VECTOR ( 'NONE', #17442, 1000.000000000000000 ) ;
#9941=TOROIDAL_SURFACE ( 'NONE', #20305, 0.2500000000000000000, 0.2500000000000000000 ) ;
#9943=VECTOR ( 'NONE', #11632, 1000.000000000000000 ) ;
#9946=DIRECTION ( 'NONE',  ( 0.000000000000000000, 0.000000000000000000, 1.000000000000000000 ) ) ;
#9947=EDGE_LOOP ( 'NONE', ( #7037, #3817, #6783, #21527 ) ) ;
#9949=EDGE_CURVE ( 'NONE', #18602, #17942, #6660, .T. ) ;
#9950=CARTESIAN_POINT ( 'NONE',  ( 26.56227312273159313, 9.958410664601840878, 42.50000000000000000 ) ) ;
#9951=AXIS2_PLACEMENT_3D ( 'NONE', #18293, #2967, #1061 ) ;
#9952=CIRCLE ( 'NONE', #9602, 0.5000000000000004441 ) ;
#9957=ORIENTED_EDGE ( 'NONE', *, *, #11169, .T. ) ;
#9958=ORIENTED_EDGE ( 'NONE', *, *, #3017, .F. ) ;
#9959=VECTOR ( 'NONE', #9502, 1000.000000000000000 ) ;
#9960=DIRECTION ( 'NONE',  ( 0.000000000000000000, 0.000000000000000000, 1.000000000000000000 ) ) ;
#9962=DIRECTION ( 'NONE',  ( 0.000000000000000000, 0.000000000000000000, 1.000000000000000000 ) ) ;
#9963=ORIENTED_EDGE ( 'NONE', *, *, #8049, .T. ) ;
#9964=CARTESIAN_POINT ( 'NONE',  ( -9.641460742840918030, 32.11873716947361856, 42.50000000000000711 ) ) ;
#9965=DIRECTION ( 'NONE',  ( -0.000000000000000000, -1.000000000000000000, 0.000000000000000000 ) ) ;
#9966=LINE ( 'NONE', #13537, #7451 ) ;
#9969=VECTOR ( 'NONE', #11790, 1000.000000000000000 ) ;
#9971=DIRECTION ( 'NONE',  ( 0.000000000000000000, 0.000000000000000000, 1.000000000000000000 ) ) ;
#9972=AXIS2_PLACEMENT_3D ( 'NONE', #21711, #9284, #7617 ) ;
#9974=CARTESIAN_POINT ( 'NONE',  ( -14.96502315657345328, -51.87273146205216534, 13.83570993898299406 ) ) ;
#9975=CARTESIAN_POINT ( 'NONE',  ( 31.50000000000002132, 71.70000000000001705, 3.500000000000000000 ) ) ;
#9976=ADVANCED_FACE ( 'NONE', ( #1259 ), #1683, .F. ) ;
#9978=CARTESIAN_POINT ( 'NONE',  ( 27.67540678000428400, -10.94079601157914716, 13.79999999999999893 ) ) ;
#9979=ORIENTED_EDGE ( 'NONE', *, *, #20001, .T. ) ;
#9982=EDGE_LOOP ( 'NONE', ( #21131, #7690, #1109, #20929 ) ) ;
#9983=CARTESIAN_POINT ( 'NONE',  ( -32.50000000000002132, 71.00000000000001421, 3.200000000000000178 ) ) ;
#9985=CIRCLE ( 'NONE', #19266, 0.3000000000000016542 ) ;
#9990=ORIENTED_EDGE ( 'NONE', *, *, #7184, .T. ) ;
#9994=EDGE_CURVE ( 'NONE', #3158, #5533, #18282, .T. ) ;
#9995=CARTESIAN_POINT ( 'NONE',  ( 24.13662752439704917, 0.000000000000000000, 3.799999999999999822 ) ) ;
#9998=AXIS2_PLACEMENT_3D ( 'NONE', #12982, #13098, #3161 ) ;
#9999=LINE ( 'NONE', #8547, #11882 ) ;
#10000=VECTOR ( 'NONE', #20256, 1000.000000000000000 ) ;
#10002=( BOUNDED_CURVE ( )  B_SPLINE_CURVE ( 3, ( #21568, #17738, #4423, #6232 ),
 .UNSPECIFIED., .F., .T. ) 
 B_SPLINE_CURVE_WITH_KNOTS ( ( 4, 4 ),
 ( 3.141592653589793116, 4.712388980384687009 ),
 .UNSPECIFIED. ) 
 CURVE ( )  GEOMETRIC_REPRESENTATION_ITEM ( )  RATIONAL_B_SPLINE_CURVE ( ( 1.000000000000000000, 0.8047378541243654926, 0.8047378541243654926, 1.000000000000000000 ) ) 
 REPRESENTATION_ITEM ( '' )  );
#10003=DIRECTION ( 'NONE',  ( 0.000000000000000000, 0.000000000000000000, 1.000000000000000000 ) ) ;
#10004=CARTESIAN_POINT ( 'NONE',  ( 0.000000000000000000, -5.000000000000000000, 7.500000000000000000 ) ) ;
#10005=VERTEX_POINT ( 'NONE', #15248 ) ;
#10006=ORIENTED_EDGE ( 'NONE', *, *, #1509, .F. ) ;
#10010=EDGE_LOOP ( 'NONE', ( #17976, #2239, #5242, #11778 ) ) ;
#10011=ADVANCED_FACE ( 'NONE', ( #22104 ), #6781, .F. ) ;
#10012=LINE ( 'NONE', #10230, #199 ) ;
#10014=CIRCLE ( 'NONE', #1471, 2.500000000000002220 ) ;
#10017=VERTEX_POINT ( 'NONE', #20182 ) ;
#10018=DIRECTION ( 'NONE',  ( 0.000000000000000000, 0.000000000000000000, 1.000000000000000000 ) ) ;
#10019=CARTESIAN_POINT ( 'NONE',  ( 32.50000000000002132, 71.00000000000001421, 3.200000000000000178 ) ) ;
#10022=CARTESIAN_POINT ( 'NONE',  ( -28.87540678000427619, -6.494748934539263274, 13.50000000000000000 ) ) ;
#10025=FACE_OUTER_BOUND ( 'NONE', #5019, .T. ) ;
#10028=DIRECTION ( 'NONE',  ( 1.000000000000000000, 0.000000000000000000, 0.000000000000000000 ) ) ;
#10029=ORIENTED_EDGE ( 'NONE', *, *, #96, .T. ) ;
#10033=ORIENTED_EDGE ( 'NONE', *, *, #19691, .F. ) ;
#10034=AXIS2_PLACEMENT_3D ( 'NONE', #8418, #16808, #15124 ) ;
#10035=FACE_OUTER_BOUND ( 'NONE', #2992, .T. ) ;
#10036=DIRECTION ( 'NONE',  ( 0.000000000000000000, 1.000000000000000000, 0.000000000000000000 ) ) ;
#10038=EDGE_LOOP ( 'NONE', ( #6060, #15866, #17872, #6088 ) ) ;
#10040=FACE_OUTER_BOUND ( 'NONE', #15605, .T. ) ;
#10042=DIRECTION ( 'NONE',  ( 1.000000000000000000, 0.000000000000000000, 0.000000000000000000 ) ) ;
#10043=ORIENTED_EDGE ( 'NONE', *, *, #14708, .T. ) ;
#10046=VERTEX_POINT ( 'NONE', #11663 ) ;
#10048=EDGE_CURVE ( 'NONE', #13253, #6305, #18840, .T. ) ;
#10051=CARTESIAN_POINT ( 'NONE',  ( -32.20000000000001705, 0.000000000000000000, 1.500000000000000000 ) ) ;
#10056=ORIENTED_EDGE ( 'NONE', *, *, #16883, .F. ) ;
#10057=CARTESIAN_POINT ( 'NONE',  ( 23.32398829872514057, 7.118794219358020148E-15, 13.50000000000000000 ) ) ;
#10059=DIRECTION ( 'NONE',  ( 1.000000000000000000, 0.000000000000000000, 0.000000000000000000 ) ) ;
#10060=ORIENTED_EDGE ( 'NONE', *, *, #7110, .F. ) ;
#10061=CARTESIAN_POINT ( 'NONE',  ( -4.127054932750482408, -33.93424481021354921, 68.00000000000000000 ) ) ;
#10062=CIRCLE ( 'NONE', #15752, 0.6999999999999992895 ) ;
#10064=ORIENTED_EDGE ( 'NONE', *, *, #5728, .T. ) ;
#10068=AXIS2_PLACEMENT_3D ( 'NONE', #611, #2293, #7136 ) ;
#10071=CARTESIAN_POINT ( 'NONE',  ( -31.50000000000002132, -71.00000000000001421, 3.500000000000000000 ) ) ;
#10072=CIRCLE ( 'NONE', #8996, 0.2500000000000002220 ) ;
#10078=CIRCLE ( 'NONE', #778, 4.999999999999997335 ) ;
#10079=ADVANCED_FACE ( 'NONE', ( #15688 ), #20993, .T. ) ;
#10081=EDGE_CURVE ( 'NONE', #8471, #13403, #361, .T. ) ;
#10084=CARTESIAN_POINT ( 'NONE',  ( 3.127054932750481964, 32.61873716947361856, 68.00000000000000000 ) ) ;
#10087=CARTESIAN_POINT ( 'NONE',  ( -32.50000000000002132, -71.00000000000001421, 1.800000000000000044 ) ) ;
#10089=AXIS2_PLACEMENT_3D ( 'NONE', #19760, #10913, #5796 ) ;
#10092=DIRECTION ( 'NONE',  ( 0.000000000000000000, 0.000000000000000000, 1.000000000000000000 ) ) ;
#10095=EDGE_LOOP ( 'NONE', ( #12754, #10726, #5065, #19255 ) ) ;
#10096=VERTEX_POINT ( 'NONE', #246 ) ;
#10099=ORIENTED_EDGE ( 'NONE', *, *, #11432, .F. ) ;
#10105=CARTESIAN_POINT ( 'NONE',  ( -14.96174975910705207, 51.86873716947361856, 68.00000000000000000 ) ) ;
#10107=DIRECTION ( 'NONE',  ( 1.000000000000000000, 0.000000000000000000, 0.000000000000000000 ) ) ;
#10109=DIRECTION ( 'NONE',  ( 1.000000000000000000, 0.000000000000000000, 0.000000000000000000 ) ) ;
#10111=CARTESIAN_POINT ( 'NONE',  ( -28.87540678000427619, 0.000000000000000000, 13.50000000000000000 ) ) ;
#10112=CARTESIAN_POINT ( 'NONE',  ( 31.50000000000002132, 71.00000000000001421, 1.800000000000000044 ) ) ;
#10114=CARTESIAN_POINT ( 'NONE',  ( -29.13662752439705272, 0.000000000000000000, 3.500000000000000000 ) ) ;
#10115=ORIENTED_EDGE ( 'NONE', *, *, #2372, .T. ) ;
#10117=ORIENTED_EDGE ( 'NONE', *, *, #15622, .F. ) ;
#10118=DIRECTION ( 'NONE',  ( 1.000000000000000000, 0.000000000000000000, 0.000000000000000000 ) ) ;
#10121=EDGE_CURVE ( 'NONE', #1107, #877, #1829, .T. ) ;
#10122=EDGE_CURVE ( 'NONE', #19547, #7401, #15963, .T. ) ;
#10126=LINE ( 'NONE', #21890, #20639 ) ;
#10127=CARTESIAN_POINT ( 'NONE',  ( 28.57540678000427548, 0.000000000000000000, 13.19999999999999929 ) ) ;
#10128=EDGE_LOOP ( 'NONE', ( #4562, #17302, #21716, #14673 ) ) ;
#10130=CARTESIAN_POINT ( 'NONE',  ( -15.21174975910705207, -51.61873716947361856, 14.00000000000000000 ) ) ;
#10134=EDGE_CURVE ( 'NONE', #13657, #16494, #17259, .T. ) ;
#10136=ORIENTED_EDGE ( 'NONE', *, *, #3559, .F. ) ;
#10139=EDGE_LOOP ( 'NONE', ( #3661, #9465, #8222, #15817 ) ) ;
#10142=LINE ( 'NONE', #20553, #10284 ) ;
#10143=EDGE_CURVE ( 'NONE', #13948, #12996, #15794, .T. ) ;
#10144=DIRECTION ( 'NONE',  ( 1.000000000000000000, 0.000000000000000000, 0.000000000000000000 ) ) ;
#10147=EDGE_LOOP ( 'NONE', ( #13590, #14388, #19833, #716 ) ) ;
#10148=DIRECTION ( 'NONE',  ( -0.000000000000000000, 0.000000000000000000, 1.000000000000000000 ) ) ;
#10149=AXIS2_PLACEMENT_3D ( 'NONE', #19327, #1968, #15616 ) ;
#10150=ORIENTED_EDGE ( 'NONE', *, *, #12114, .F. ) ;
#10151=CARTESIAN_POINT ( 'NONE',  ( 15.95292532278785913, 32.61873716947361856, 68.00000000000000000 ) ) ;
#10153=DIRECTION ( 'NONE',  ( 1.000000000000000000, 0.000000000000000000, 0.000000000000000000 ) ) ;
#10155=ORIENTED_EDGE ( 'NONE', *, *, #10675, .T. ) ;
#10156=DIRECTION ( 'NONE',  ( -2.832483164223434527E-16, 1.000000000000000000, 0.000000000000000000 ) ) ;
#10157=CARTESIAN_POINT ( 'NONE',  ( -31.50000000000002132, 71.00000000000001421, 1.800000000000000044 ) ) ;
#10161=LINE ( 'NONE', #6846, #7442 ) ;
#10162=ORIENTED_EDGE ( 'NONE', *, *, #1561, .T. ) ;
#10163=CARTESIAN_POINT ( 'NONE',  ( -14.96174975910705207, -41.81054587065082728, 13.75000000000000000 ) ) ;
#10164=CIRCLE ( 'NONE', #14791, 2.000000000000000000 ) ;
#10168=EDGE_CURVE ( 'NONE', #14982, #21652, #19559, .T. ) ;
#10173=CYLINDRICAL_SURFACE ( 'NONE', #14896, 1.000000000000000888 ) ;
#10176=LINE ( 'NONE', #18566, #15289 ) ;
#10177=ORIENTED_EDGE ( 'NONE', *, *, #9251, .T. ) ;
#10179=CARTESIAN_POINT ( 'NONE',  ( -29.50000000000002132, 0.000000000000000000, 0.2999999999999947153 ) ) ;
#10180=CARTESIAN_POINT ( 'NONE',  ( -3.627054932750481964, 32.61873716947361856, 68.00000000000000000 ) ) ;
#10181=CARTESIAN_POINT ( 'NONE',  ( 29.13662752439705272, 0.000000000000000000, 3.799999999999999822 ) ) ;
#10186=CARTESIAN_POINT ( 'NONE',  ( -4.127054932750482408, 33.43424481021354921, 42.50000000000000000 ) ) ;
#10187=LINE ( 'NONE', #8194, #15078 ) ;
#10188=CARTESIAN_POINT ( 'NONE',  ( 29.13662752439705272, -5.000000000000000000, 7.500000000000000000 ) ) ;
#10189=AXIS2_PLACEMENT_3D ( 'NONE', #21951, #6624, #13949 ) ;
#10193=ADVANCED_FACE ( 'NONE', ( #7541 ), #4166, .T. ) ;
#10194=CYLINDRICAL_SURFACE ( 'NONE', #16686, 0.2999999999999999334 ) ;
#10195=ORIENTED_EDGE ( 'NONE', *, *, #20228, .F. ) ;
#10198=DIRECTION ( 'NONE',  ( 0.000000000000000000, -0.000000000000000000, -1.000000000000000000 ) ) ;
#10200=ORIENTED_EDGE ( 'NONE', *, *, #13630, .F. ) ;
#10201=PLANE ( 'NONE',  #291 ) ;
#10202=EDGE_CURVE ( 'NONE', #7888, #4947, #7755, .T. ) ;
#10204=ORIENTED_EDGE ( 'NONE', *, *, #2972, .T. ) ;
#10206=VECTOR ( 'NONE', #16299, 1000.000000000000000 ) ;
#10207=ORIENTED_EDGE ( 'NONE', *, *, #2869, .T. ) ;
#10208=AXIS2_PLACEMENT_3D ( 'NONE', #5444, #12232, #19081 ) ;
#10210=CARTESIAN_POINT ( 'NONE',  ( 15.95292532278785913, -52.09333383871509682, 13.79999999999999893 ) ) ;
#10212=CARTESIAN_POINT ( 'NONE',  ( 15.00584427753688921, -51.86868465798484351, 13.49999999999999645 ) ) ;
#10216=DIRECTION ( 'NONE',  ( 0.000000000000000000, 0.000000000000000000, 1.000000000000000000 ) ) ;
#10219=DIRECTION ( 'NONE',  ( 0.000000000000000000, -0.000000000000000000, -1.000000000000000000 ) ) ;
#10222=ORIENTED_EDGE ( 'NONE', *, *, #8311, .F. ) ;
#10224=VECTOR ( 'NONE', #7144, 1000.000000000000000 ) ;
#10225=ORIENTED_EDGE ( 'NONE', *, *, #7618, .F. ) ;
#10227=ADVANCED_FACE ( 'NONE', ( #13378 ), #3428, .T. ) ;
#10228=CARTESIAN_POINT ( 'NONE',  ( 0.000000000000000000, 32.11873716947361856, 109.6002446535588319 ) ) ;
#10229=ORIENTED_EDGE ( 'NONE', *, *, #7319, .T. ) ;
#10230=CARTESIAN_POINT ( 'NONE',  ( 28.87540678000427619, -63.74634676501045050, 13.19999999999999929 ) ) ;
#10233=DIRECTION ( 'NONE',  ( 0.000000000000000000, 0.000000000000000000, -1.000000000000000000 ) ) ;
#10234=CIRCLE ( 'NONE', #19158, 0.5000000000000004441 ) ;
#10235=AXIS2_PLACEMENT_3D ( 'NONE', #1719, #1496, #18502 ) ;
#10236=AXIS2_PLACEMENT_3D ( 'NONE', #9454, #11352, #14709 ) ;
#10238=LINE ( 'NONE', #10022, #4870 ) ;
#10239=EDGE_LOOP ( 'NONE', ( #17968, #663, #1466, #6887 ) ) ;
#10241=FACE_OUTER_BOUND ( 'NONE', #4371, .T. ) ;
#10242=EDGE_CURVE ( 'NONE', #4102, #20280, #20661, .T. ) ;
#10248=DIRECTION ( 'NONE',  ( -1.000000000000000000, 0.000000000000000000, 0.000000000000000000 ) ) ;
#10249=ORIENTED_EDGE ( 'NONE', *, *, #21151, .T. ) ;
#10250=LINE ( 'NONE', #9834, #14685 ) ;
#10251=CARTESIAN_POINT ( 'NONE',  ( 3.627054932750481964, 32.93424481021354921, 68.00000000000000000 ) ) ;
#10253=VECTOR ( 'NONE', #12063, 1000.000000000000000 ) ;
#10255=AXIS2_PLACEMENT_3D ( 'NONE', #14477, #21337, #12804 ) ;
#10256=CIRCLE ( 'NONE', #20964, 0.5000000000000004441 ) ;
#10258=ORIENTED_EDGE ( 'NONE', *, *, #17677, .F. ) ;
#10260=EDGE_CURVE ( 'NONE', #11697, #7044, #2042, .T. ) ;
#10261=LINE ( 'NONE', #6812, #15357 ) ;
#10263=CARTESIAN_POINT ( 'NONE',  ( 15.95292532278785913, 34.11873716947361856, 68.00000000000000000 ) ) ;
#10265=ORIENTED_EDGE ( 'NONE', *, *, #10242, .F. ) ;
#10266=DIRECTION ( 'NONE',  ( 0.000000000000000000, 1.000000000000000000, 0.000000000000000000 ) ) ;
#10267=EDGE_LOOP ( 'NONE', ( #16436, #16042, #12046, #15031 ) ) ;
#10269=CIRCLE ( 'NONE', #21043, 5.299999999999998934 ) ;
#10270=CARTESIAN_POINT ( 'NONE',  ( 23.02398829872513986, -2.157133568460768647, 7.500000000000000000 ) ) ;
#10272=CIRCLE ( 'NONE', #597, 0.2999999999999999334 ) ;
#10276=CARTESIAN_POINT ( 'NONE',  ( 23.02398829872513630, 2.558844643944980568, 13.47100117844888167 ) ) ;
#10279=AXIS2_PLACEMENT_3D ( 'NONE', #13243, #3185, #8111 ) ;
#10282=EDGE_LOOP ( 'NONE', ( #19557, #11255, #1133, #5980 ) ) ;
#10284=VECTOR ( 'NONE', #1623, 1000.000000000000000 ) ;
#10285=CYLINDRICAL_SURFACE ( 'NONE', #16633, 0.2999999999999999334 ) ;
#10287=CARTESIAN_POINT ( 'NONE',  ( -14.66174975910705136, -32.10873716947361345, 13.79999999999999893 ) ) ;
#10288=CARTESIAN_POINT ( 'NONE',  ( 15.95292532278785913, 50.11873716947361856, 13.50000000000000000 ) ) ;
#10289=CIRCLE ( 'NONE', #2413, 0.2500000000000002220 ) ;
#10290=CIRCLE ( 'NONE', #4207, 2.299999999999993161 ) ;
#10292=ORIENTED_EDGE ( 'NONE', *, *, #21974, .T. ) ;
#10297=AXIS2_PLACEMENT_3D ( 'NONE', #18721, #20418, #20181 ) ;
#10298=TOROIDAL_SURFACE ( 'NONE', #17418, 1.000000000000000000, 0.5000000000000000000 ) ;
#10301=PLANE ( 'NONE',  #21715 ) ;
#10306=ADVANCED_FACE ( 'NONE', ( #15167 ), #11809, .T. ) ;
#10307=TOROIDAL_SURFACE ( 'NONE', #638, 4.700000000000004619, 0.2999999999999999889 ) ;
#10312=DIRECTION ( 'NONE',  ( -0.000000000000000000, -0.000000000000000000, -1.000000000000000000 ) ) ;
#10313=VECTOR ( 'NONE', #16009, 1000.000000000000000 ) ;
#10315=ORIENTED_EDGE ( 'NONE', *, *, #11543, .F. ) ;
#10320=ORIENTED_EDGE ( 'NONE', *, *, #2791, .T. ) ;
#10327=AXIS2_PLACEMENT_3D ( 'NONE', #12042, #20568, #21009 ) ;
#10329=CIRCLE ( 'NONE', #1008, 3.500000000000003109 ) ;
#10330=ORIENTED_EDGE ( 'NONE', *, *, #16015, .T. ) ;
#10332=DIRECTION ( 'NONE',  ( 0.000000000000000000, 0.000000000000000000, -1.000000000000000000 ) ) ;
#10333=CARTESIAN_POINT ( 'NONE',  ( 14.96512931750545938, -51.87344388792876515, 13.83591901640606459 ) ) ;
#10335=CARTESIAN_POINT ( 'NONE',  ( -15.95292532278785913, 52.11873716947361856, 68.50000000000000000 ) ) ;
#10337=CARTESIAN_POINT ( 'NONE',  ( 4.127054932750481520, -33.43424481021354921, 68.00000000000000000 ) ) ;
#10338=CARTESIAN_POINT ( 'NONE',  ( -17.45292532278785913, 34.11873716947361856, 68.50000000000000000 ) ) ;
#10339=AXIS2_PLACEMENT_3D ( 'NONE', #21012, #5802, #6020 ) ;
#10340=CARTESIAN_POINT ( 'NONE',  ( 23.04906723162513416, -2.296088124452698942, 13.26119099173120475 ) ) ;
#10341=CARTESIAN_POINT ( 'NONE',  ( 25.37540678000427263, -68.74634676501045760, 7.200000000000000178 ) ) ;
#10342=FACE_OUTER_BOUND ( 'NONE', #17496, .T. ) ;
#10346=VECTOR ( 'NONE', #10949, 1000.000000000000000 ) ;
#10348=DIRECTION ( 'NONE',  ( 1.000000000000000000, 0.000000000000000000, 0.000000000000000000 ) ) ;
#10350=ORIENTED_EDGE ( 'NONE', *, *, #14872, .F. ) ;
#10351=CARTESIAN_POINT ( 'NONE',  ( -15.95292532278785913, 50.11873716947361856, 68.00000000000000000 ) ) ;
#10354=CARTESIAN_POINT ( 'NONE',  ( -25.37540678000427263, 63.74634676501045050, 13.50000000000000000 ) ) ;
#10355=( GEOMETRIC_REPRESENTATION_CONTEXT ( 3 ) GLOBAL_UNCERTAINTY_ASSIGNED_CONTEXT ( ( #1235 ) ) GLOBAL_UNIT_ASSIGNED_CONTEXT ( ( #13754, #20276, #6972 ) ) REPRESENTATION_CONTEXT ( 'NONE', 'WORKASPACE' ) );
#10356=VECTOR ( 'NONE', #17224, 1000.000000000000000 ) ;
#10357=ADVANCED_FACE ( 'NONE', ( #10701 ), #3990, .T. ) ;
#10358=DIRECTION ( 'NONE',  ( -0.000000000000000000, -0.000000000000000000, -1.000000000000000000 ) ) ;
#10360=CARTESIAN_POINT ( 'NONE',  ( -28.57540678000427548, -63.74634676501045050, 13.50000000000000000 ) ) ;
#10362=CARTESIAN_POINT ( 'NONE',  ( 0.000000000000000000, 38.74634676501045760, 42.50000000000000000 ) ) ;
#10363=DIRECTION ( 'NONE',  ( 2.832483164223434527E-16, -1.000000000000000000, -0.000000000000000000 ) ) ;
#10365=DIRECTION ( 'NONE',  ( -0.000000000000000000, -0.000000000000000000, -1.000000000000000000 ) ) ;
#10366=CARTESIAN_POINT ( 'NONE',  ( 29.13662752439705272, -4.700000000000000178, 3.500000000000000000 ) ) ;
#10368=DIRECTION ( 'NONE',  ( 1.000000000000000000, 0.000000000000000000, 0.000000000000000000 ) ) ;
#10370=DIRECTION ( 'NONE',  ( 0.000000000000000000, 0.000000000000000000, 1.000000000000000000 ) ) ;
#10371=ORIENTED_EDGE ( 'NONE', *, *, #13781, .F. ) ;
#10372=ORIENTED_EDGE ( 'NONE', *, *, #16885, .F. ) ;
#10374=DIRECTION ( 'NONE',  ( 0.000000000000000000, -1.000000000000000000, 0.000000000000000000 ) ) ;
#10378=CIRCLE ( 'NONE', #4277, 1.000000000000000888 ) ;
#10380=ADVANCED_FACE ( 'NONE', ( #281 ), #14261, .F. ) ;
#10382=DIRECTION ( 'NONE',  ( 0.000000000000000000, 0.000000000000000000, -1.000000000000000000 ) ) ;
#10385=DIRECTION ( 'NONE',  ( 0.000000000000000000, 0.000000000000000000, 1.000000000000000000 ) ) ;
#10389=CARTESIAN_POINT ( 'NONE',  ( 23.02398829872513986, 3.528912754968628551, 13.80000000000000071 ) ) ;
#10391=DIRECTION ( 'NONE',  ( -0.000000000000000000, -0.000000000000000000, -1.000000000000000000 ) ) ;
#10392=CIRCLE ( 'NONE', #5751, 0.2999999999999999334 ) ;
#10393=AXIS2_PLACEMENT_3D ( 'NONE', #1732, #3194, #15381 ) ;
#10394=CARTESIAN_POINT ( 'NONE',  ( -25.37540678000427263, -67.54634676501045476, 7.500000000000000000 ) ) ;
#10396=DIRECTION ( 'NONE',  ( 0.000000000000000000, 0.000000000000000000, -1.000000000000000000 ) ) ;
#10399=DIRECTION ( 'NONE',  ( -0.000000000000000000, 0.000000000000000000, 1.000000000000000000 ) ) ;
#10400=ORIENTED_EDGE ( 'NONE', *, *, #9038, .F. ) ;
#10403=ORIENTED_EDGE ( 'NONE', *, *, #21645, .T. ) ;
#10410=VERTEX_POINT ( 'NONE', #10580 ) ;
#10411=DIRECTION ( 'NONE',  ( -2.388292521039847891E-16, 0.000000000000000000, -1.000000000000000000 ) ) ;
#10412=DIRECTION ( 'NONE',  ( -1.000000000000000000, 0.000000000000000000, 0.000000000000000000 ) ) ;
#10417=FACE_OUTER_BOUND ( 'NONE', #8278, .T. ) ;
#10420=CARTESIAN_POINT ( 'NONE',  ( 3.627054932750481964, 33.43424481021354921, 7.321391277662001151 ) ) ;
#10421=CYLINDRICAL_SURFACE ( 'NONE', #21722, 2.500000000000002220 ) ;
#10422=CIRCLE ( 'NONE', #7215, 4.351418481279137218 ) ;
#10423=CARTESIAN_POINT ( 'NONE',  ( 26.37540678000427619, -10.94079601157914716, 42.50000000000000000 ) ) ;
#10424=AXIS2_PLACEMENT_3D ( 'NONE', #17021, #12505, #3925 ) ;
#10427=DIRECTION ( 'NONE',  ( 0.000000000000000000, 0.000000000000000000, 1.000000000000000000 ) ) ;
#10429=EDGE_CURVE ( 'NONE', #3082, #10879, #4197, .T. ) ;
#10432=VECTOR ( 'NONE', #1850, 1000.000000000000000 ) ;
#10436=CARTESIAN_POINT ( 'NONE',  ( 4.127054932750481520, 33.43424481021354921, 68.00000000000000000 ) ) ;
#10438=DIRECTION ( 'NONE',  ( -1.000000000000000000, 0.000000000000000000, 0.000000000000000000 ) ) ;
#10440=VECTOR ( 'NONE', #17907, 1000.000000000000000 ) ;
#10441=CARTESIAN_POINT ( 'NONE',  ( -23.02398829872513630, 2.211005313989852894, 13.25071573983079887 ) ) ;
#10442=CIRCLE ( 'NONE', #5808, 0.5000000000000004441 ) ;
#10444=DIRECTION ( 'NONE',  ( 0.000000000000000000, -1.000000000000000000, 0.000000000000000000 ) ) ;
#10445=CARTESIAN_POINT ( 'NONE',  ( 23.11756190325309035, -2.646657027129584172, 13.40142076604335841 ) ) ;
#10446=DIRECTION ( 'NONE',  ( 1.000000000000000000, 0.000000000000000000, 0.000000000000000000 ) ) ;
#10449=ORIENTED_EDGE ( 'NONE', *, *, #14882, .T. ) ;
#10450=ORIENTED_EDGE ( 'NONE', *, *, #20262, .F. ) ;
#10454=ORIENTED_EDGE ( 'NONE', *, *, #17908, .T. ) ;
#10457=AXIS2_PLACEMENT_3D ( 'NONE', #976, #2998, #18094 ) ;
#10458=CARTESIAN_POINT ( 'NONE',  ( 14.66174975910705847, 0.000000000000000000, 13.50000000000000000 ) ) ;
#10459=CARTESIAN_POINT ( 'NONE',  ( 32.20000000000001705, 71.00000000000001421, 3.200000000000000178 ) ) ;
#10462=DIRECTION ( 'NONE',  ( -0.000000000000000000, -1.000000000000000000, 0.000000000000000000 ) ) ;
#10463=AXIS2_PLACEMENT_3D ( 'NONE', #3504, #20513, #1481 ) ;
#10464=CARTESIAN_POINT ( 'NONE',  ( 0.000000000000000000, -67.54634676501045476, 7.799999999999999822 ) ) ;
#10468=CARTESIAN_POINT ( 'NONE',  ( -3.127054932750481964, -32.11873716947361856, 68.50000000000000000 ) ) ;
#10469=CARTESIAN_POINT ( 'NONE',  ( -4.127054932750482408, -32.93424481021354921, 68.50000000000000000 ) ) ;
#10473=VERTEX_POINT ( 'NONE', #21326 ) ;
#10475=ORIENTED_EDGE ( 'NONE', *, *, #20339, .F. ) ;
#10481=EDGE_CURVE ( 'NONE', #20437, #21381, #14367, .T. ) ;
#10482=ORIENTED_EDGE ( 'NONE', *, *, #6134, .T. ) ;
#10484=ORIENTED_EDGE ( 'NONE', *, *, #8286, .F. ) ;
#10487=FACE_OUTER_BOUND ( 'NONE', #20812, .T. ) ;
#10490=DIRECTION ( 'NONE',  ( -0.000000000000000000, -0.000000000000000000, -1.000000000000000000 ) ) ;
#10491=DIRECTION ( 'NONE',  ( 0.000000000000000000, 0.000000000000000000, 1.000000000000000000 ) ) ;
#10493=CARTESIAN_POINT ( 'NONE',  ( 0.000000000000000000, -52.10286008774954780, 13.87500000000000000 ) ) ;
#10494=LINE ( 'NONE', #15308, #16387 ) ;
#10495=EDGE_LOOP ( 'NONE', ( #5278, #15186, #2344, #5677 ) ) ;
#10497=VERTEX_POINT ( 'NONE', #2963 ) ;
#10506=EDGE_CURVE ( 'NONE', #20211, #15626, #6002, .T. ) ;
#10509=ORIENTED_EDGE ( 'NONE', *, *, #20142, .T. ) ;
#10510=DIRECTION ( 'NONE',  ( 1.000000000000000000, 0.000000000000000000, 0.000000000000000000 ) ) ;
#10513=CARTESIAN_POINT ( 'NONE',  ( -15.95292532278785913, 50.11873716947361856, 68.50000000000000000 ) ) ;
#10514=DIRECTION ( 'NONE',  ( 1.000000000000000000, 0.000000000000000000, 0.000000000000000000 ) ) ;
#10516=ORIENTED_EDGE ( 'NONE', *, *, #15131, .F. ) ;
#10517=CARTESIAN_POINT ( 'NONE',  ( -9.141460742840918030, -32.93424481021354921, 68.00000000000000000 ) ) ;
#10519=DIRECTION ( 'NONE',  ( 0.000000000000000000, 0.000000000000000000, 1.000000000000000000 ) ) ;
#10520=ADVANCED_FACE ( 'NONE', ( #2857 ), #9341, .T. ) ;
#10521=CARTESIAN_POINT ( 'NONE',  ( 9.641460742840918030, -32.11873716947361856, 68.00000000000000000 ) ) ;
#10524=CARTESIAN_POINT ( 'NONE',  ( -14.96174975910705207, 51.76873716947361714, 13.50000000000000000 ) ) ;
#10526=ORIENTED_EDGE ( 'NONE', *, *, #12682, .F. ) ;
#10528=VERTEX_POINT ( 'NONE', #4412 ) ;
#10529=CARTESIAN_POINT ( 'NONE',  ( 23.02398829872514341, -3.297363125858362665, 13.54387027667928933 ) ) ;
#10531=VERTEX_POINT ( 'NONE', #14465 ) ;
#10532=DIRECTION ( 'NONE',  ( 2.388292521039847891E-16, 0.000000000000000000, 1.000000000000000000 ) ) ;
#10533=CARTESIAN_POINT ( 'NONE',  ( 30.37540678000427619, -63.74634676501045050, 7.500000000000000000 ) ) ;
#10534=DIRECTION ( 'NONE',  ( 0.000000000000000000, 0.000000000000000000, -1.000000000000000000 ) ) ;
#10535=AXIS2_PLACEMENT_3D ( 'NONE', #15948, #7485, #14284 ) ;
#10539=CARTESIAN_POINT ( 'NONE',  ( -23.02398829872514341, 2.558598175897728755, 13.47089014135852736 ) ) ;
#10542=DIRECTION ( 'NONE',  ( -1.000000000000000000, 0.000000000000000000, 0.000000000000000000 ) ) ;
#10543=CYLINDRICAL_SURFACE ( 'NONE', #14631, 0.2999999999999999334 ) ;
#10544=CARTESIAN_POINT ( 'NONE',  ( -25.37540678000427263, -68.74634676501045760, 7.500000000000000000 ) ) ;
#10548=LINE ( 'NONE', #8988, #21753 ) ;
#10550=VERTEX_POINT ( 'NONE', #9448 ) ;
#10551=AXIS2_PLACEMENT_3D ( 'NONE', #9466, #11041, #7922 ) ;
#10552=VECTOR ( 'NONE', #6350, 1000.000000000000000 ) ;
#10554=DIRECTION ( 'NONE',  ( 1.000000000000000000, 0.000000000000000000, -2.388292521039847891E-16 ) ) ;
#10555=CARTESIAN_POINT ( 'NONE',  ( 28.87540678000427619, 63.74634676501045050, 13.50000000000000000 ) ) ;
#10558=PLANE ( 'NONE',  #13215 ) ;
#10559=DIRECTION ( 'NONE',  ( 0.000000000000000000, 0.000000000000000000, 1.000000000000000000 ) ) ;
#10561=CARTESIAN_POINT ( 'NONE',  ( -15.21174975910705207, -41.81054587065082728, 68.25000000000000000 ) ) ;
#10562=CARTESIAN_POINT ( 'NONE',  ( -27.37540678000427974, -10.94079601157914716, 42.50000000000000000 ) ) ;
#10563=CARTESIAN_POINT ( 'NONE',  ( 0.000000000000000000, 67.24634676501045760, 13.50000000000000000 ) ) ;
#10564=DIRECTION ( 'NONE',  ( -0.000000000000000000, -1.000000000000000000, -0.000000000000000000 ) ) ;
#10568=VERTEX_POINT ( 'NONE', #12669 ) ;
#10569=DIRECTION ( 'NONE',  ( 1.000000000000000000, 0.000000000000000000, 0.000000000000000000 ) ) ;
#10571=DIRECTION ( 'NONE',  ( -0.000000000000000000, 0.000000000000000000, 1.000000000000000000 ) ) ;
#10572=ORIENTED_EDGE ( 'NONE', *, *, #680, .F. ) ;
#10575=DIRECTION ( 'NONE',  ( 0.000000000000000000, -1.000000000000000000, -0.000000000000000000 ) ) ;
#10577=LINE ( 'NONE', #5349, #12485 ) ;
#10578=VECTOR ( 'NONE', #16212, 1000.000000000000000 ) ;
#10580=CARTESIAN_POINT ( 'NONE',  ( 23.02398829872514341, -5.683640910026986681, 42.50000000000000000 ) ) ;
#10581=VECTOR ( 'NONE', #1697, 1000.000000000000000 ) ;
#10583=ORIENTED_EDGE ( 'NONE', *, *, #5488, .F. ) ;
#10585=VECTOR ( 'NONE', #4710, 1000.000000000000000 ) ;
#10587=ORIENTED_EDGE ( 'NONE', *, *, #2972, .F. ) ;
#10588=CARTESIAN_POINT ( 'NONE',  ( -28.79994065384636315, -6.566898051583388352, 13.40260211333369256 ) ) ;
#10590=DIRECTION ( 'NONE',  ( 0.000000000000000000, -1.000000000000000000, 0.000000000000000000 ) ) ;
#10591=LINE ( 'NONE', #5571, #10224 ) ;
#10593=CARTESIAN_POINT ( 'NONE',  ( 23.04273156199908712, 2.261510999193106386, 13.20000000000004015 ) ) ;
#10599=ORIENTED_EDGE ( 'NONE', *, *, #8254, .F. ) ;
#10600=AXIS2_PLACEMENT_3D ( 'NONE', #7912, #20196, #13144 ) ;
#10603=CIRCLE ( 'NONE', #12365, 0.2999999999999999334 ) ;
#10604=EDGE_CURVE ( 'NONE', #17808, #630, #9864, .T. ) ;
#10606=DIRECTION ( 'NONE',  ( 0.000000000000000000, -1.000000000000000000, 0.000000000000000000 ) ) ;
#10607=ORIENTED_EDGE ( 'NONE', *, *, #12703, .F. ) ;
#10608=AXIS2_PLACEMENT_3D ( 'NONE', #20058, #20391, #16558 ) ;
#10614=EDGE_LOOP ( 'NONE', ( #12611, #10371, #4559, #16869 ) ) ;
#10618=ORIENTED_EDGE ( 'NONE', *, *, #15261, .F. ) ;
#10621=CARTESIAN_POINT ( 'NONE',  ( 30.07540678000427548, 63.74634676501045050, 7.200000000000000178 ) ) ;
#10622=CARTESIAN_POINT ( 'NONE',  ( 3.627054932750481964, 32.61873716947361856, 68.50000000000000000 ) ) ;
#10627=EDGE_CURVE ( 'NONE', #18406, #17937, #6119, .T. ) ;
#10630=TOROIDAL_SURFACE ( 'NONE', #19207, 1.500000000000000000, 0.5000000000000000000 ) ;
#10631=VECTOR ( 'NONE', #12953, 1000.000000000000000 ) ;
#10632=ORIENTED_EDGE ( 'NONE', *, *, #8738, .F. ) ;
#10633=DIRECTION ( 'NONE',  ( -0.000000000000000000, 1.000000000000000000, 0.000000000000000000 ) ) ;
#10636=ORIENTED_EDGE ( 'NONE', *, *, #7013, .T. ) ;
#10638=CARTESIAN_POINT ( 'NONE',  ( -25.37540678000426908, 38.74634676501045760, 13.79999999999999893 ) ) ;
#10641=ORIENTED_EDGE ( 'NONE', *, *, #15476, .F. ) ;
#10642=ADVANCED_FACE ( 'NONE', ( #20422 ), #11631, .T. ) ;
#10643=CARTESIAN_POINT ( 'NONE',  ( 23.04273156199908357, -2.261510999192897220, 13.19999999999999218 ) ) ;
#10644=ORIENTED_EDGE ( 'NONE', *, *, #18025, .T. ) ;
#10647=AXIS2_PLACEMENT_3D ( 'NONE', #18079, #6253, #2987 ) ;
#10648=ORIENTED_EDGE ( 'NONE', *, *, #16305, .F. ) ;
#10651=PLANE ( 'NONE',  #1287 ) ;
#10652=VECTOR ( 'NONE', #5722, 1000.000000000000000 ) ;
#10656=EDGE_CURVE ( 'NONE', #11890, #20195, #10012, .T. ) ;
#10657=CARTESIAN_POINT ( 'NONE',  ( -23.04897344237150492, 2.295898177910673965, 13.26544997878583487 ) ) ;
#10658=FACE_OUTER_BOUND ( 'NONE', #4030, .T. ) ;
#10662=AXIS2_PLACEMENT_3D ( 'NONE', #12986, #19616, #21420 ) ;
#10664=ORIENTED_EDGE ( 'NONE', *, *, #11376, .T. ) ;
#10667=DIRECTION ( 'NONE',  ( 0.000000000000000000, -1.000000000000000000, 0.000000000000000000 ) ) ;
#10668=TOROIDAL_SURFACE ( 'NONE', #18165, 4.051418481279135619, 0.2999999999999999889 ) ;
#10670=AXIS2_PLACEMENT_3D ( 'NONE', #2618, #18173, #17833 ) ;
#10671=CARTESIAN_POINT ( 'NONE',  ( 3.127054932750481964, 33.43424481021354921, 68.50000000000000000 ) ) ;
#10672=AXIS2_PLACEMENT_3D ( 'NONE', #1807, #4827, #21855 ) ;
#10673=ORIENTED_EDGE ( 'NONE', *, *, #8101, .F. ) ;
#10674=CIRCLE ( 'NONE', #12094, 0.3000000000000003775 ) ;
#10675=EDGE_CURVE ( 'NONE', #6635, #5485, #12692, .T. ) ;
#10676=ADVANCED_FACE ( 'NONE', ( #6450 ), #17046, .F. ) ;
#10677=CARTESIAN_POINT ( 'NONE',  ( -23.02398829872513986, 5.683640910026983128, 42.50000000000000000 ) ) ;
#10678=AXIS2_PLACEMENT_3D ( 'NONE', #6601, #18097, #13396 ) ;
#10679=DIRECTION ( 'NONE',  ( -1.000000000000000000, 0.000000000000000000, 0.000000000000000000 ) ) ;
#10680=VERTEX_POINT ( 'NONE', #20091 ) ;
#10681=DIRECTION ( 'NONE',  ( -1.000000000000000000, 0.000000000000000000, 0.000000000000000000 ) ) ;
#10683=DIRECTION ( 'NONE',  ( -1.000000000000000000, -0.000000000000000000, -0.000000000000000000 ) ) ;
#10688=LINE ( 'NONE', #17910, #18827 ) ;
#10690=CARTESIAN_POINT ( 'NONE',  ( -29.17540678000427690, -63.74634676501045050, 7.500000000000000000 ) ) ;
#10693=EDGE_CURVE ( 'NONE', #8671, #4102, #8560, .T. ) ;
#10694=ORIENTED_EDGE ( 'NONE', *, *, #13731, .F. ) ;
#10695=EDGE_LOOP ( 'NONE', ( #12403, #6806, #21853, #2582 ) ) ;
#10697=CARTESIAN_POINT ( 'NONE',  ( -29.01868551570922605, -6.499165645473476971, 7.532495484408729958 ) ) ;
#10699=DIRECTION ( 'NONE',  ( 0.000000000000000000, 0.000000000000000000, 1.000000000000000000 ) ) ;
#10700=EDGE_LOOP ( 'NONE', ( #5578, #21412, #8592, #19530 ) ) ;
#10701=FACE_OUTER_BOUND ( 'NONE', #4756, .T. ) ;
#10705=CARTESIAN_POINT ( 'NONE',  ( 31.50000000000002132, -72.00000000000001421, 1.800000000000000044 ) ) ;
#10706=DIRECTION ( 'NONE',  ( -0.000000000000000000, -0.000000000000000000, -1.000000000000000000 ) ) ;
#10708=CARTESIAN_POINT ( 'NONE',  ( -28.87540678000427619, -6.494748934539263274, 13.19999999999999929 ) ) ;
#10710=CARTESIAN_POINT ( 'NONE',  ( 17.45292532278785913, 0.000000000000000000, 68.00000000000000000 ) ) ;
#10713=DIRECTION ( 'NONE',  ( 1.000000000000000000, 0.000000000000000000, -0.000000000000000000 ) ) ;
#10714=CARTESIAN_POINT ( 'NONE',  ( 23.04273156199908357, -2.261510999192741345, 13.50000000000000000 ) ) ;
#10715=LINE ( 'NONE', #10493, #14066 ) ;
#10716=DIRECTION ( 'NONE',  ( -0.000000000000000000, 1.000000000000000000, 0.000000000000000000 ) ) ;
#10717=ORIENTED_EDGE ( 'NONE', *, *, #18340, .F. ) ;
#10718=CIRCLE ( 'NONE', #19289, 1.299999999999999156 ) ;
#10722=STYLED_ITEM ( 'NONE', ( #5173 ), #7548 ) ;
#10723=DIRECTION ( 'NONE',  ( 0.000000000000000000, -1.000000000000000000, 0.000000000000000000 ) ) ;
#10724=VECTOR ( 'NONE', #8590, 1000.000000000000000 ) ;
#10726=ORIENTED_EDGE ( 'NONE', *, *, #20453, .T. ) ;
#10727=ORIENTED_EDGE ( 'NONE', *, *, #5701, .T. ) ;
#10729=VERTEX_POINT ( 'NONE', #18846 ) ;
#10731=EDGE_CURVE ( 'NONE', #2970, #10879, #3187, .T. ) ;
#10732=ADVANCED_FACE ( 'NONE', ( #12312 ), #13902, .F. ) ;
#10733=ORIENTED_EDGE ( 'NONE', *, *, #19340, .T. ) ;
#10734=AXIS2_PLACEMENT_3D ( 'NONE', #20219, #3100, #16746 ) ;
#10735=ORIENTED_EDGE ( 'NONE', *, *, #7078, .T. ) ;
#10736=CARTESIAN_POINT ( 'NONE',  ( 27.37540678000426908, 36.74634676501047181, 42.50000000000000000 ) ) ;
#10737=AXIS2_PLACEMENT_3D ( 'NONE', #19295, #19071, #2163 ) ;
#10738=DIRECTION ( 'NONE',  ( 0.000000000000000000, 0.000000000000000000, -1.000000000000000000 ) ) ;
#10739=CARTESIAN_POINT ( 'NONE',  ( 28.87540678000427619, 6.494748934539263274, 7.720760502796167657 ) ) ;
#10741=VERTEX_POINT ( 'NONE', #3236 ) ;
#10742=DIRECTION ( 'NONE',  ( 0.000000000000000000, 0.000000000000000000, 1.000000000000000000 ) ) ;
#10743=ADVANCED_FACE ( 'NONE', ( #8613 ), #10285, .T. ) ;
#10745=CARTESIAN_POINT ( 'NONE',  ( 15.21174975910705918, 52.39333383871510108, 13.50000000000000000 ) ) ;
#10747=ORIENTED_EDGE ( 'NONE', *, *, #19901, .F. ) ;
#10748=CARTESIAN_POINT ( 'NONE',  ( 30.67540678000428045, 0.000000000000000000, 3.799999999999999822 ) ) ;
#10752=DIRECTION ( 'NONE',  ( 0.000000000000000000, -1.000000000000000000, 0.000000000000000000 ) ) ;
#10758=CARTESIAN_POINT ( 'NONE',  ( 23.02398829872514341, -2.192121262983568908, 13.33089993820311925 ) ) ;
#10760=ORIENTED_EDGE ( 'NONE', *, *, #6310, .F. ) ;
#10764=DIRECTION ( 'NONE',  ( -0.000000000000000000, 0.000000000000000000, 1.000000000000000000 ) ) ;
#10767=EDGE_CURVE ( 'NONE', #9267, #4383, #4911, .T. ) ;
#10770=PLANE ( 'NONE',  #5553 ) ;
#10772=ADVANCED_FACE ( 'NONE', ( #1650 ), #11723, .F. ) ;
#10778=DIRECTION ( 'NONE',  ( 0.000000000000000000, 0.000000000000000000, 1.000000000000000000 ) ) ;
#10781=ORIENTED_EDGE ( 'NONE', *, *, #14677, .F. ) ;
#10783=AXIS2_PLACEMENT_3D ( 'NONE', #11213, #18034, #6437 ) ;
#10784=CIRCLE ( 'NONE', #20799, 2.000000000000000000 ) ;
#10788=ORIENTED_EDGE ( 'NONE', *, *, #15782, .F. ) ;
#10789=CARTESIAN_POINT ( 'NONE',  ( 3.127054932750481964, 32.11873716947361856, 68.00000000000000000 ) ) ;
#10790=DIRECTION ( 'NONE',  ( 0.000000000000000000, 0.000000000000000000, -1.000000000000000000 ) ) ;
#10791=DIRECTION ( 'NONE',  ( 1.000000000000000000, 0.000000000000000000, 0.000000000000000000 ) ) ;
#10792=CARTESIAN_POINT ( 'NONE',  ( -8.641460742840918030, 32.93424481021354921, 68.50000000000000000 ) ) ;
#10800=EDGE_CURVE ( 'NONE', #8248, #6058, #5137, .T. ) ;
#10801=ORIENTED_EDGE ( 'NONE', *, *, #9675, .F. ) ;
#10806=DIRECTION ( 'NONE',  ( 1.000000000000000000, 0.000000000000000000, 0.000000000000000000 ) ) ;
#10807=TOROIDAL_SURFACE ( 'NONE', #2220, 3.800000000000002931, 0.2999999999999999889 ) ;
#10808=DIRECTION ( 'NONE',  ( 0.000000000000000000, 1.000000000000000000, 0.000000000000000000 ) ) ;
#10809=ORIENTED_EDGE ( 'NONE', *, *, #7736, .T. ) ;
#10812=VERTEX_POINT ( 'NONE', #18331 ) ;
#10813=DIRECTION ( 'NONE',  ( -2.388292521039847891E-16, 0.000000000000000000, -1.000000000000000000 ) ) ;
#10815=LINE ( 'NONE', #396, #15718 ) ;
#10816=DIRECTION ( 'NONE',  ( 1.000000000000000000, 0.000000000000000000, -0.000000000000000000 ) ) ;
#10817=ORIENTED_EDGE ( 'NONE', *, *, #16178, .F. ) ;
#10818=PLANE ( 'NONE',  #11283 ) ;
#10821=CARTESIAN_POINT ( 'NONE',  ( -23.04692967985607055, -2.284552260428336368, 13.25236378595243103 ) ) ;
#10822=ORIENTED_EDGE ( 'NONE', *, *, #1108, .F. ) ;
#10824=EDGE_CURVE ( 'NONE', #12787, #4126, #11940, .T. ) ;
#10825=ORIENTED_EDGE ( 'NONE', *, *, #21718, .T. ) ;
#10826=LINE ( 'NONE', #409, #18764 ) ;
#10828=ORIENTED_EDGE ( 'NONE', *, *, #3092, .F. ) ;
#10829=EDGE_LOOP ( 'NONE', ( #2879, #2551, #7560, #9762 ) ) ;
#10830=DIRECTION ( 'NONE',  ( -1.000000000000000000, 0.000000000000000000, 0.000000000000000000 ) ) ;
#10833=EDGE_LOOP ( 'NONE', ( #5782, #6422, #14132, #16607 ) ) ;
#10834=DIRECTION ( 'NONE',  ( -0.000000000000000000, -0.000000000000000000, -1.000000000000000000 ) ) ;
#10835=DIRECTION ( 'NONE',  ( 0.000000000000000000, 0.000000000000000000, 1.000000000000000000 ) ) ;
#10837=DIRECTION ( 'NONE',  ( 1.000000000000000000, 0.000000000000000000, 0.000000000000000000 ) ) ;
#10838=PLANE ( 'NONE',  #12545 ) ;
#10839=ORIENTED_EDGE ( 'NONE', *, *, #18523, .F. ) ;
#10841=LINE ( 'NONE', #5498, #22160 ) ;
#10847=ORIENTED_EDGE ( 'NONE', *, *, #9505, .T. ) ;
#10849=ORIENTED_EDGE ( 'NONE', *, *, #8563, .F. ) ;
#10850=CARTESIAN_POINT ( 'NONE',  ( 29.37540678000427619, -5.000000000000000000, 7.200000000000000178 ) ) ;
#10851=ORIENTED_EDGE ( 'NONE', *, *, #21239, .T. ) ;
#10855=CARTESIAN_POINT ( 'NONE',  ( 23.07499583180669589, -2.433548416302916628, 13.33575415462846081 ) ) ;
#10856=ORIENTED_EDGE ( 'NONE', *, *, #12421, .F. ) ;
#10857=CARTESIAN_POINT ( 'NONE',  ( 23.32398829872514057, 2.157133568460765538, 13.19999999999999929 ) ) ;
#10858=ORIENTED_EDGE ( 'NONE', *, *, #17758, .F. ) ;
#10860=CYLINDRICAL_SURFACE ( 'NONE', #14506, 0.2999999999999999334 ) ;
#10862=DIRECTION ( 'NONE',  ( 3.052134192567367925E-16, -1.000000000000000000, 0.000000000000000000 ) ) ;
#10864=ADVANCED_FACE ( 'NONE', ( #8935 ), #17421, .F. ) ;
#10865=EDGE_CURVE ( 'NONE', #13985, #5446, #19886, .T. ) ;
#10866=CARTESIAN_POINT ( 'NONE',  ( -23.02398829872513986, 2.279831973701412107, 13.43058255391197697 ) ) ;
#10868=EDGE_CURVE ( 'NONE', #6809, #11011, #7487, .T. ) ;
#10869=CARTESIAN_POINT ( 'NONE',  ( 0.000000000000000000, 32.61873716947361856, 68.00000000000000000 ) ) ;
#10871=LINE ( 'NONE', #17909, #20912 ) ;
#10874=EDGE_CURVE ( 'NONE', #12853, #5745, #17638, .T. ) ;
#10877=CARTESIAN_POINT ( 'NONE',  ( 3.627054932750481520, 32.93424481021354921, 42.50000000000000000 ) ) ;
#10879=VERTEX_POINT ( 'NONE', #4013 ) ;
#10883=CARTESIAN_POINT ( 'NONE',  ( -9.141460742840918030, -32.61873716947361856, 7.321391277662001151 ) ) ;
#10884=ORIENTED_EDGE ( 'NONE', *, *, #7546, .F. ) ;
#10889=CARTESIAN_POINT ( 'NONE',  ( 14.75227361498200551, 52.14371094787964722, 13.50000000000000000 ) ) ;
#10890=DIRECTION ( 'NONE',  ( 0.000000000000000000, 0.000000000000000000, -1.000000000000000000 ) ) ;
#10895=CARTESIAN_POINT ( 'NONE',  ( 4.127054932750481520, -32.93424481021354921, 68.50000000000000000 ) ) ;
#10896=ORIENTED_EDGE ( 'NONE', *, *, #21637, .F. ) ;
#10902=DIRECTION ( 'NONE',  ( 0.000000000000000000, 0.000000000000000000, 1.000000000000000000 ) ) ;
#10904=CARTESIAN_POINT ( 'NONE',  ( 8.641460742840918030, -32.93424481021354921, 68.00000000000000000 ) ) ;
#10907=DIRECTION ( 'NONE',  ( -1.000000000000000000, 0.000000000000000000, 0.000000000000000000 ) ) ;
#10909=CARTESIAN_POINT ( 'NONE',  ( -28.87540678000428329, -6.494748934539265051, 13.24746166461178554 ) ) ;
#10911=LINE ( 'NONE', #9126, #7458 ) ;
#10913=DIRECTION ( 'NONE',  ( 1.000000000000000000, 0.000000000000000000, -2.388292521039847891E-16 ) ) ;
#10914=VECTOR ( 'NONE', #4992, 1000.000000000000000 ) ;
#10915=DIRECTION ( 'NONE',  ( 0.000000000000000000, 0.000000000000000000, 1.000000000000000000 ) ) ;
#10920=FACE_OUTER_BOUND ( 'NONE', #21654, .T. ) ;
#10923=FACE_OUTER_BOUND ( 'NONE', #4733, .T. ) ;
#10926=DIRECTION ( 'NONE',  ( 0.000000000000000000, 0.000000000000000000, 1.000000000000000000 ) ) ;
#10927=DIRECTION ( 'NONE',  ( 0.000000000000000000, 0.000000000000000000, 1.000000000000000000 ) ) ;
#10928=ORIENTED_EDGE ( 'NONE', *, *, #19560, .F. ) ;
#10937=EDGE_CURVE ( 'NONE', #7824, #3013, #15841, .T. ) ;
#10938=CIRCLE ( 'NONE', #15213, 2.500000000000002220 ) ;
#10942=DIRECTION ( 'NONE',  ( 0.000000000000000000, 0.000000000000000000, -1.000000000000000000 ) ) ;
#10945=DIRECTION ( 'NONE',  ( 0.000000000000000000, 0.000000000000000000, 1.000000000000000000 ) ) ;
#10946=ORIENTED_EDGE ( 'NONE', *, *, #16324, .F. ) ;
#10948=AXIS2_PLACEMENT_3D ( 'NONE', #19732, #14568, #6096 ) ;
#10949=DIRECTION ( 'NONE',  ( -0.000000000000000000, -1.000000000000000000, 0.000000000000000000 ) ) ;
#10952=CARTESIAN_POINT ( 'NONE',  ( -4.127054932750482408, 32.93424481021354921, 42.50000000000000000 ) ) ;
#10953=VERTEX_POINT ( 'NONE', #8720 ) ;
#10954=CIRCLE ( 'NONE', #575, 2.500000000000002220 ) ;
#10955=ADVANCED_FACE ( 'NONE', ( #14166 ), #8821, .F. ) ;
#10957=VECTOR ( 'NONE', #11910, 1000.000000000000000 ) ;
#10958=ORIENTED_EDGE ( 'NONE', *, *, #17306, .T. ) ;
#10961=LINE ( 'NONE', #14760, #251 ) ;
#10962=ORIENTED_EDGE ( 'NONE', *, *, #21069, .F. ) ;
#10963=VERTEX_POINT ( 'NONE', #19110 ) ;
#10965=ADVANCED_FACE ( 'NONE', ( #18899 ), #4522, .T. ) ;
#10969=CARTESIAN_POINT ( 'NONE',  ( 29.13662752439705272, 0.000000000000000000, 3.799999999999999822 ) ) ;
#10971=LINE ( 'NONE', #14534, #3429 ) ;
#10974=TOROIDAL_SURFACE ( 'NONE', #13822, 1.300000000000000044, 0.2999999999999999889 ) ;
#10975=AXIS2_PLACEMENT_3D ( 'NONE', #817, #16032, #9333 ) ;
#10978=AXIS2_PLACEMENT_3D ( 'NONE', #17945, #7902, #4195 ) ;
#10980=AXIS2_PLACEMENT_3D ( 'NONE', #7236, #9231, #17831 ) ;
#10981=EDGE_CURVE ( 'NONE', #4245, #17392, #17861, .T. ) ;
#10982=DIRECTION ( 'NONE',  ( -0.000000000000000000, -0.000000000000000000, 1.000000000000000000 ) ) ;
#10983=ORIENTED_EDGE ( 'NONE', *, *, #13195, .F. ) ;
#10985=LINE ( 'NONE', #11431, #6023 ) ;
#10987=VECTOR ( 'NONE', #16418, 1000.000000000000000 ) ;
#10990=EDGE_LOOP ( 'NONE', ( #5491, #14231, #510, #15030 ) ) ;
#10991=EDGE_CURVE ( 'NONE', #5643, #18174, #10256, .T. ) ;
#10992=EDGE_CURVE ( 'NONE', #11808, #13948, #19664, .T. ) ;
#10993=EDGE_CURVE ( 'NONE', #4678, #20293, #18199, .T. ) ;
#10996=CIRCLE ( 'NONE', #21739, 0.2500000000000002220 ) ;
#10997=FACE_BOUND ( 'NONE', #12541, .T. ) ;
#10998=CARTESIAN_POINT ( 'NONE',  ( -23.04273156199908357, -2.261510999192741345, 13.50000000000000000 ) ) ;
#11000=CARTESIAN_POINT ( 'NONE',  ( 9.641460742840918030, 32.11873716947361856, 68.00000000000000000 ) ) ;
#11002=CARTESIAN_POINT ( 'NONE',  ( 14.71479891986436606, 52.07369784111803312, 13.50000000000000000 ) ) ;
#11003=DIRECTION ( 'NONE',  ( -1.000000000000000000, 0.000000000000000000, 0.000000000000000000 ) ) ;
#11006=EDGE_CURVE ( 'NONE', #11511, #18, #15233, .T. ) ;
#11007=ORIENTED_EDGE ( 'NONE', *, *, #1344, .T. ) ;
#11010=CARTESIAN_POINT ( 'NONE',  ( -25.37540678000427263, -63.74634676501045050, 13.19999999999999929 ) ) ;
#11011=VERTEX_POINT ( 'NONE', #16272 ) ;
#11014=DIRECTION ( 'NONE',  ( 0.000000000000000000, 1.000000000000000000, 0.000000000000000000 ) ) ;
#11017=ORIENTED_EDGE ( 'NONE', *, *, #14919, .F. ) ;
#11018=DIRECTION ( 'NONE',  ( -1.000000000000000000, 0.000000000000000000, 0.000000000000000000 ) ) ;
#11020=EDGE_CURVE ( 'NONE', #877, #17577, #19775, .T. ) ;
#11021=ORIENTED_EDGE ( 'NONE', *, *, #15854, .T. ) ;
#11022=DIRECTION ( 'NONE',  ( 0.000000000000000000, 0.000000000000000000, -1.000000000000000000 ) ) ;
#11024=DIRECTION ( 'NONE',  ( 0.000000000000000000, 0.000000000000000000, 1.000000000000000000 ) ) ;
#11025=EDGE_CURVE ( 'NONE', #17779, #8815, #18449, .T. ) ;
#11027=DIRECTION ( 'NONE',  ( 0.000000000000000000, 0.000000000000000000, 1.000000000000000000 ) ) ;
#11029=CARTESIAN_POINT ( 'NONE',  ( 14.96174975910705918, -32.10873716947361345, 13.05380965755522737 ) ) ;
#11030=DIRECTION ( 'NONE',  ( 1.000000000000000000, 0.000000000000000000, 0.000000000000000000 ) ) ;
#11031=VERTEX_POINT ( 'NONE', #8023 ) ;
#11035=DIRECTION ( 'NONE',  ( 1.000000000000000000, 0.000000000000000000, 0.000000000000000000 ) ) ;
#11036=CARTESIAN_POINT ( 'NONE',  ( -23.05999184077137443, -2.354728237135332414, 13.30000967910993737 ) ) ;
#11038=( NAMED_UNIT ( * ) PLANE_ANGLE_UNIT ( ) SI_UNIT ( $, .RADIAN. ) );
#11039=EDGE_CURVE ( 'NONE', #16873, #3099, #12736, .T. ) ;
#11041=DIRECTION ( 'NONE',  ( -1.000000000000000000, -0.000000000000000000, -0.000000000000000000 ) ) ;
#11045=CARTESIAN_POINT ( 'NONE',  ( -26.37540678000427619, -10.94079601157914716, 13.50000000000000000 ) ) ;
#11047=DIRECTION ( 'NONE',  ( 1.000000000000000000, 0.000000000000000000, -0.000000000000000000 ) ) ;
#11051=ORIENTED_EDGE ( 'NONE', *, *, #4083, .F. ) ;
#11052=ADVANCED_FACE ( 'NONE', ( #14485 ), #12707, .F. ) ;
#11054=CARTESIAN_POINT ( 'NONE',  ( -25.37540678000427263, -63.74634676501045050, 7.500000000000000000 ) ) ;
#11057=CARTESIAN_POINT ( 'NONE',  ( -17.93704824106378837, 38.74634676501045760, 13.87500000000000000 ) ) ;
#11058=CIRCLE ( 'NONE', #20024, 0.5000000000000004441 ) ;
#11060=CARTESIAN_POINT ( 'NONE',  ( -30.37540678000427619, 63.74634676501045050, 7.500000000000000000 ) ) ;
#11061=ORIENTED_EDGE ( 'NONE', *, *, #14013, .T. ) ;
#11062=CARTESIAN_POINT ( 'NONE',  ( 29.13662752439705272, 0.000000000000000000, 7.500000000000000000 ) ) ;
#11063=LINE ( 'NONE', #18102, #19997 ) ;
#11069=EDGE_CURVE ( 'NONE', #15395, #10953, #4159, .T. ) ;
#11070=ORIENTED_EDGE ( 'NONE', *, *, #18415, .F. ) ;
#11072=DIRECTION ( 'NONE',  ( 0.000000000000000000, 0.000000000000000000, -1.000000000000000000 ) ) ;
#11076=VECTOR ( 'NONE', #7889, 1000.000000000000000 ) ;
#11077=ORIENTED_EDGE ( 'NONE', *, *, #9152, .T. ) ;
#11078=ORIENTED_EDGE ( 'NONE', *, *, #12419, .T. ) ;
#11080=ORIENTED_EDGE ( 'NONE', *, *, #9215, .T. ) ;
#11083=CARTESIAN_POINT ( 'NONE',  ( -29.50000000000002132, 2.473451120191013430, 1.500000000000001332 ) ) ;
#11085=CIRCLE ( 'NONE', #8607, 0.2999999999999999334 ) ;
#11086=AXIS2_PLACEMENT_3D ( 'NONE', #7196, #12423, #558 ) ;
#11088=CARTESIAN_POINT ( 'NONE',  ( -25.37540678000427263, -63.74634676501045050, 7.500000000000000000 ) ) ;
#11089=DIRECTION ( 'NONE',  ( 0.000000000000000000, 0.000000000000000000, -1.000000000000000000 ) ) ;
#11092=DIRECTION ( 'NONE',  ( 0.000000000000000000, 1.000000000000000000, 0.000000000000000000 ) ) ;
#11095=DIRECTION ( 'NONE',  ( 1.000000000000000000, 0.000000000000000000, -2.388292521039847891E-16 ) ) ;
#11097=ORIENTED_EDGE ( 'NONE', *, *, #21217, .F. ) ;
#11099=PLANE ( 'NONE',  #19922 ) ;
#11101=ORIENTED_EDGE ( 'NONE', *, *, #8726, .T. ) ;
#11102=CIRCLE ( 'NONE', #2234, 0.2999999999999999334 ) ;
#11103=CARTESIAN_POINT ( 'NONE',  ( 29.37540678000427619, 6.000000000000000000, 7.500000000000000000 ) ) ;
#11105=DIRECTION ( 'NONE',  ( 1.000000000000000000, 0.000000000000000000, 0.000000000000000000 ) ) ;
#11112=EDGE_CURVE ( 'NONE', #18524, #12867, #5614, .T. ) ;
#11113=DIRECTION ( 'NONE',  ( 1.000000000000000000, 0.000000000000000000, 0.000000000000000000 ) ) ;
#11116=EDGE_LOOP ( 'NONE', ( #3564, #13468, #15646, #14496 ) ) ;
#11117=CARTESIAN_POINT ( 'NONE',  ( 14.96174975910707161, 41.81054587065082728, 68.25000000000000000 ) ) ;
#11119=ORIENTED_EDGE ( 'NONE', *, *, #21260, .T. ) ;
#11120=AXIS2_PLACEMENT_3D ( 'NONE', #1037, #21759, #1145 ) ;
#11125=ORIENTED_EDGE ( 'NONE', *, *, #11516, .T. ) ;
#11127=CARTESIAN_POINT ( 'NONE',  ( 32.50000000000002132, -71.00000000000001421, 3.500000000000000000 ) ) ;
#11128=EDGE_CURVE ( 'NONE', #16858, #5434, #1400, .T. ) ;
#11130=CARTESIAN_POINT ( 'NONE',  ( -30.37540678000427619, -63.74634676501045050, 7.200000000000000178 ) ) ;
#11132=DIRECTION ( 'NONE',  ( 0.000000000000000000, 0.000000000000000000, 1.000000000000000000 ) ) ;
#11138=ORIENTED_EDGE ( 'NONE', *, *, #2961, .T. ) ;
#11142=ADVANCED_FACE ( 'NONE', ( #11479 ), #2982, .T. ) ;
#11146=CARTESIAN_POINT ( 'NONE',  ( -23.02398829872513630, -2.501746539338826292, 13.57884938331724101 ) ) ;
#11148=ORIENTED_EDGE ( 'NONE', *, *, #9520, .F. ) ;
#11149=FACE_OUTER_BOUND ( 'NONE', #13803, .T. ) ;
#11151=EDGE_CURVE ( 'NONE', #1798, #12977, #8817, .T. ) ;
#11152=DIRECTION ( 'NONE',  ( 1.000000000000000000, 0.000000000000000000, 0.000000000000000000 ) ) ;
#11153=VERTEX_POINT ( 'NONE', #21681 ) ;
#11154=ORIENTED_EDGE ( 'NONE', *, *, #11285, .T. ) ;
#11156=VECTOR ( 'NONE', #7509, 1000.000000000000000 ) ;
#11157=EDGE_CURVE ( 'NONE', #19467, #1047, #9920, .T. ) ;
#11158=DIRECTION ( 'NONE',  ( -0.000000000000000000, 1.000000000000000000, 0.000000000000000000 ) ) ;
#11159=CARTESIAN_POINT ( 'NONE',  ( -23.02398829872514341, -2.157133568461118589, 13.20000000000008100 ) ) ;
#11162=DIRECTION ( 'NONE',  ( 0.000000000000000000, 1.000000000000000000, -0.000000000000000000 ) ) ;
#11164=CARTESIAN_POINT ( 'NONE',  ( -29.20000000000002061, -68.70000000000001705, 0.000000000000000000 ) ) ;
#11165=VERTEX_POINT ( 'NONE', #6474 ) ;
#11166=FACE_OUTER_BOUND ( 'NONE', #12183, .T. ) ;
#11169=EDGE_CURVE ( 'NONE', #9425, #19429, #8246, .T. ) ;
#11171=DIRECTION ( 'NONE',  ( 0.000000000000000000, 0.000000000000000000, -1.000000000000000000 ) ) ;
#11172=EDGE_CURVE ( 'NONE', #13253, #2258, #13786, .T. ) ;
#11178=ORIENTED_EDGE ( 'NONE', *, *, #2869, .F. ) ;
#11181=ORIENTED_EDGE ( 'NONE', *, *, #11128, .F. ) ;
#11184=DIRECTION ( 'NONE',  ( 1.000000000000000000, 0.000000000000000000, 0.000000000000000000 ) ) ;
#11186=CARTESIAN_POINT ( 'NONE',  ( 29.50000000000002132, 0.000000000000000000, 1.500000000000000000 ) ) ;
#11189=DIRECTION ( 'NONE',  ( 0.000000000000000000, 0.000000000000000000, 1.000000000000000000 ) ) ;
#11190=DIRECTION ( 'NONE',  ( -0.000000000000000000, -0.000000000000000000, -1.000000000000000000 ) ) ;
#11192=DIRECTION ( 'NONE',  ( 0.000000000000000000, 1.000000000000000000, 0.000000000000000000 ) ) ;
#11193=EDGE_CURVE ( 'NONE', #5317, #11913, #6356, .T. ) ;
#11194=ORIENTED_EDGE ( 'NONE', *, *, #8561, .T. ) ;
#11195=CYLINDRICAL_SURFACE ( 'NONE', #4529, 3.500000000000003109 ) ;
#11197=DIRECTION ( 'NONE',  ( 3.052134192567367925E-16, 1.000000000000000000, -0.000000000000000000 ) ) ;
#11198=ORIENTED_EDGE ( 'NONE', *, *, #11427, .T. ) ;
#11200=DIRECTION ( 'NONE',  ( -2.388292521039847891E-16, 0.000000000000000000, -1.000000000000000000 ) ) ;
#11201=ORIENTED_EDGE ( 'NONE', *, *, #487, .T. ) ;
#11202=ORIENTED_EDGE ( 'NONE', *, *, #13925, .T. ) ;
#11203=CIRCLE ( 'NONE', #2278, 0.5000000000000004441 ) ;
#11205=FACE_OUTER_BOUND ( 'NONE', #19951, .T. ) ;
#11206=AXIS2_PLACEMENT_3D ( 'NONE', #8395, #18576, #17001 ) ;
#11209=DIRECTION ( 'NONE',  ( -1.000000000000000000, -0.000000000000000000, -0.000000000000000000 ) ) ;
#11212=DIRECTION ( 'NONE',  ( -0.000000000000000000, -0.000000000000000000, -1.000000000000000000 ) ) ;
#11213=CARTESIAN_POINT ( 'NONE',  ( -3.127054932750481964, -32.61873716947361856, 68.00000000000000000 ) ) ;
#11214=CARTESIAN_POINT ( 'NONE',  ( -28.86382559268571057, 6.505889654322387194, 13.29319881794719294 ) ) ;
#11215=FACE_OUTER_BOUND ( 'NONE', #357, .T. ) ;
#11216=CARTESIAN_POINT ( 'NONE',  ( -23.26716210542296182, 3.307210766252304701, 13.50000000000000355 ) ) ;
#11220=ORIENTED_EDGE ( 'NONE', *, *, #34, .T. ) ;
#11223=CARTESIAN_POINT ( 'NONE',  ( 14.96174975910705385, 51.80685496129630963, 13.81241846611418644 ) ) ;
#11225=ORIENTED_EDGE ( 'NONE', *, *, #2779, .T. ) ;
#11226=ADVANCED_FACE ( 'NONE', ( #4997 ), #15058, .F. ) ;
#11229=CARTESIAN_POINT ( 'NONE',  ( 14.96174975910705918, -41.81054587065082728, 13.62426406871192874 ) ) ;
#11231=EDGE_CURVE ( 'NONE', #5864, #6786, #1747, .T. ) ;
#11232=LINE ( 'NONE', #21663, #6385 ) ;
#11233=DIRECTION ( 'NONE',  ( 0.000000000000000000, 0.000000000000000000, 1.000000000000000000 ) ) ;
#11236=VERTEX_POINT ( 'NONE', #13156 ) ;
#11237=DIRECTION ( 'NONE',  ( 1.000000000000000000, -0.000000000000000000, -0.000000000000000000 ) ) ;
#11242=AXIS2_PLACEMENT_3D ( 'NONE', #19543, #2537, #20005 ) ;
#11243=VECTOR ( 'NONE', #7535, 1000.000000000000000 ) ;
#11247=DIRECTION ( 'NONE',  ( -1.000000000000000000, 0.000000000000000000, 0.000000000000000000 ) ) ;
#11250=CARTESIAN_POINT ( 'NONE',  ( -15.21174975910704852, 52.39333383871510108, 13.50000000000000000 ) ) ;
#11251=DIRECTION ( 'NONE',  ( 0.000000000000000000, 0.000000000000000000, 1.000000000000000000 ) ) ;
#11253=DIRECTION ( 'NONE',  ( 0.000000000000000000, 1.000000000000000000, 0.000000000000000000 ) ) ;
#11254=EDGE_LOOP ( 'NONE', ( #15957, #14756, #2151, #17309, #4258, #9456 ) ) ;
#11255=ORIENTED_EDGE ( 'NONE', *, *, #12512, .F. ) ;
#11256=DIRECTION ( 'NONE',  ( 0.000000000000000000, 1.000000000000000000, 0.000000000000000000 ) ) ;
#11257=AXIS2_PLACEMENT_3D ( 'NONE', #16840, #13263, #20207 ) ;
#11258=EDGE_CURVE ( 'NONE', #11905, #3329, #3816, .T. ) ;
#11259=CARTESIAN_POINT ( 'NONE',  ( -15.95292532278785913, -52.39333383871510108, 13.79999999999999716 ) ) ;
#11260=DIRECTION ( 'NONE',  ( 0.000000000000000000, 0.000000000000000000, -1.000000000000000000 ) ) ;
#11261=ADVANCED_FACE ( 'NONE', ( #12017 ), #4172, .T. ) ;
#11263=CARTESIAN_POINT ( 'NONE',  ( 25.37540678000427263, 67.24634676501045760, 13.50000000000000000 ) ) ;
#11265=VERTEX_POINT ( 'NONE', #9012 ) ;
#11268=LINE ( 'NONE', #16430, #12103 ) ;
#11269=EDGE_LOOP ( 'NONE', ( #11119, #7264, #12701, #13495, #14361 ) ) ;
#11272=DIRECTION ( 'NONE',  ( 0.000000000000000000, 0.000000000000000000, 1.000000000000000000 ) ) ;
#11275=CIRCLE ( 'NONE', #1631, 0.5000000000000004441 ) ;
#11276=CIRCLE ( 'NONE', #9496, 1.000000000000000000 ) ;
#11279=EDGE_CURVE ( 'NONE', #13182, #15775, #3750, .T. ) ;
#11282=DIRECTION ( 'NONE',  ( 1.000000000000000000, 0.000000000000000000, 0.000000000000000000 ) ) ;
#11283=AXIS2_PLACEMENT_3D ( 'NONE', #17629, #10713, #2198 ) ;
#11285=EDGE_CURVE ( 'NONE', #19432, #19665, #2023, .T. ) ;
#11286=CARTESIAN_POINT ( 'NONE',  ( 27.37540678000427619, 5.683640910026986681, 13.50000000000000000 ) ) ;
#11288=ADVANCED_FACE ( 'NONE', ( #20983 ), #11669, .T. ) ;
#11289=AXIS2_PLACEMENT_3D ( 'NONE', #13908, #7435, #5537 ) ;
#11294=CARTESIAN_POINT ( 'NONE',  ( 25.37540678000427263, -63.74634676501045050, 7.500000000000000000 ) ) ;
#11297=DIRECTION ( 'NONE',  ( -0.000000000000000000, -1.000000000000000000, -0.000000000000000000 ) ) ;
#11298=AXIS2_PLACEMENT_3D ( 'NONE', #16593, #20191, #16388 ) ;
#11299=DIRECTION ( 'NONE',  ( -0.000000000000000000, -1.000000000000000000, -0.000000000000000000 ) ) ;
#11300=VECTOR ( 'NONE', #11237, 1000.000000000000000 ) ;
#11302=CIRCLE ( 'NONE', #18811, 0.2999999999999999334 ) ;
#11304=CARTESIAN_POINT ( 'NONE',  ( 8.641460742840918030, 32.93424481021354921, 68.50000000000000000 ) ) ;
#11306=ORIENTED_EDGE ( 'NONE', *, *, #3173, .F. ) ;
#11308=ORIENTED_EDGE ( 'NONE', *, *, #9821, .T. ) ;
#11314=ORIENTED_EDGE ( 'NONE', *, *, #10993, .T. ) ;
#11317=AXIS2_PLACEMENT_3D ( 'NONE', #20266, #17005, #10092 ) ;
#11318=VERTEX_POINT ( 'NONE', #8789 ) ;
#11320=VECTOR ( 'NONE', #16530, 1000.000000000000000 ) ;
#11321=CARTESIAN_POINT ( 'NONE',  ( 15.07117748393522483, -52.06955913406978453, 13.87289863735440321 ) ) ;
#11323=DIRECTION ( 'NONE',  ( 0.000000000000000000, -0.000000000000000000, -1.000000000000000000 ) ) ;
#11326=DIRECTION ( 'NONE',  ( 1.000000000000000000, 0.000000000000000000, 0.000000000000000000 ) ) ;
#11329=CARTESIAN_POINT ( 'NONE',  ( -23.21392692125925805, 3.086569931169079073, 13.48002932626963712 ) ) ;
#11331=CARTESIAN_POINT ( 'NONE',  ( 15.21174975910705918, -52.39333383871510108, 13.50000000000000000 ) ) ;
#11333=VECTOR ( 'NONE', #14624, 1000.000000000000000 ) ;
#11335=CIRCLE ( 'NONE', #6368, 3.200000000000001510 ) ;
#11336=CIRCLE ( 'NONE', #617, 2.274596669241485181 ) ;
#11339=FACE_OUTER_BOUND ( 'NONE', #11503, .T. ) ;
#11347=AXIS2_PLACEMENT_3D ( 'NONE', #18019, #4488, #4727 ) ;
#11349=DIRECTION ( 'NONE',  ( -1.000000000000000000, 0.000000000000000000, 0.000000000000000000 ) ) ;
#11350=CARTESIAN_POINT ( 'NONE',  ( -9.141460742840918030, 32.61873716947361856, 68.50000000000000000 ) ) ;
#11351=CARTESIAN_POINT ( 'NONE',  ( 3.127054932750481964, -32.11873716947361856, 68.00000000000000000 ) ) ;
#11352=DIRECTION ( 'NONE',  ( 0.000000000000000000, -0.000000000000000000, -1.000000000000000000 ) ) ;
#11354=TOROIDAL_SURFACE ( 'NONE', #1710, 0.2500000000000000000, 0.2500000000000000000 ) ;
#11355=CARTESIAN_POINT ( 'NONE',  ( 0.000000000000000000, 32.11873716947361856, 42.50000000000000711 ) ) ;
#11358=LINE ( 'NONE', #2867, #11300 ) ;
#11361=DIRECTION ( 'NONE',  ( 0.000000000000000000, 0.000000000000000000, -1.000000000000000000 ) ) ;
#11362=ORIENTED_EDGE ( 'NONE', *, *, #7467, .T. ) ;
#11363=EDGE_CURVE ( 'NONE', #20718, #20941, #18556, .T. ) ;
#11365=AXIS2_PLACEMENT_3D ( 'NONE', #19, #3157, #6633 ) ;
#11367=AXIS2_PLACEMENT_3D ( 'NONE', #9028, #5568, #11027 ) ;
#11368=ORIENTED_EDGE ( 'NONE', *, *, #7989, .T. ) ;
#11370=DIRECTION ( 'NONE',  ( 1.000000000000000000, 0.000000000000000000, 0.000000000000000000 ) ) ;
#11371=ORIENTED_EDGE ( 'NONE', *, *, #21873, .F. ) ;
#11372=ORIENTED_EDGE ( 'NONE', *, *, #20023, .F. ) ;
#11374=CARTESIAN_POINT ( 'NONE',  ( -15.21174975910705207, 52.39333383871510108, 13.50000000000000000 ) ) ;
#11375=CARTESIAN_POINT ( 'NONE',  ( 25.37540678000427263, -69.04634676501045476, 3.500000000000000000 ) ) ;
#11376=EDGE_CURVE ( 'NONE', #8891, #11318, #14521, .T. ) ;
#11380=VECTOR ( 'NONE', #10491, 1000.000000000000000 ) ;
#11385=LINE ( 'NONE', #9822, #13121 ) ;
#11386=CARTESIAN_POINT ( 'NONE',  ( -23.02398829872513986, -2.334736181298132873, 13.36928379767489439 ) ) ;
#11387=CARTESIAN_POINT ( 'NONE',  ( -25.37540678000427263, -63.74634676501045050, 7.500000000000000000 ) ) ;
#11388=DIRECTION ( 'NONE',  ( -1.000000000000000000, -0.000000000000000000, -0.000000000000000000 ) ) ;
#11391=ADVANCED_FACE ( 'NONE', ( #20547 ), #12233, .F. ) ;
#11392=LINE ( 'NONE', #8044, #8832 ) ;
#11393=VERTEX_POINT ( 'NONE', #19082 ) ;
#11395=DIRECTION ( 'NONE',  ( 0.000000000000000000, 0.000000000000000000, -1.000000000000000000 ) ) ;
#11397=AXIS2_PLACEMENT_3D ( 'NONE', #7222, #12321, #10559 ) ;
#11399=ORIENTED_EDGE ( 'NONE', *, *, #842, .F. ) ;
#11402=EDGE_CURVE ( 'NONE', #3263, #6391, #19538, .T. ) ;
#11407=CYLINDRICAL_SURFACE ( 'NONE', #11732, 0.5000000000000000000 ) ;
#11410=CARTESIAN_POINT ( 'NONE',  ( -29.13662752439705272, 0.000000000000000000, 13.50000000000000000 ) ) ;
#11412=FACE_OUTER_BOUND ( 'NONE', #14109, .T. ) ;
#11419=DIRECTION ( 'NONE',  ( -0.000000000000000000, -0.000000000000000000, -1.000000000000000000 ) ) ;
#11421=ADVANCED_FACE ( 'NONE', ( #14883 ), #3106, .F. ) ;
#11422=ORIENTED_EDGE ( 'NONE', *, *, #8536, .T. ) ;
#11427=EDGE_CURVE ( 'NONE', #16763, #12996, #5276, .T. ) ;
#11428=PRODUCT ( 'Main Body', 'Main Body', '', ( #7288 ) ) ;
#11431=CARTESIAN_POINT ( 'NONE',  ( 17.95292532278785913, 0.000000000000000000, 68.00000000000000000 ) ) ;
#11432=EDGE_CURVE ( 'NONE', #17106, #9117, #953, .T. ) ;
#11436=VERTEX_POINT ( 'NONE', #17827 ) ;
#11440=CARTESIAN_POINT ( 'NONE',  ( -14.75141514895150152, -52.14252005765846576, 13.50000000000000355 ) ) ;
#11441=AXIS2_PLACEMENT_3D ( 'NONE', #153, #7002, #13792 ) ;
#11448=CARTESIAN_POINT ( 'NONE',  ( -23.06007706085599906, 2.355179835980773628, 13.30024289742314636 ) ) ;
#11450=EDGE_LOOP ( 'NONE', ( #19744, #17550, #17829, #13160 ) ) ;
#11453=ADVANCED_FACE ( 'NONE', ( #17714 ), #12785, .F. ) ;
#11454=CIRCLE ( 'NONE', #18934, 0.2999999999999999334 ) ;
#11460=DIRECTION ( 'NONE',  ( 0.000000000000000000, 0.000000000000000000, -1.000000000000000000 ) ) ;
#11462=LINE ( 'NONE', #18054, #18880 ) ;
#11463=CYLINDRICAL_SURFACE ( 'NONE', #7374, 0.2999999999999999334 ) ;
#11464=EDGE_LOOP ( 'NONE', ( #20085, #21407, #12355, #4946, #19699, #18529 ) ) ;
#11465=DIRECTION ( 'NONE',  ( 0.000000000000000000, 0.000000000000000000, -1.000000000000000000 ) ) ;
#11468=VECTOR ( 'NONE', #15290, 1000.000000000000000 ) ;
#11469=EDGE_CURVE ( 'NONE', #17779, #19855, #20056, .T. ) ;
#11470=DIRECTION ( 'NONE',  ( 1.000000000000000000, 0.000000000000000000, 0.000000000000000000 ) ) ;
#11474=LINE ( 'NONE', #19077, #6656 ) ;
#11479=FACE_OUTER_BOUND ( 'NONE', #21105, .T. ) ;
#11480=ORIENTED_EDGE ( 'NONE', *, *, #7668, .F. ) ;
#11485=CARTESIAN_POINT ( 'NONE',  ( 3.127054932750481964, 32.93424481021354921, 68.00000000000000000 ) ) ;
#11490=CYLINDRICAL_SURFACE ( 'NONE', #18125, 0.5000000000000004441 ) ;
#11491=CARTESIAN_POINT ( 'NONE',  ( -23.32398829872514057, 7.118794219358020148E-15, 13.50000000000000000 ) ) ;
#11493=AXIS2_PLACEMENT_3D ( 'NONE', #5358, #9128, #5569 ) ;
#11494=CARTESIAN_POINT ( 'NONE',  ( 18.22752199202934520, 50.11873716947361856, 13.50000000000000000 ) ) ;
#11496=LINE ( 'NONE', #18325, #4953 ) ;
#11497=ADVANCED_FACE ( 'NONE', ( #8197 ), #4188, .T. ) ;
#11498=AXIS2_PLACEMENT_3D ( 'NONE', #13888, #12634, #15678 ) ;
#11500=AXIS2_PLACEMENT_3D ( 'NONE', #16371, #21432, #19973 ) ;
#11503=EDGE_LOOP ( 'NONE', ( #3351, #4640, #2615, #1537 ) ) ;
#11504=EDGE_CURVE ( 'NONE', #2381, #12853, #2396, .T. ) ;
#11511=VERTEX_POINT ( 'NONE', #7660 ) ;
#11512=FACE_OUTER_BOUND ( 'NONE', #6448, .T. ) ;
#11513=AXIS2_PLACEMENT_3D ( 'NONE', #6055, #17992, #2666 ) ;
#11514=AXIS2_PLACEMENT_3D ( 'NONE', #4242, #9274, #14182 ) ;
#11516=EDGE_CURVE ( 'NONE', #19066, #15364, #8133, .T. ) ;
#11517=DIRECTION ( 'NONE',  ( 0.000000000000000000, 0.000000000000000000, 1.000000000000000000 ) ) ;
#11518=LINE ( 'NONE', #1330, #2751 ) ;
#11520=CIRCLE ( 'NONE', #13308, 2.000000000000000000 ) ;
#11522=DIRECTION ( 'NONE',  ( 1.000000000000000000, 0.000000000000000000, 0.000000000000000000 ) ) ;
#11523=DIRECTION ( 'NONE',  ( 0.000000000000000000, 0.000000000000000000, -1.000000000000000000 ) ) ;
#11525=CARTESIAN_POINT ( 'NONE',  ( 23.02398829872513986, 3.528912754968628551, 13.79999999999999893 ) ) ;
#11527=CARTESIAN_POINT ( 'NONE',  ( -29.13662752439705272, 0.000000000000000000, 7.200000000000000178 ) ) ;
#11528=ORIENTED_EDGE ( 'NONE', *, *, #9485, .F. ) ;
#11529=DIRECTION ( 'NONE',  ( 1.000000000000000000, 0.000000000000000000, 0.000000000000000000 ) ) ;
#11533=LINE ( 'NONE', #16906, #16356 ) ;
#11535=ADVANCED_FACE ( 'NONE', ( #6527 ), #13319, .F. ) ;
#11538=ORIENTED_EDGE ( 'NONE', *, *, #18639, .F. ) ;
#11540=ORIENTED_EDGE ( 'NONE', *, *, #5013, .F. ) ;
#11542=FACE_OUTER_BOUND ( 'NONE', #1712, .T. ) ;
#11543=EDGE_CURVE ( 'NONE', #19547, #3082, #20986, .T. ) ;
#11544=CARTESIAN_POINT ( 'NONE',  ( -30.67540678000428045, 63.74634676501045050, 3.500000000000000000 ) ) ;
#11545=ORIENTED_EDGE ( 'NONE', *, *, #1158, .F. ) ;
#11546=EDGE_CURVE ( 'NONE', #9267, #17841, #10272, .T. ) ;
#11549=DIRECTION ( 'NONE',  ( 0.000000000000000000, 0.000000000000000000, 1.000000000000000000 ) ) ;
#11551=ORIENTED_EDGE ( 'NONE', *, *, #6695, .F. ) ;
#11552=VERTEX_POINT ( 'NONE', #15445 ) ;
#11556=ADVANCED_FACE ( 'NONE', ( #212 ), #6628, .T. ) ;
#11559=VECTOR ( 'NONE', #1557, 1000.000000000000000 ) ;
#11564=CARTESIAN_POINT ( 'NONE',  ( -15.95292532278785913, -52.11873716947361856, 14.00000000000000000 ) ) ;
#11567=ORIENTED_EDGE ( 'NONE', *, *, #10992, .F. ) ;
#11571=DIRECTION ( 'NONE',  ( 0.000000000000000000, 0.000000000000000000, 1.000000000000000000 ) ) ;
#11573=EDGE_LOOP ( 'NONE', ( #2927, #18701, #17807, #21970 ) ) ;
#11575=CARTESIAN_POINT ( 'NONE',  ( -8.641460742840918030, -32.93424481021354921, 68.00000000000000000 ) ) ;
#11578=ORIENTED_EDGE ( 'NONE', *, *, #20353, .F. ) ;
#11584=ORIENTED_EDGE ( 'NONE', *, *, #20245, .T. ) ;
#11585=EDGE_CURVE ( 'NONE', #10953, #18524, #8523, .T. ) ;
#11586=ORIENTED_EDGE ( 'NONE', *, *, #17439, .T. ) ;
#11588=CARTESIAN_POINT ( 'NONE',  ( -14.83748569039512155, -41.93480993936275780, 13.49999999999999822 ) ) ;
#11589=CYLINDRICAL_SURFACE ( 'NONE', #6721, 0.2999999999999999334 ) ;
#11595=ADVANCED_FACE ( 'NONE', ( #6861 ), #10194, .F. ) ;
#11602=ORIENTED_EDGE ( 'NONE', *, *, #9442, .F. ) ;
#11603=DIRECTION ( 'NONE',  ( -1.000000000000000000, 0.000000000000000000, 0.000000000000000000 ) ) ;
#11606=ORIENTED_EDGE ( 'NONE', *, *, #13604, .T. ) ;
#11609=ADVANCED_FACE ( 'NONE', ( #18804 ), #20602, .F. ) ;
#11610=VERTEX_POINT ( 'NONE', #3480 ) ;
#11612=DIRECTION ( 'NONE',  ( 1.000000000000000000, -0.000000000000000000, -0.000000000000000000 ) ) ;
#11618=CARTESIAN_POINT ( 'NONE',  ( -18.22752199202934520, 50.11873716947361856, 13.50000000000000000 ) ) ;
#11619=AXIS2_PLACEMENT_3D ( 'NONE', #5220, #12016, #17178 ) ;
#11621=CIRCLE ( 'NONE', #14126, 2.500000000000002220 ) ;
#11622=DIRECTION ( 'NONE',  ( 0.000000000000000000, 0.000000000000000000, 1.000000000000000000 ) ) ;
#11623=CARTESIAN_POINT ( 'NONE',  ( 26.61833302554978786, 9.663695060508649348, 13.79999999999999893 ) ) ;
#11624=DIRECTION ( 'NONE',  ( 0.000000000000000000, 1.000000000000000000, 0.000000000000000000 ) ) ;
#11625=CARTESIAN_POINT ( 'NONE',  ( 28.90789898151107451, -6.496209923375007911, 7.643284004395015430 ) ) ;
#11629=DIRECTION ( 'NONE',  ( 2.832483164223434527E-16, 1.000000000000000000, -0.000000000000000000 ) ) ;
#11630=AXIS2_PLACEMENT_3D ( 'NONE', #20351, #5361, #5469 ) ;
#11631=TOROIDAL_SURFACE ( 'NONE', #1989, 1.000000000000000000, 0.5000000000000000000 ) ;
#11632=DIRECTION ( 'NONE',  ( 1.000000000000000000, -0.000000000000000000, 0.000000000000000000 ) ) ;
#11635=VERTEX_POINT ( 'NONE', #6963 ) ;
#11637=EDGE_CURVE ( 'NONE', #444, #5889, #11336, .T. ) ;
#11639=EDGE_CURVE ( 'NONE', #9803, #13239, #7068, .T. ) ;
#11641=CIRCLE ( 'NONE', #4510, 5.300000000000006040 ) ;
#11642=EDGE_LOOP ( 'NONE', ( #9876, #1469, #20401, #15836, #5121 ) ) ;
#11643=ORIENTED_EDGE ( 'NONE', *, *, #15099, .F. ) ;
#11646=CIRCLE ( 'NONE', #3460, 2.000000000000001776 ) ;
#11647=VECTOR ( 'NONE', #20328, 1000.000000000000000 ) ;
#11648=PLANE ( 'NONE',  #7465 ) ;
#11649=VECTOR ( 'NONE', #4811, 1000.000000000000000 ) ;
#11650=ORIENTED_EDGE ( 'NONE', *, *, #9538, .F. ) ;
#11652=EDGE_CURVE ( 'NONE', #5901, #10741, #5391, .T. ) ;
#11653=CARTESIAN_POINT ( 'NONE',  ( -23.18284705826593850, 2.947275247953579758, 13.45749238763917610 ) ) ;
#11654=FACE_OUTER_BOUND ( 'NONE', #11573, .T. ) ;
#11656=TOROIDAL_SURFACE ( 'NONE', #14168, 1.500000000000000000, 0.5000000000000000000 ) ;
#11659=ORIENTED_EDGE ( 'NONE', *, *, #9935, .T. ) ;
#11660=ORIENTED_EDGE ( 'NONE', *, *, #49, .T. ) ;
#11663=CARTESIAN_POINT ( 'NONE',  ( -30.07540678000427548, -6.000000000000000000, 7.500000000000000000 ) ) ;
#11664=EDGE_CURVE ( 'NONE', #15364, #2605, #3495, .T. ) ;
#11666=ADVANCED_FACE ( 'NONE', ( #3699 ), #433, .F. ) ;
#11669=TOROIDAL_SURFACE ( 'NONE', #14176, 0.2500000000000000000, 0.2500000000000000000 ) ;
#11670=CARTESIAN_POINT ( 'NONE',  ( 14.96174975910705918, -51.80685496129632384, 13.81241846611418467 ) ) ;
#11671=AXIS2_PLACEMENT_3D ( 'NONE', #18096, #14633, #14845 ) ;
#11672=ORIENTED_EDGE ( 'NONE', *, *, #8618, .F. ) ;
#11673=DIRECTION ( 'NONE',  ( 0.000000000000000000, 0.000000000000000000, 1.000000000000000000 ) ) ;
#11675=CARTESIAN_POINT ( 'NONE',  ( 28.57540678000427548, -63.74634676501045050, 13.19999999999999929 ) ) ;
#11676=CARTESIAN_POINT ( 'NONE',  ( -15.95292532278785913, 50.11873716947361856, 13.79999999999999893 ) ) ;
#11677=DIRECTION ( 'NONE',  ( -0.000000000000000000, 1.000000000000000000, -0.000000000000000000 ) ) ;
#11678=ORIENTED_EDGE ( 'NONE', *, *, #20197, .T. ) ;
#11679=DIRECTION ( 'NONE',  ( -1.000000000000000000, 0.000000000000000000, 0.000000000000000000 ) ) ;
#11681=ADVANCED_FACE ( 'NONE', ( #769 ), #13972, .F. ) ;
#11686=ORIENTED_EDGE ( 'NONE', *, *, #17867, .F. ) ;
#11689=CARTESIAN_POINT ( 'NONE',  ( 0.000000000000000000, -5.299999999999999822, 7.200000000000000178 ) ) ;
#11691=FACE_OUTER_BOUND ( 'NONE', #20178, .T. ) ;
#11693=CARTESIAN_POINT ( 'NONE',  ( 30.07540678000427548, 6.000000000000000000, 7.200000000000000178 ) ) ;
#11695=VERTEX_POINT ( 'NONE', #14410 ) ;
#11697=VERTEX_POINT ( 'NONE', #17456 ) ;
#11698=CARTESIAN_POINT ( 'NONE',  ( -14.66174975910705136, -51.76873716947361714, 13.80000000000000071 ) ) ;
#11701=CARTESIAN_POINT ( 'NONE',  ( -8.641460742840918030, -33.43424481021354921, 68.00000000000000000 ) ) ;
#11702=EDGE_CURVE ( 'NONE', #3289, #2536, #1694, .T. ) ;
#11703=EDGE_LOOP ( 'NONE', ( #16580, #8507, #6557, #8353 ) ) ;
#11708=DIRECTION ( 'NONE',  ( 1.000000000000000000, 0.000000000000000000, 0.000000000000000000 ) ) ;
#11709=AXIS2_PLACEMENT_3D ( 'NONE', #11054, #17873, #8039 ) ;
#11711=DIRECTION ( 'NONE',  ( 0.000000000000000000, 1.000000000000000000, 0.000000000000000000 ) ) ;
#11712=CARTESIAN_POINT ( 'NONE',  ( -23.02398829872513986, -3.528912754968629439, 13.80000000000000071 ) ) ;
#11716=AXIS2_PLACEMENT_3D ( 'NONE', #18884, #17193, #1867 ) ;
#11720=ORIENTED_EDGE ( 'NONE', *, *, #18920, .F. ) ;
#11721=CARTESIAN_POINT ( 'NONE',  ( -3.627054932750481964, -32.61873716947361856, 42.50000000000000000 ) ) ;
#11723=CYLINDRICAL_SURFACE ( 'NONE', #16275, 5.000000000000000888 ) ;
#11724=VECTOR ( 'NONE', #16046, 1000.000000000000000 ) ;
#11725=CIRCLE ( 'NONE', #8532, 0.5000000000000004441 ) ;
#11727=LINE ( 'NONE', #8172, #2815 ) ;
#11732=AXIS2_PLACEMENT_3D ( 'NONE', #21167, #11072, #1207 ) ;
#11733=DIRECTION ( 'NONE',  ( 1.000000000000000000, -0.000000000000000000, -0.000000000000000000 ) ) ;
#11734=VECTOR ( 'NONE', #16874, 1000.000000000000000 ) ;
#11737=FACE_OUTER_BOUND ( 'NONE', #14780, .T. ) ;
#11739=DIRECTION ( 'NONE',  ( 0.000000000000000000, 0.000000000000000000, 1.000000000000000000 ) ) ;
#11742=DIRECTION ( 'NONE',  ( -1.000000000000000000, -0.000000000000000000, -0.000000000000000000 ) ) ;
#11744=CYLINDRICAL_SURFACE ( 'NONE', #3191, 3.500000000000003109 ) ;
#11751=DIRECTION ( 'NONE',  ( -0.000000000000000000, -0.000000000000000000, -1.000000000000000000 ) ) ;
#11752=DIRECTION ( 'NONE',  ( 0.000000000000000000, -1.000000000000000000, 0.000000000000000000 ) ) ;
#11753=ORIENTED_EDGE ( 'NONE', *, *, #4762, .F. ) ;
#11754=CARTESIAN_POINT ( 'NONE',  ( 28.87540678000427619, 0.000000000000000000, 7.799999999999999822 ) ) ;
#11755=ORIENTED_EDGE ( 'NONE', *, *, #18650, .F. ) ;
#11756=VERTEX_POINT ( 'NONE', #15863 ) ;
#11757=CARTESIAN_POINT ( 'NONE',  ( 8.641460742840918030, 32.93424481021354921, 42.50000000000000000 ) ) ;
#11760=( NAMED_UNIT ( * ) SI_UNIT ( $, .STERADIAN. ) SOLID_ANGLE_UNIT ( ) );
#11761=ORIENTED_EDGE ( 'NONE', *, *, #18920, .T. ) ;
#11762=ORIENTED_EDGE ( 'NONE', *, *, #9076, .T. ) ;
#11763=DIRECTION ( 'NONE',  ( 0.000000000000000000, -1.000000000000000000, 0.000000000000000000 ) ) ;
#11764=CARTESIAN_POINT ( 'NONE',  ( 14.66174975910705847, -51.76873716947361004, 13.50000000000000000 ) ) ;
#11765=DIRECTION ( 'NONE',  ( 0.000000000000000000, 0.000000000000000000, 1.000000000000000000 ) ) ;
#11766=AXIS2_PLACEMENT_3D ( 'NONE', #14573, #5984, #14352 ) ;
#11767=CARTESIAN_POINT ( 'NONE',  ( 17.95292532278785913, 0.000000000000000000, 42.50000000000000711 ) ) ;
#11768=EDGE_LOOP ( 'NONE', ( #2569, #16668, #17049, #5715 ) ) ;
#11770=AXIS2_PLACEMENT_3D ( 'NONE', #8761, #3619, #17355 ) ;
#11772=CIRCLE ( 'NONE', #13569, 0.2999999999999999334 ) ;
#11777=ORIENTED_EDGE ( 'NONE', *, *, #9399, .T. ) ;
#11778=ORIENTED_EDGE ( 'NONE', *, *, #16477, .T. ) ;
#11782=VECTOR ( 'NONE', #3858, 1000.000000000000000 ) ;
#11784=ORIENTED_EDGE ( 'NONE', *, *, #13222, .T. ) ;
#11786=CARTESIAN_POINT ( 'NONE',  ( 3.127054932750481964, -32.61873716947361856, 109.6002446535588319 ) ) ;
#11787=DIRECTION ( 'NONE',  ( -1.000000000000000000, 0.000000000000000000, 0.000000000000000000 ) ) ;
#11788=ORIENTED_EDGE ( 'NONE', *, *, #1204, .F. ) ;
#11789=CYLINDRICAL_SURFACE ( 'NONE', #22049, 0.3000000000000016542 ) ;
#11790=DIRECTION ( 'NONE',  ( 0.000000000000000000, -0.000000000000000000, -1.000000000000000000 ) ) ;
#11792=CARTESIAN_POINT ( 'NONE',  ( 17.95292532278785913, 0.000000000000000000, 109.6002446535588319 ) ) ;
#11793=EDGE_CURVE ( 'NONE', #18174, #11393, #1105, .T. ) ;
#11796=DIRECTION ( 'NONE',  ( 0.000000000000000000, 0.000000000000000000, -1.000000000000000000 ) ) ;
#11797=AXIS2_PLACEMENT_3D ( 'NONE', #10857, #4045, #1929 ) ;
#11798=ORIENTED_EDGE ( 'NONE', *, *, #13752, .F. ) ;
#11800=DIRECTION ( 'NONE',  ( 0.000000000000000000, 0.000000000000000000, 1.000000000000000000 ) ) ;
#11802=ORIENTED_EDGE ( 'NONE', *, *, #19313, .F. ) ;
#11804=ORIENTED_EDGE ( 'NONE', *, *, #8754, .F. ) ;
#11806=CARTESIAN_POINT ( 'NONE',  ( -30.37540678000427619, 0.000000000000000000, 7.500000000000000000 ) ) ;
#11807=LINE ( 'NONE', #15283, #696 ) ;
#11808=VERTEX_POINT ( 'NONE', #13190 ) ;
#11809=CYLINDRICAL_SURFACE ( 'NONE', #624, 0.5000000000000004441 ) ;
#11813=ORIENTED_EDGE ( 'NONE', *, *, #3218, .T. ) ;
#11816=CARTESIAN_POINT ( 'NONE',  ( 25.37540678000426908, 38.74634676501045760, 42.50000000000000000 ) ) ;
#11820=CARTESIAN_POINT ( 'NONE',  ( 23.02398829872513986, 2.157133568461118589, 13.20000000000007923 ) ) ;
#11825=CYLINDRICAL_SURFACE ( 'NONE', #7839, 0.5000000000000004441 ) ;
#11828=EDGE_CURVE ( 'NONE', #6444, #14759, #12841, .T. ) ;
#11831=EDGE_LOOP ( 'NONE', ( #21499, #21994, #4548, #7190 ) ) ;
#11833=DIRECTION ( 'NONE',  ( -1.000000000000000000, 0.000000000000000000, 0.000000000000000000 ) ) ;
#11835=ORIENTED_EDGE ( 'NONE', *, *, #9505, .F. ) ;
#11837=DIRECTION ( 'NONE',  ( 1.000000000000000000, 0.000000000000000000, 0.000000000000000000 ) ) ;
#11839=CIRCLE ( 'NONE', #15057, 2.500000000000002220 ) ;
#11840=EDGE_LOOP ( 'NONE', ( #14532, #10155, #8230, #12040 ) ) ;
#11842=CIRCLE ( 'NONE', #13638, 1.984122918275925462 ) ;
#11845=CARTESIAN_POINT ( 'NONE',  ( -29.44760963940965226, 2.533475775848048617, 0.1250376690123979340 ) ) ;
#11846=AXIS2_PLACEMENT_3D ( 'NONE', #36, #20632, #21978 ) ;
#11852=LINE ( 'NONE', #18687, #8261 ) ;
#11854=DIRECTION ( 'NONE',  ( 0.000000000000000000, 0.000000000000000000, 1.000000000000000000 ) ) ;
#11855=DIRECTION ( 'NONE',  ( 1.000000000000000000, 0.000000000000000000, 0.000000000000000000 ) ) ;
#11856=DIRECTION ( 'NONE',  ( -0.000000000000000000, -0.000000000000000000, -1.000000000000000000 ) ) ;
#11857=ORIENTED_EDGE ( 'NONE', *, *, #2779, .F. ) ;
#11860=ORIENTED_EDGE ( 'NONE', *, *, #19331, .F. ) ;
#11862=AXIS2_PLACEMENT_3D ( 'NONE', #19448, #21367, #10942 ) ;
#11864=VERTEX_POINT ( 'NONE', #19689 ) ;
#11865=CARTESIAN_POINT ( 'NONE',  ( 0.000000000000000000, 68.70000000000001705, 0.2999999999999947153 ) ) ;
#11867=VERTEX_POINT ( 'NONE', #2568 ) ;
#11869=ORIENTED_EDGE ( 'NONE', *, *, #1542, .T. ) ;
#11871=ORIENTED_EDGE ( 'NONE', *, *, #49, .F. ) ;
#11872=AXIS2_PLACEMENT_3D ( 'NONE', #867, #21603, #9393 ) ;
#11873=CARTESIAN_POINT ( 'NONE',  ( -25.37540678000426908, 38.74634676501045760, 42.50000000000000000 ) ) ;
#11875=CARTESIAN_POINT ( 'NONE',  ( 0.000000000000000000, -52.11873716947361856, 68.00000000000000000 ) ) ;
#11878=CARTESIAN_POINT ( 'NONE',  ( -23.32398829872514057, 3.528912754968630328, 13.50000000000000000 ) ) ;
#11879=DIRECTION ( 'NONE',  ( -0.000000000000000000, -0.000000000000000000, -1.000000000000000000 ) ) ;
#11880=CARTESIAN_POINT ( 'NONE',  ( -28.87540678000427263, 6.494748934539262386, 7.720760203330568672 ) ) ;
#11881=DIRECTION ( 'NONE',  ( 0.000000000000000000, 0.000000000000000000, 1.000000000000000000 ) ) ;
#11882=VECTOR ( 'NONE', #6983, 1000.000000000000000 ) ;
#11883=DIRECTION ( 'NONE',  ( -1.000000000000000000, 0.000000000000000000, 0.000000000000000000 ) ) ;
#11890=VERTEX_POINT ( 'NONE', #1319 ) ;
#11895=CARTESIAN_POINT ( 'NONE',  ( 15.95292532278785913, 51.61873716947361856, 14.00000000000000000 ) ) ;
#11898=DIRECTION ( 'NONE',  ( 0.000000000000000000, 0.000000000000000000, 1.000000000000000000 ) ) ;
#11901=DIRECTION ( 'NONE',  ( -0.000000000000000000, 1.000000000000000000, 0.000000000000000000 ) ) ;
#11902=CARTESIAN_POINT ( 'NONE',  ( 27.37540678000426908, 36.74634676501047181, 42.50000000000000000 ) ) ;
#11903=CARTESIAN_POINT ( 'NONE',  ( 14.96174975910707161, -51.61873716947361856, 68.00000000000000000 ) ) ;
#11904=DIRECTION ( 'NONE',  ( -1.000000000000000000, 0.000000000000000000, 0.000000000000000000 ) ) ;
#11905=VERTEX_POINT ( 'NONE', #21378 ) ;
#11907=ORIENTED_EDGE ( 'NONE', *, *, #19073, .F. ) ;
#11910=DIRECTION ( 'NONE',  ( -0.000000000000000000, 1.000000000000000000, -0.000000000000000000 ) ) ;
#11911=EDGE_CURVE ( 'NONE', #4141, #2085, #6168, .T. ) ;
#11913=VERTEX_POINT ( 'NONE', #16194 ) ;
#11915=CARTESIAN_POINT ( 'NONE',  ( 15.95292532278785913, -50.11873716947361856, 13.79999999999999893 ) ) ;
#11921=EDGE_CURVE ( 'NONE', #11695, #1150, #101, .T. ) ;
#11922=ORIENTED_EDGE ( 'NONE', *, *, #9251, .F. ) ;
#11923=CARTESIAN_POINT ( 'NONE',  ( -29.37540678000427619, -6.000000000000000000, 3.500000000000000000 ) ) ;
#11926=CARTESIAN_POINT ( 'NONE',  ( -23.32398829872514057, -3.528912754968629439, 13.50000000000000178 ) ) ;
#11930=EDGE_LOOP ( 'NONE', ( #4474, #17741, #1375, #8413 ) ) ;
#11931=FACE_OUTER_BOUND ( 'NONE', #21854, .T. ) ;
#11932=CIRCLE ( 'NONE', #11206, 4.351418481279133665 ) ;
#11934=CARTESIAN_POINT ( 'NONE',  ( -31.50000000000002132, 71.00000000000001421, 3.200000000000000178 ) ) ;
#11936=ORIENTED_EDGE ( 'NONE', *, *, #15438, .T. ) ;
#11940=LINE ( 'NONE', #9950, #1264 ) ;
#11941=ORIENTED_EDGE ( 'NONE', *, *, #17702, .F. ) ;
#11945=DIRECTION ( 'NONE',  ( 0.000000000000000000, 0.000000000000000000, 1.000000000000000000 ) ) ;
#11948=ORIENTED_EDGE ( 'NONE', *, *, #960, .T. ) ;
#11950=DIRECTION ( 'NONE',  ( 0.000000000000000000, 0.000000000000000000, 1.000000000000000000 ) ) ;
#11954=CARTESIAN_POINT ( 'NONE',  ( -31.50000000000002132, -71.00000000000001421, 1.800000000000000044 ) ) ;
#11958=EDGE_CURVE ( 'NONE', #5997, #19359, #8380, .T. ) ;
#11959=FACE_OUTER_BOUND ( 'NONE', #7995, .T. ) ;
#11960=CARTESIAN_POINT ( 'NONE',  ( -29.37540678000427619, -5.299999999999999822, 7.500000000000000000 ) ) ;
#11964=DIRECTION ( 'NONE',  ( -1.000000000000000000, 0.000000000000000000, 0.000000000000000000 ) ) ;
#11965=LINE ( 'NONE', #1459, #5967 ) ;
#11967=EDGE_LOOP ( 'NONE', ( #19782, #20099, #7159, #2287 ) ) ;
#11968=DIRECTION ( 'NONE',  ( 0.000000000000000000, 0.000000000000000000, 1.000000000000000000 ) ) ;
#11971=ORIENTED_EDGE ( 'NONE', *, *, #18680, .F. ) ;
#11972=ADVANCED_FACE ( 'NONE', ( #3455 ), #8276, .F. ) ;
#11974=VERTEX_POINT ( 'NONE', #18441 ) ;
#11977=AXIS2_PLACEMENT_3D ( 'NONE', #13391, #15411, #15300 ) ;
#11978=ORIENTED_EDGE ( 'NONE', *, *, #15767, .F. ) ;
#11979=CARTESIAN_POINT ( 'NONE',  ( 25.37540678000427263, 67.24634676501045760, 7.799999999999999822 ) ) ;
#11982=CARTESIAN_POINT ( 'NONE',  ( -29.13662752439705272, 5.299999999999999822, 7.200000000000000178 ) ) ;
#11983=CARTESIAN_POINT ( 'NONE',  ( -17.95292532278785913, 34.11873716947361856, 42.50000000000000711 ) ) ;
#11984=DIRECTION ( 'NONE',  ( -1.000000000000000000, 0.000000000000000000, 0.000000000000000000 ) ) ;
#11985=DIRECTION ( 'NONE',  ( 0.000000000000000000, 0.000000000000000000, 1.000000000000000000 ) ) ;
#11986=CYLINDRICAL_SURFACE ( 'NONE', #9276, 0.5000000000000004441 ) ;
#11989=PLANE ( 'NONE',  #9729 ) ;
#11990=CIRCLE ( 'NONE', #14495, 0.2500000000000002220 ) ;
#11991=ORIENTED_EDGE ( 'NONE', *, *, #14359, .F. ) ;
#11992=VECTOR ( 'NONE', #17822, 1000.000000000000000 ) ;
#11993=VECTOR ( 'NONE', #17495, 1000.000000000000000 ) ;
#11995=CARTESIAN_POINT ( 'NONE',  ( 30.67540678000428045, -6.000000000000000000, 3.500000000000000000 ) ) ;
#11997=ORIENTED_EDGE ( 'NONE', *, *, #18318, .F. ) ;
#12003=DIRECTION ( 'NONE',  ( 0.000000000000000000, 0.000000000000000000, 1.000000000000000000 ) ) ;
#12005=CIRCLE ( 'NONE', #19175, 4.351418481279137218 ) ;
#12008=DIRECTION ( 'NONE',  ( 0.000000000000000000, 0.000000000000000000, 1.000000000000000000 ) ) ;
#12012=CARTESIAN_POINT ( 'NONE',  ( -14.96174975910705207, 51.76873716947361714, 13.79999999999999716 ) ) ;
#12013=EDGE_CURVE ( 'NONE', #10473, #1026, #21377, .T. ) ;
#12016=DIRECTION ( 'NONE',  ( -0.000000000000000000, 0.000000000000000000, 1.000000000000000000 ) ) ;
#12017=FACE_OUTER_BOUND ( 'NONE', #9682, .T. ) ;
#12020=ORIENTED_EDGE ( 'NONE', *, *, #2295, .F. ) ;
#12022=AXIS2_PLACEMENT_3D ( 'NONE', #20443, #16734, #5111 ) ;
#12023=VERTEX_POINT ( 'NONE', #18903 ) ;
#12026=LINE ( 'NONE', #20669, #20670 ) ;
#12028=CIRCLE ( 'NONE', #14512, 0.5000000000000004441 ) ;
#12032=CARTESIAN_POINT ( 'NONE',  ( -23.20993114852232964, -3.065002284660066412, 13.47295189337462418 ) ) ;
#12033=VECTOR ( 'NONE', #18598, 1000.000000000000000 ) ;
#12034=CARTESIAN_POINT ( 'NONE',  ( -15.95292532278785913, 51.61873716947361856, 68.50000000000000000 ) ) ;
#12035=ADVANCED_FACE ( 'NONE', ( #15425 ), #17211, .T. ) ;
#12037=AXIS2_PLACEMENT_3D ( 'NONE', #10420, #6746, #16788 ) ;
#12040=ORIENTED_EDGE ( 'NONE', *, *, #12652, .T. ) ;
#12041=CARTESIAN_POINT ( 'NONE',  ( 23.02398829872514696, 2.334736181298144864, 13.36928379767489616 ) ) ;
#12042=CARTESIAN_POINT ( 'NONE',  ( 15.95292532278785913, -34.11873716947361856, 42.50000000000000711 ) ) ;
#12046=ORIENTED_EDGE ( 'NONE', *, *, #19114, .T. ) ;
#12047=CARTESIAN_POINT ( 'NONE',  ( -29.37540678000427619, 6.000000000000000000, 3.500000000000000000 ) ) ;
#12049=DIRECTION ( 'NONE',  ( 1.000000000000000000, 0.000000000000000000, 0.000000000000000000 ) ) ;
#12050=ORIENTED_EDGE ( 'NONE', *, *, #11652, .F. ) ;
#12052=DIRECTION ( 'NONE',  ( 0.000000000000000000, 0.000000000000000000, -1.000000000000000000 ) ) ;
#12053=CIRCLE ( 'NONE', #5296, 2.800000000000003819 ) ;
#12063=DIRECTION ( 'NONE',  ( 0.000000000000000000, -1.000000000000000000, -0.000000000000000000 ) ) ;
#12064=ORIENTED_EDGE ( 'NONE', *, *, #12900, .F. ) ;
#12067=DIRECTION ( 'NONE',  ( -0.000000000000000000, -0.000000000000000000, -1.000000000000000000 ) ) ;
#12068=AXIS2_PLACEMENT_3D ( 'NONE', #10151, #18652, #20458 ) ;
#12072=EDGE_CURVE ( 'NONE', #17577, #8891, #15992, .T. ) ;
#12073=CIRCLE ( 'NONE', #18147, 1.000000000000000888 ) ;
#12075=AXIS2_PLACEMENT_3D ( 'NONE', #8432, #15892, #20748 ) ;
#12077=ORIENTED_EDGE ( 'NONE', *, *, #5363, .T. ) ;
#12083=ORIENTED_EDGE ( 'NONE', *, *, #8192, .T. ) ;
#12084=LINE ( 'NONE', #10638, #13863 ) ;
#12087=AXIS2_PLACEMENT_3D ( 'NONE', #1429, #14969, #4795 ) ;
#12090=CARTESIAN_POINT ( 'NONE',  ( 23.02398829872513986, -2.876860926786022787, 13.71498478227960227 ) ) ;
#12092=AXIS2_PLACEMENT_3D ( 'NONE', #10157, #6710, #16973 ) ;
#12094=AXIS2_PLACEMENT_3D ( 'NONE', #3238, #1434, #3009 ) ;
#12096=CYLINDRICAL_SURFACE ( 'NONE', #5992, 0.5000000000000004441 ) ;
#12097=CARTESIAN_POINT ( 'NONE',  ( 23.02398829872513986, 2.279713943076942417, 13.43059441564925116 ) ) ;
#12098=DIRECTION ( 'NONE',  ( -1.000000000000000000, 0.000000000000000000, 0.000000000000000000 ) ) ;
#12099=EDGE_CURVE ( 'NONE', #16241, #4674, #1979, .T. ) ;
#12100=CARTESIAN_POINT ( 'NONE',  ( 3.127054932750481964, 32.61873716947361856, 68.50000000000000000 ) ) ;
#12101=ADVANCED_FACE ( 'NONE', ( #7267 ), #9047, .F. ) ;
#12102=LINE ( 'NONE', #15465, #19008 ) ;
#12103=VECTOR ( 'NONE', #1098, 1000.000000000000000 ) ;
#12104=CARTESIAN_POINT ( 'NONE',  ( 30.37540678000427619, -6.000000000000000000, 7.200000000000000178 ) ) ;
#12105=FACE_OUTER_BOUND ( 'NONE', #14525, .T. ) ;
#12106=EDGE_CURVE ( 'NONE', #19588, #17808, #8827, .T. ) ;
#12108=AXIS2_PLACEMENT_3D ( 'NONE', #8893, #7116, #15698 ) ;
#12109=EDGE_LOOP ( 'NONE', ( #14705, #6962, #10449, #599 ) ) ;
#12111=CARTESIAN_POINT ( 'NONE',  ( 17.45292532278785913, 50.11873716947361856, 68.50000000000000000 ) ) ;
#12112=CARTESIAN_POINT ( 'NONE',  ( 3.127054932750481964, -33.43424481021354921, 68.50000000000000000 ) ) ;
#12113=ORIENTED_EDGE ( 'NONE', *, *, #13222, .F. ) ;
#12114=EDGE_CURVE ( 'NONE', #13197, #4860, #19572, .T. ) ;
#12117=TOROIDAL_SURFACE ( 'NONE', #18553, 0.7000000000000000666, 0.2999999999999999889 ) ;
#12119=ORIENTED_EDGE ( 'NONE', *, *, #2948, .T. ) ;
#12120=CARTESIAN_POINT ( 'NONE',  ( -9.641460742840918030, -32.61873716947361856, 68.00000000000000000 ) ) ;
#12121=CARTESIAN_POINT ( 'NONE',  ( -3.127054932750481964, -32.61873716947361856, 68.00000000000000000 ) ) ;
#12123=DIRECTION ( 'NONE',  ( 1.000000000000000000, 0.000000000000000000, 0.000000000000000000 ) ) ;
#12124=CARTESIAN_POINT ( 'NONE',  ( 14.96174975910705918, -41.81054587065082728, 13.80000000000001315 ) ) ;
#12125=LINE ( 'NONE', #12325, #21653 ) ;
#12128=DIRECTION ( 'NONE',  ( 0.000000000000000000, 0.000000000000000000, -1.000000000000000000 ) ) ;
#12132=EDGE_LOOP ( 'NONE', ( #1626, #358, #13700, #12601 ) ) ;
#12135=DIRECTION ( 'NONE',  ( 1.000000000000000000, 0.000000000000000000, 0.000000000000000000 ) ) ;
#12139=ORIENTED_EDGE ( 'NONE', *, *, #12106, .F. ) ;
#12140=CYLINDRICAL_SURFACE ( 'NONE', #14676, 2.000000000000001776 ) ;
#12141=ADVANCED_FACE ( 'NONE', ( #12376 ), #5814, .F. ) ;
#12146=CARTESIAN_POINT ( 'NONE',  ( -9.141460742840918030, -33.43424481021354921, 42.50000000000000000 ) ) ;
#12148=CARTESIAN_POINT ( 'NONE',  ( 23.29450335057348198, 3.413880037201885820, 13.50000000000000178 ) ) ;
#12151=CIRCLE ( 'NONE', #732, 0.2999999999999999334 ) ;
#12152=FACE_OUTER_BOUND ( 'NONE', #1865, .T. ) ;
#12159=EDGE_LOOP ( 'NONE', ( #16348, #19136, #18539, #12759 ) ) ;
#12160=DIRECTION ( 'NONE',  ( -0.000000000000000000, -0.000000000000000000, -1.000000000000000000 ) ) ;
#12168=FACE_OUTER_BOUND ( 'NONE', #21080, .T. ) ;
#12176=CYLINDRICAL_SURFACE ( 'NONE', #18559, 4.351418481279137218 ) ;
#12179=DIRECTION ( 'NONE',  ( -0.000000000000000000, -0.000000000000000000, 1.000000000000000000 ) ) ;
#12180=CARTESIAN_POINT ( 'NONE',  ( -29.13662752439705272, 0.000000000000000000, -18.50000000000000000 ) ) ;
#12181=AXIS2_PLACEMENT_3D ( 'NONE', #14905, #2952, #2607 ) ;
#12182=ADVANCED_FACE ( 'NONE', ( #2318 ), #11354, .T. ) ;
#12183=EDGE_LOOP ( 'NONE', ( #4751, #6951, #15017, #10330 ) ) ;
#12184=ORIENTED_EDGE ( 'NONE', *, *, #4636, .F. ) ;
#12188=VERTEX_POINT ( 'NONE', #12264 ) ;
#12191=CARTESIAN_POINT ( 'NONE',  ( 23.02398829872513986, -3.418849134688107139, 13.52821124852847134 ) ) ;
#12193=EDGE_LOOP ( 'NONE', ( #18636, #10781, #14620, #15843, #9388 ) ) ;
#12195=FACE_OUTER_BOUND ( 'NONE', #20617, .T. ) ;
#12197=AXIS2_PLACEMENT_3D ( 'NONE', #10710, #17526, #2195 ) ;
#12199=AXIS2_PLACEMENT_3D ( 'NONE', #14771, #6289, #4610 ) ;
#12201=VECTOR ( 'NONE', #2801, 1000.000000000000000 ) ;
#12202=AXIS2_PLACEMENT_3D ( 'NONE', #19123, #8510, #15327 ) ;
#12203=DIRECTION ( 'NONE',  ( 0.000000000000000000, -0.000000000000000000, -1.000000000000000000 ) ) ;
#12204=CARTESIAN_POINT ( 'NONE',  ( 23.04273156199908357, -2.261510999192740901, 13.19999999999999929 ) ) ;
#12207=DIRECTION ( 'NONE',  ( 0.000000000000000000, 0.000000000000000000, 1.000000000000000000 ) ) ;
#12208=EDGE_LOOP ( 'NONE', ( #9732, #1030, #19491, #9512, #9744, #12209 ) ) ;
#12209=ORIENTED_EDGE ( 'NONE', *, *, #345, .F. ) ;
#12213=EDGE_CURVE ( 'NONE', #2230, #20083, #8940, .T. ) ;
#12216=CIRCLE ( 'NONE', #14012, 0.2999999999999999334 ) ;
#12217=EDGE_CURVE ( 'NONE', #21878, #9228, #16070, .T. ) ;
#12218=EDGE_CURVE ( 'NONE', #483, #17330, #16412, .T. ) ;
#12220=CARTESIAN_POINT ( 'NONE',  ( 29.17540678000427690, 0.000000000000000000, 7.799999999999999822 ) ) ;
#12221=ORIENTED_EDGE ( 'NONE', *, *, #17047, .F. ) ;
#12222=DIRECTION ( 'NONE',  ( 0.000000000000000000, 0.000000000000000000, -1.000000000000000000 ) ) ;
#12227=DIRECTION ( 'NONE',  ( 1.000000000000000000, 0.000000000000000000, 0.000000000000000000 ) ) ;
#12228=DIRECTION ( 'NONE',  ( 1.000000000000000000, -0.000000000000000000, -0.000000000000000000 ) ) ;
#12229=EDGE_CURVE ( 'NONE', #10879, #7401, #266, .T. ) ;
#12230=EDGE_LOOP ( 'NONE', ( #19281, #3789, #14317, #19846, #21498, #11907 ) ) ;
#12231=CARTESIAN_POINT ( 'NONE',  ( -3.627054932750481964, 32.93424481021354921, 13.50000000000000000 ) ) ;
#12232=DIRECTION ( 'NONE',  ( 0.000000000000000000, 0.000000000000000000, 1.000000000000000000 ) ) ;
#12233=PLANE ( 'NONE',  #6704 ) ;
#12234=ORIENTED_EDGE ( 'NONE', *, *, #19816, .T. ) ;
#12236=VERTEX_POINT ( 'NONE', #2545 ) ;
#12237=CARTESIAN_POINT ( 'NONE',  ( 23.02398829872513986, 7.027230193580998154E-15, 42.50000000000000000 ) ) ;
#12242=DIRECTION ( 'NONE',  ( -0.000000000000000000, -0.000000000000000000, -1.000000000000000000 ) ) ;
#12243=EDGE_CURVE ( 'NONE', #1577, #20269, #20295, .T. ) ;
#12247=CARTESIAN_POINT ( 'NONE',  ( -29.17540678000427690, -6.499884319688664647, 7.500000000000000000 ) ) ;
#12250=CARTESIAN_POINT ( 'NONE',  ( 29.13662752439705272, 0.000000000000000000, 0.3000000000000016542 ) ) ;
#12252=CARTESIAN_POINT ( 'NONE',  ( 3.127054932750481964, -32.93424481021354921, 68.00000000000000000 ) ) ;
#12253=CARTESIAN_POINT ( 'NONE',  ( -25.37540678000429395, -39.04634676501046187, 13.79999999999999893 ) ) ;
#12256=ORIENTED_EDGE ( 'NONE', *, *, #3942, .F. ) ;
#12257=CYLINDRICAL_SURFACE ( 'NONE', #2321, 0.5000000000000004441 ) ;
#12259=( BOUNDED_SURFACE ( )  B_SPLINE_SURFACE ( 3, 2, ( 
 ( #11820, #5131, #10593 ),
 ( #1964, #16972, #19101 ),
 ( #294, #17097, #18769 ),
 ( #8811, #12041, #7033 ),
 ( #1871, #13827, #18890 ),
 ( #18658, #10276, #3442 ),
 ( #8605, #20791, #3770 ),
 ( #8485, #20685, #1215 ),
 ( #5243, #15302, #15413 ),
 ( #87, #13716, #3565 ),
 ( #8066, #14871, #12148 ),
 ( #10389, #179, #3670 ) ),
 .UNSPECIFIED., .F., .F., .T. ) 
 B_SPLINE_SURFACE_WITH_KNOTS ( ( 4, 2, 2, 2, 2, 4 ),
 ( 3, 3 ),
 ( 0.0007953085288493483155, 0.0009951922240469498245, 0.001195075919244551225, 0.001594843309639754243, 0.001994610700034957045, 0.002394378090430160280 ),
 ( 0.000000000000000000, 1.000000000000000000 ),
 .UNSPECIFIED. ) 
 GEOMETRIC_REPRESENTATION_ITEM ( )  RATIONAL_B_SPLINE_SURFACE ( (
 ( 1.000000000000000000, 0.9842566880020464648, 1.000000000000000000),
 ( 1.000000000000000000, 0.9842682545141110406, 1.000000000000000000),
 ( 1.000000000000000000, 0.9790935905989446297, 1.000000000000000000),
 ( 1.000000000000000000, 0.9652215946044104822, 1.000000000000000000),
 ( 1.000000000000000000, 0.9566241109334278070, 1.000000000000000000),
 ( 1.000000000000000000, 0.9283687200450853050, 1.000000000000000000),
 ( 1.000000000000000000, 0.9065874062052554638, 1.000000000000000000),
 ( 1.000000000000000000, 0.8577429740253610380, 1.000000000000000000),
 ( 1.000000000000000000, 0.8312249658974324440, 1.000000000000000000),
 ( 1.000000000000000000, 0.7732701221512614520, 1.000000000000000000),
 ( 1.000000000000000000, 0.7418345472258666140, 1.000000000000000000),
 ( 1.000000000000000000, 0.7071067811865475727, 1.000000000000000000) ) ) 
 REPRESENTATION_ITEM ( '' )  SURFACE ( )  );
#12261=EDGE_LOOP ( 'NONE', ( #6147, #12119, #7952, #3370 ) ) ;
#12262=DIRECTION ( 'NONE',  ( 0.000000000000000000, -1.000000000000000000, 0.000000000000000000 ) ) ;
#12264=CARTESIAN_POINT ( 'NONE',  ( 17.95292532278785913, -50.11873716947361856, 13.99999999999999822 ) ) ;
#12269=ORIENTED_EDGE ( 'NONE', *, *, #7943, .F. ) ;
#12271=AXIS2_PLACEMENT_3D ( 'NONE', #15439, #5051, #20052 ) ;
#12273=AXIS2_PLACEMENT_3D ( 'NONE', #2530, #16161, #21340 ) ;
#12274=DIRECTION ( 'NONE',  ( 1.000000000000000000, 0.000000000000000000, -2.388292521039847891E-16 ) ) ;
#12278=CARTESIAN_POINT ( 'NONE',  ( 29.44686415200675711, 2.575389668538635046, 0.1239436336148718037 ) ) ;
#12283=ORIENTED_EDGE ( 'NONE', *, *, #6338, .T. ) ;
#12284=EDGE_CURVE ( 'NONE', #13976, #9183, #1183, .T. ) ;
#12287=CARTESIAN_POINT ( 'NONE',  ( -29.17540678000427690, 63.74634676501045050, 7.799999999999999822 ) ) ;
#12290=CARTESIAN_POINT ( 'NONE',  ( -17.95292532278785913, -50.11873716947361856, 68.00000000000000000 ) ) ;
#12291=ORIENTED_EDGE ( 'NONE', *, *, #4734, .F. ) ;
#12294=CARTESIAN_POINT ( 'NONE',  ( 27.37540678000427974, -10.94079601157914716, 13.79999999999999893 ) ) ;
#12298=CIRCLE ( 'NONE', #13388, 0.2999999999999999334 ) ;
#12299=CIRCLE ( 'NONE', #2672, 0.2999999999999999334 ) ;
#12300=CARTESIAN_POINT ( 'NONE',  ( -23.02398829872514341, 2.624711895713190302, 13.63074282194510189 ) ) ;
#12301=DIRECTION ( 'NONE',  ( -0.000000000000000000, -1.000000000000000000, -0.000000000000000000 ) ) ;
#12303=DIRECTION ( 'NONE',  ( -1.000000000000000000, 0.000000000000000000, 0.000000000000000000 ) ) ;
#12304=ADVANCED_FACE ( 'NONE', ( #2888 ), #9715, .T. ) ;
#12305=DIRECTION ( 'NONE',  ( -1.000000000000000000, 0.000000000000000000, 0.000000000000000000 ) ) ;
#12307=ORIENTED_EDGE ( 'NONE', *, *, #2588, .T. ) ;
#12308=DIRECTION ( 'NONE',  ( -1.000000000000000000, 0.000000000000000000, 0.000000000000000000 ) ) ;
#12310=VERTEX_POINT ( 'NONE', #7695 ) ;
#12311=TOROIDAL_SURFACE ( 'NONE', #14471, 4.051418481279137396, 0.2999999999999999889 ) ;
#12312=FACE_OUTER_BOUND ( 'NONE', #5442, .T. ) ;
#12314=ORIENTED_EDGE ( 'NONE', *, *, #20474, .F. ) ;
#12317=DIRECTION ( 'NONE',  ( 0.000000000000000000, -0.000000000000000000, -1.000000000000000000 ) ) ;
#12318=CIRCLE ( 'NONE', #6652, 0.2999999999999999334 ) ;
#12320=FACE_BOUND ( 'NONE', #1472, .T. ) ;
#12321=DIRECTION ( 'NONE',  ( 0.000000000000000000, 1.000000000000000000, -0.000000000000000000 ) ) ;
#12322=LINE ( 'NONE', #9325, #19710 ) ;
#12325=CARTESIAN_POINT ( 'NONE',  ( -29.17540678000427690, 0.000000000000000000, 7.500000000000000000 ) ) ;
#12326=AXIS2_PLACEMENT_3D ( 'NONE', #4149, #7407, #5515 ) ;
#12327=MECHANICAL_DESIGN_GEOMETRIC_PRESENTATION_REPRESENTATION('',(#522),#2336);
#12328=VECTOR ( 'NONE', #10816, 1000.000000000000000 ) ;
#12329=ADVANCED_FACE ( 'NONE', ( #14618 ), #851, .T. ) ;
#12330=VERTEX_POINT ( 'NONE', #2765 ) ;
#12333=EDGE_CURVE ( 'NONE', #9267, #13403, #21044, .T. ) ;
#12335=ORIENTED_EDGE ( 'NONE', *, *, #9994, .F. ) ;
#12337=ORIENTED_EDGE ( 'NONE', *, *, #15931, .T. ) ;
#12338=CARTESIAN_POINT ( 'NONE',  ( -29.09616841400578124, -6.500357067309672665, 7.499999999999999112 ) ) ;
#12340=CARTESIAN_POINT ( 'NONE',  ( 25.37540678000429395, -39.04634676501046187, 13.79999999999999893 ) ) ;
#12345=VECTOR ( 'NONE', #5300, 1000.000000000000000 ) ;
#12348=CIRCLE ( 'NONE', #20238, 4.700000000000002842 ) ;
#12350=ORIENTED_EDGE ( 'NONE', *, *, #4213, .T. ) ;
#12351=CARTESIAN_POINT ( 'NONE',  ( 25.37540678000429395, -38.74634676501045760, 42.50000000000000000 ) ) ;
#12352=CARTESIAN_POINT ( 'NONE',  ( -25.37540678000426908, 36.74634676501047181, 13.50000000000000000 ) ) ;
#12354=DIRECTION ( 'NONE',  ( 1.000000000000000000, 0.000000000000000000, 0.000000000000000000 ) ) ;
#12355=ORIENTED_EDGE ( 'NONE', *, *, #9770, .F. ) ;
#12358=DIRECTION ( 'NONE',  ( 0.000000000000000000, 0.000000000000000000, 1.000000000000000000 ) ) ;
#12361=VECTOR ( 'NONE', #18053, 1000.000000000000000 ) ;
#12363=AXIS2_PLACEMENT_3D ( 'NONE', #15275, #22007, #18634 ) ;
#12365=AXIS2_PLACEMENT_3D ( 'NONE', #16778, #8390, #1448 ) ;
#12366=ADVANCED_FACE ( 'NONE', ( #2649 ), #304, .F. ) ;
#12368=CARTESIAN_POINT ( 'NONE',  ( 17.95292532278785913, 50.11873716947361856, 13.99999999999999822 ) ) ;
#12371=EDGE_LOOP ( 'NONE', ( #4164, #8036, #2007, #5343 ) ) ;
#12372=CIRCLE ( 'NONE', #4163, 3.500000000000003109 ) ;
#12375=EDGE_CURVE ( 'NONE', #8611, #16245, #15234, .T. ) ;
#12376=FACE_OUTER_BOUND ( 'NONE', #17647, .T. ) ;
#12377=ORIENTED_EDGE ( 'NONE', *, *, #13546, .T. ) ;
#12378=TOROIDAL_SURFACE ( 'NONE', #15956, 2.274596669241483848, 0.2999999999999999889 ) ;
#12380=VECTOR ( 'NONE', #4707, 1000.000000000000000 ) ;
#12383=EDGE_CURVE ( 'NONE', #10729, #17715, #130, .T. ) ;
#12385=DIRECTION ( 'NONE',  ( 1.000000000000000000, 0.000000000000000000, 0.000000000000000000 ) ) ;
#12386=AXIS2_PLACEMENT_3D ( 'NONE', #3845, #6894, #14106 ) ;
#12387=AXIS2_PLACEMENT_3D ( 'NONE', #15063, #4439, #18077 ) ;
#12390=EDGE_CURVE ( 'NONE', #17937, #21191, #9952, .T. ) ;
#12392=( BOUNDED_CURVE ( )  B_SPLINE_CURVE ( 3, ( #17099, #22156, #21923, #8267 ),
 .UNSPECIFIED., .F., .T. ) 
 B_SPLINE_CURVE_WITH_KNOTS ( ( 4, 4 ),
 ( 4.712388980384689674, 6.283185307179586232 ),
 .UNSPECIFIED. ) 
 CURVE ( )  GEOMETRIC_REPRESENTATION_ITEM ( )  RATIONAL_B_SPLINE_CURVE ( ( 1.000000000000000000, 0.8047378541243649375, 0.8047378541243649375, 1.000000000000000000 ) ) 
 REPRESENTATION_ITEM ( '' )  );
#12395=VECTOR ( 'NONE', #13278, 1000.000000000000000 ) ;
#12396=AXIS2_PLACEMENT_3D ( 'NONE', #5266, #18679, #13534 ) ;
#12398=EDGE_CURVE ( 'NONE', #12330, #8378, #11725, .T. ) ;
#12400=DIRECTION ( 'NONE',  ( -0.000000000000000000, -0.000000000000000000, -1.000000000000000000 ) ) ;
#12403=ORIENTED_EDGE ( 'NONE', *, *, #21199, .T. ) ;
#12404=ORIENTED_EDGE ( 'NONE', *, *, #4968, .F. ) ;
#12405=CARTESIAN_POINT ( 'NONE',  ( 30.67540678000428045, -63.74634676501045050, 3.500000000000000000 ) ) ;
#12406=TOROIDAL_SURFACE ( 'NONE', #17783, 3.800000000000002931, 0.2999999999999999889 ) ;
#12409=EDGE_LOOP ( 'NONE', ( #7959, #18561, #15025, #20171 ) ) ;
#12410=CARTESIAN_POINT ( 'NONE',  ( 23.29441641503727567, -3.413540866333718338, 13.50000000000000000 ) ) ;
#12411=VERTEX_POINT ( 'NONE', #15024 ) ;
#12416=EDGE_CURVE ( 'NONE', #8409, #4651, #20073, .T. ) ;
#12417=DIRECTION ( 'NONE',  ( 0.000000000000000000, 0.000000000000000000, 1.000000000000000000 ) ) ;
#12418=CARTESIAN_POINT ( 'NONE',  ( 0.000000000000000000, -68.74634676501045760, 3.799999999999999822 ) ) ;
#12419=EDGE_CURVE ( 'NONE', #16692, #630, #18826, .T. ) ;
#12421=EDGE_CURVE ( 'NONE', #15670, #10812, #6980, .T. ) ;
#12423=DIRECTION ( 'NONE',  ( 0.000000000000000000, -1.000000000000000000, 0.000000000000000000 ) ) ;
#12424=CARTESIAN_POINT ( 'NONE',  ( -23.13130088652691541, 2.712279394122547593, 13.41537141447312109 ) ) ;
#12425=DIRECTION ( 'NONE',  ( -1.000000000000000000, 0.000000000000000000, 0.000000000000000000 ) ) ;
#12426=CARTESIAN_POINT ( 'NONE',  ( 23.04392555272741205, -2.268071869891188364, 13.22877247997975481 ) ) ;
#12428=CIRCLE ( 'NONE', #5273, 0.2999999999999999334 ) ;
#12429=CIRCLE ( 'NONE', #8549, 1.974596669241483804 ) ;
#12431=ORIENTED_EDGE ( 'NONE', *, *, #12984, .F. ) ;
#12434=CIRCLE ( 'NONE', #2810, 0.6999999999999992895 ) ;
#12436=B_SPLINE_CURVE_WITH_KNOTS ( 'NONE', 3,
 ( #14802, #6217, #17943, #21320, #7900, #2617, #11223, #6325 ),
 .UNSPECIFIED., .F., .F.,
 ( 4, 2, 2, 4 ),
 ( 0.000000000000000000, 0.0002393859945378754744, 0.0003590789918068118427, 0.0004787719890757481840 ),
 .UNSPECIFIED. ) ;
#12438=ORIENTED_EDGE ( 'NONE', *, *, #7063, .T. ) ;
#12442=ADVANCED_FACE ( 'NONE', ( #6548 ), #11648, .F. ) ;
#12443=CIRCLE ( 'NONE', #5709, 1.000000000000000888 ) ;
#12444=LINE ( 'NONE', #1932, #5950 ) ;
#12445=ORIENTED_EDGE ( 'NONE', *, *, #6674, .F. ) ;
#12446=CARTESIAN_POINT ( 'NONE',  ( -3.127054932750481964, 32.93424481021354921, 68.00000000000000000 ) ) ;
#12447=DIRECTION ( 'NONE',  ( 0.000000000000000000, 0.000000000000000000, 1.000000000000000000 ) ) ;
#12449=DIRECTION ( 'NONE',  ( 0.000000000000000000, 0.000000000000000000, 1.000000000000000000 ) ) ;
#12456=ORIENTED_EDGE ( 'NONE', *, *, #20977, .F. ) ;
#12457=VERTEX_POINT ( 'NONE', #18484 ) ;
#12458=DIRECTION ( 'NONE',  ( -0.000000000000000000, -0.000000000000000000, -1.000000000000000000 ) ) ;
#12460=VERTEX_POINT ( 'NONE', #11544 ) ;
#12462=VECTOR ( 'NONE', #4478, 1000.000000000000000 ) ;
#12465=CARTESIAN_POINT ( 'NONE',  ( -25.37540678000429395, -38.74634676501045760, 42.50000000000000000 ) ) ;
#12472=CARTESIAN_POINT ( 'NONE',  ( 31.50000000000002132, -72.00000000000001421, 3.200000000000000178 ) ) ;
#12474=CARTESIAN_POINT ( 'NONE',  ( 32.50000000000002132, 71.00000000000001421, 1.800000000000000044 ) ) ;
#12476=CYLINDRICAL_SURFACE ( 'NONE', #20525, 1.000000000000000888 ) ;
#12477=CARTESIAN_POINT ( 'NONE',  ( -23.14059574490498505, -2.755557770589328381, 13.42404417222473612 ) ) ;
#12479=DIRECTION ( 'NONE',  ( 0.000000000000000000, 0.000000000000000000, 1.000000000000000000 ) ) ;
#12481=EDGE_LOOP ( 'NONE', ( #9861, #19959, #15059, #19607 ) ) ;
#12483=VECTOR ( 'NONE', #6089, 1000.000000000000000 ) ;
#12484=FACE_OUTER_BOUND ( 'NONE', #12519, .T. ) ;
#12485=VECTOR ( 'NONE', #16144, 1000.000000000000000 ) ;
#12487=ORIENTED_EDGE ( 'NONE', *, *, #9557, .F. ) ;
#12488=VERTEX_POINT ( 'NONE', #9995 ) ;
#12490=ADVANCED_FACE ( 'NONE', ( #6876 ), #20284, .F. ) ;
#12492=ORIENTED_EDGE ( 'NONE', *, *, #15931, .F. ) ;
#12493=ORIENTED_EDGE ( 'NONE', *, *, #8146, .T. ) ;
#12494=ADVANCED_FACE ( 'NONE', ( #13563 ), #8655, .F. ) ;
#12496=ADVANCED_FACE ( 'NONE', ( #4960 ), #8416, .F. ) ;
#12497=AXIS2_PLACEMENT_3D ( 'NONE', #13619, #1421, #1637 ) ;
#12502=CARTESIAN_POINT ( 'NONE',  ( -3.627054932750481964, -32.93424481021354921, 68.00000000000000000 ) ) ;
#12504=CARTESIAN_POINT ( 'NONE',  ( -31.50000000000002132, -72.00000000000001421, 3.200000000000000178 ) ) ;
#12505=DIRECTION ( 'NONE',  ( 1.000000000000000000, 0.000000000000000000, 0.000000000000000000 ) ) ;
#12508=DIRECTION ( 'NONE',  ( 0.000000000000000000, 0.000000000000000000, 1.000000000000000000 ) ) ;
#12512=EDGE_CURVE ( 'NONE', #18203, #1535, #3526, .T. ) ;
#12513=AXIS2_PLACEMENT_3D ( 'NONE', #5306, #3384, #29 ) ;
#12514=EDGE_LOOP ( 'NONE', ( #14204, #11948, #7872, #3685 ) ) ;
#12517=CARTESIAN_POINT ( 'NONE',  ( -27.37540678000426908, 36.74634676501047181, 42.50000000000000000 ) ) ;
#12519=EDGE_LOOP ( 'NONE', ( #6214, #711, #21572, #8051 ) ) ;
#12520=EDGE_LOOP ( 'NONE', ( #18050, #5620, #10099, #14894 ) ) ;
#12521=CARTESIAN_POINT ( 'NONE',  ( 23.04897344237150492, -2.295898177910679738, 13.26544997878583487 ) ) ;
#12523=CARTESIAN_POINT ( 'NONE',  ( -27.37540678000426908, 36.74634676501047181, 13.79999999999999893 ) ) ;
#12524=ADVANCED_FACE ( 'NONE', ( #7611 ), #6756, .F. ) ;
#12526=LINE ( 'NONE', #14090, #13773 ) ;
#12527=DIRECTION ( 'NONE',  ( 0.000000000000000000, 1.000000000000000000, -0.000000000000000000 ) ) ;
#12531=CARTESIAN_POINT ( 'NONE',  ( -3.627054932750481964, -33.43424481021354921, 42.50000000000000000 ) ) ;
#12534=CARTESIAN_POINT ( 'NONE',  ( -15.21174975910705207, -51.61873716947361856, 68.50000000000000000 ) ) ;
#12536=ORIENTED_EDGE ( 'NONE', *, *, #6878, .T. ) ;
#12537=EDGE_LOOP ( 'NONE', ( #8527, #3901, #17858, #9787 ) ) ;
#12541=EDGE_LOOP ( 'NONE', ( #8581, #15155, #8328, #5007, #13951, #10204, #2597, #8863, #3576, #11061, #10648, #17727, #5031, #1888, #11080, #8578, #5938, #14417, #11971, #6005 ) ) ;
#12543=VERTEX_POINT ( 'NONE', #4125 ) ;
#12544=ORIENTED_EDGE ( 'NONE', *, *, #10731, .F. ) ;
#12545=AXIS2_PLACEMENT_3D ( 'NONE', #17655, #12608, #19450 ) ;
#12547=AXIS2_PLACEMENT_3D ( 'NONE', #3386, #15240, #20410 ) ;
#12548=DIRECTION ( 'NONE',  ( 0.000000000000000000, 0.000000000000000000, 1.000000000000000000 ) ) ;
#12549=CIRCLE ( 'NONE', #16114, 0.5000000000000000000 ) ;
#12550=CARTESIAN_POINT ( 'NONE',  ( 26.63662752439704917, 3.061616997868386099E-16, 3.500000000000000000 ) ) ;
#12552=LINE ( 'NONE', #14351, #21815 ) ;
#12553=FACE_OUTER_BOUND ( 'NONE', #4925, .T. ) ;
#12555=CARTESIAN_POINT ( 'NONE',  ( 15.21174975910706095, 52.00603550409435627, 13.50000000000000000 ) ) ;
#12556=CARTESIAN_POINT ( 'NONE',  ( -15.21174975910705207, 52.39333383871510108, 13.50000000000000000 ) ) ;
#12557=CARTESIAN_POINT ( 'NONE',  ( -25.37540678000427263, 67.24634676501045760, 13.50000000000000000 ) ) ;
#12558=ORIENTED_EDGE ( 'NONE', *, *, #10481, .F. ) ;
#12561=DIRECTION ( 'NONE',  ( 0.000000000000000000, 0.000000000000000000, -1.000000000000000000 ) ) ;
#12563=EDGE_LOOP ( 'NONE', ( #20321, #6539, #6107, #14722 ) ) ;
#12564=ORIENTED_EDGE ( 'NONE', *, *, #16978, .T. ) ;
#12567=TOROIDAL_SURFACE ( 'NONE', #13287, 2.299999999999993161, 0.2999999999999999889 ) ;
#12569=ADVANCED_FACE ( 'NONE', ( #19565 ), #2560, .F. ) ;
#12573=DIRECTION ( 'NONE',  ( 0.000000000000000000, -0.000000000000000000, 1.000000000000000000 ) ) ;
#12574=ORIENTED_EDGE ( 'NONE', *, *, #21659, .T. ) ;
#12575=CARTESIAN_POINT ( 'NONE',  ( 29.13662752439705272, 0.000000000000000000, 13.19999999999999929 ) ) ;
#12576=DIRECTION ( 'NONE',  ( 0.000000000000000000, -0.000000000000000000, -1.000000000000000000 ) ) ;
#12579=CARTESIAN_POINT ( 'NONE',  ( 3.127054932750481964, -33.43424481021354921, 68.00000000000000000 ) ) ;
#12583=ORIENTED_EDGE ( 'NONE', *, *, #19638, .F. ) ;
#12584=CARTESIAN_POINT ( 'NONE',  ( 30.37540678000427619, 63.74634676501045050, 7.500000000000000000 ) ) ;
#12585=CARTESIAN_POINT ( 'NONE',  ( -27.37540678000427619, 5.683640910026986681, 13.79999999999999893 ) ) ;
#12589=EDGE_CURVE ( 'NONE', #10528, #1711, #18222, .T. ) ;
#12591=EDGE_LOOP ( 'NONE', ( #7752, #12064, #9111, #4720 ) ) ;
#12592=CARTESIAN_POINT ( 'NONE',  ( 25.37540678000426908, 39.04634676501046187, 13.79999999999999893 ) ) ;
#12593=CARTESIAN_POINT ( 'NONE',  ( -23.02398829872513986, -3.528912754968629439, 13.79999999999999893 ) ) ;
#12595=ORIENTED_EDGE ( 'NONE', *, *, #11006, .T. ) ;
#12597=ADVANCED_FACE ( 'NONE', ( #8268 ), #18550, .T. ) ;
#12601=ORIENTED_EDGE ( 'NONE', *, *, #7856, .T. ) ;
#12602=DIRECTION ( 'NONE',  ( 0.000000000000000000, 0.000000000000000000, 1.000000000000000000 ) ) ;
#12605=LINE ( 'NONE', #21251, #20111 ) ;
#12606=DIRECTION ( 'NONE',  ( 0.000000000000000000, 0.000000000000000000, -1.000000000000000000 ) ) ;
#12608=DIRECTION ( 'NONE',  ( -0.000000000000000000, 1.000000000000000000, 0.000000000000000000 ) ) ;
#12611=ORIENTED_EDGE ( 'NONE', *, *, #247, .T. ) ;
#12612=DIRECTION ( 'NONE',  ( 0.000000000000000000, -1.000000000000000000, 0.000000000000000000 ) ) ;
#12613=CARTESIAN_POINT ( 'NONE',  ( -14.96174975910705207, 51.61873716947361856, 68.00000000000000000 ) ) ;
#12616=EDGE_CURVE ( 'NONE', #21319, #15844, #3160, .T. ) ;
#12624=ORIENTED_EDGE ( 'NONE', *, *, #1442, .T. ) ;
#12628=LINE ( 'NONE', #14208, #1440 ) ;
#12629=DIRECTION ( 'NONE',  ( 0.000000000000000000, 0.000000000000000000, -1.000000000000000000 ) ) ;
#12631=AXIS2_PLACEMENT_3D ( 'NONE', #7479, #14277, #21011 ) ;
#12633=CARTESIAN_POINT ( 'NONE',  ( -9.141460742840918030, 33.43424481021354921, 7.321391277662001151 ) ) ;
#12634=DIRECTION ( 'NONE',  ( 1.000000000000000000, 0.000000000000000000, 0.000000000000000000 ) ) ;
#12636=LINE ( 'NONE', #9464, #14308 ) ;
#12638=ADVANCED_FACE ( 'NONE', ( #3002 ), #20231, .F. ) ;
#12639=CARTESIAN_POINT ( 'NONE',  ( 23.02398829872513986, 7.027230193580998154E-15, 7.500000000000000000 ) ) ;
#12643=DIRECTION ( 'NONE',  ( 1.000000000000000000, 0.000000000000000000, 0.000000000000000000 ) ) ;
#12644=EDGE_CURVE ( 'NONE', #1806, #3604, #12429, .T. ) ;
#12645=ORIENTED_EDGE ( 'NONE', *, *, #12758, .F. ) ;
#12646=ORIENTED_EDGE ( 'NONE', *, *, #20339, .T. ) ;
#12647=AXIS2_PLACEMENT_3D ( 'NONE', #7865, #684, #14661 ) ;
#12650=ORIENTED_EDGE ( 'NONE', *, *, #15662, .F. ) ;
#12651=DIRECTION ( 'NONE',  ( -1.000000000000000000, -2.891205793294662451E-15, 0.000000000000000000 ) ) ;
#12652=EDGE_CURVE ( 'NONE', #4334, #18447, #6419, .T. ) ;
#12653=CARTESIAN_POINT ( 'NONE',  ( 17.95292532278785913, -50.11873716947361856, 68.00000000000000000 ) ) ;
#12654=CARTESIAN_POINT ( 'NONE',  ( 14.96512931750545938, 51.87344388792876515, 13.83591901640606459 ) ) ;
#12656=CARTESIAN_POINT ( 'NONE',  ( -17.93704824106378837, 50.11873716947361856, 13.87500000000000000 ) ) ;
#12659=DIRECTION ( 'NONE',  ( -0.000000000000000000, 1.000000000000000000, -0.000000000000000000 ) ) ;
#12662=CIRCLE ( 'NONE', #16967, 0.2999999999999999334 ) ;
#12663=ORIENTED_EDGE ( 'NONE', *, *, #19576, .F. ) ;
#12665=ORIENTED_EDGE ( 'NONE', *, *, #9851, .F. ) ;
#12666=DIRECTION ( 'NONE',  ( -3.052134192567367925E-16, 1.000000000000000000, 0.000000000000000000 ) ) ;
#12667=EDGE_CURVE ( 'NONE', #2503, #18174, #11268, .T. ) ;
#12668=LINE ( 'NONE', #21438, #14180 ) ;
#12669=CARTESIAN_POINT ( 'NONE',  ( 29.37540678000427619, -5.299999999999999822, 7.500000000000000000 ) ) ;
#12670=VERTEX_POINT ( 'NONE', #14747 ) ;
#12671=CYLINDRICAL_SURFACE ( 'NONE', #20402, 0.5000000000000004441 ) ;
#12675=CARTESIAN_POINT ( 'NONE',  ( -27.37540678000427619, 10.94079601157914539, 13.79999999999999893 ) ) ;
#12676=AXIS2_PLACEMENT_3D ( 'NONE', #11575, #22133, #13370 ) ;
#12677=DIRECTION ( 'NONE',  ( 0.000000000000000000, -1.000000000000000000, 0.000000000000000000 ) ) ;
#12679=CIRCLE ( 'NONE', #6657, 0.5000000000000004441 ) ;
#12681=DIRECTION ( 'NONE',  ( 1.000000000000000000, 0.000000000000000000, 0.000000000000000000 ) ) ;
#12682=EDGE_CURVE ( 'NONE', #10568, #17690, #9619, .T. ) ;
#12684=DIRECTION ( 'NONE',  ( 1.000000000000000000, 0.000000000000000000, 0.000000000000000000 ) ) ;
#12686=EDGE_CURVE ( 'NONE', #497, #16854, #19911, .T. ) ;
#12692=CIRCLE ( 'NONE', #20234, 1.999999999999991340 ) ;
#12695=CARTESIAN_POINT ( 'NONE',  ( -14.98285978764165449, 51.83353206222920306, 13.49999999999971756 ) ) ;
#12697=CARTESIAN_POINT ( 'NONE',  ( 14.96174975910705918, 32.10873716947361345, 13.79999999999999893 ) ) ;
#12701=ORIENTED_EDGE ( 'NONE', *, *, #14050, .F. ) ;
#12703=EDGE_CURVE ( 'NONE', #17559, #19232, #12443, .T. ) ;
#12706=CIRCLE ( 'NONE', #22034, 0.6999999999999992895 ) ;
#12707=TOROIDAL_SURFACE ( 'NONE', #20622, 1.300000000000000044, 0.2999999999999999889 ) ;
#12708=CARTESIAN_POINT ( 'NONE',  ( 15.95292532278785913, -51.61873716947361856, 68.00000000000000000 ) ) ;
#12709=TOROIDAL_SURFACE ( 'NONE', #3089, 0.2500000000000000000, 0.2500000000000000000 ) ;
#12713=LINE ( 'NONE', #11060, #5977 ) ;
#12721=ORIENTED_EDGE ( 'NONE', *, *, #3746, .F. ) ;
#12724=AXIS2_PLACEMENT_3D ( 'NONE', #10895, #9110, #21740 ) ;
#12726=ORIENTED_EDGE ( 'NONE', *, *, #1669, .F. ) ;
#12730=EDGE_LOOP ( 'NONE', ( #19776, #963, #16538, #1524 ) ) ;
#12732=VECTOR ( 'NONE', #821, 1000.000000000000000 ) ;
#12733=DIRECTION ( 'NONE',  ( 2.832483164223434527E-16, -1.000000000000000000, -0.000000000000000000 ) ) ;
#12734=VERTEX_POINT ( 'NONE', #3675 ) ;
#12736=B_SPLINE_CURVE_WITH_KNOTS ( 'NONE', 3,
 ( #21576, #16064, #9708, #2758, #21238, #11146, #16511, #2430, #9595, #12593 ),
 .UNSPECIFIED., .F., .F.,
 ( 4, 2, 2, 2, 4 ),
 ( 0.000000000000000000, 0.0001998921237118768868, 0.0003997842474237537735, 0.0007995684948475064628, 0.001599136989695014444 ),
 .UNSPECIFIED. ) ;
#12737=EDGE_CURVE ( 'NONE', #630, #4678, #10494, .T. ) ;
#12741=AXIS2_PLACEMENT_3D ( 'NONE', #13330, #20168, #3169 ) ;
#12742=ADVANCED_FACE ( 'NONE', ( #8490 ), #298, .F. ) ;
#12743=CIRCLE ( 'NONE', #3125, 3.500000000000003109 ) ;
#12747=CARTESIAN_POINT ( 'NONE',  ( 29.20000000000002061, 50.00000000000000000, 0.000000000000000000 ) ) ;
#12749=DIRECTION ( 'NONE',  ( 0.000000000000000000, 0.000000000000000000, 1.000000000000000000 ) ) ;
#12751=B_SPLINE_CURVE_WITH_KNOTS ( 'NONE', 3,
 ( #3293, #8558, #20419, #15367, #19982, #16584, #8331, #6446 ),
 .UNSPECIFIED., .F., .F.,
 ( 4, 2, 2, 4 ),
 ( -3.464559252384133923E-06, 0.0002895415592466213275, 0.0004360446184961240686, 0.0005825476777456268639 ),
 .UNSPECIFIED. ) ;
#12754=ORIENTED_EDGE ( 'NONE', *, *, #18214, .F. ) ;
#12755=VERTEX_POINT ( 'NONE', #18895 ) ;
#12758=EDGE_CURVE ( 'NONE', #1150, #5485, #4615, .T. ) ;
#12759=ORIENTED_EDGE ( 'NONE', *, *, #3524, .T. ) ;
#12761=CIRCLE ( 'NONE', #17427, 2.800000000000003819 ) ;
#12764=ORIENTED_EDGE ( 'NONE', *, *, #6167, .F. ) ;
#12765=AXIS2_PLACEMENT_3D ( 'NONE', #6515, #16993, #20593 ) ;
#12769=CARTESIAN_POINT ( 'NONE',  ( -15.21174975910705207, -52.39333383871510108, 13.50000000000000000 ) ) ;
#12771=CARTESIAN_POINT ( 'NONE',  ( 23.02398829872513986, 5.683640910026983128, 13.79999999999999893 ) ) ;
#12773=CARTESIAN_POINT ( 'NONE',  ( 17.92752199202933738, -38.74634676501045760, 13.62426406871192874 ) ) ;
#12775=DIRECTION ( 'NONE',  ( -1.000000000000000000, 0.000000000000000000, 0.000000000000000000 ) ) ;
#12776=CARTESIAN_POINT ( 'NONE',  ( 14.66918479711007706, 51.92478806352735887, 13.50000000000000000 ) ) ;
#12777=CARTESIAN_POINT ( 'NONE',  ( -26.37540678000427619, -10.94079601157914716, 13.79999999999999893 ) ) ;
#12778=AXIS2_PLACEMENT_3D ( 'NONE', #16154, #17844, #5464 ) ;
#12779=AXIS2_PLACEMENT_3D ( 'NONE', #14402, #10945, #7505 ) ;
#12785=CYLINDRICAL_SURFACE ( 'NONE', #17761, 0.5000000000000000000 ) ;
#12786=ORIENTED_EDGE ( 'NONE', *, *, #5145, .T. ) ;
#12787=VERTEX_POINT ( 'NONE', #13624 ) ;
#12792=ADVANCED_FACE ( 'NONE', ( #182 ), #11825, .F. ) ;
#12793=VERTEX_POINT ( 'NONE', #3338 ) ;
#12795=ORIENTED_EDGE ( 'NONE', *, *, #7736, .F. ) ;
#12804=DIRECTION ( 'NONE',  ( 1.000000000000000000, 0.000000000000000000, 0.000000000000000000 ) ) ;
#12805=AXIS2_PLACEMENT_3D ( 'NONE', #22162, #6838, #13953 ) ;
#12806=EDGE_CURVE ( 'NONE', #16971, #17841, #18915, .T. ) ;
#12808=CARTESIAN_POINT ( 'NONE',  ( 17.92752199202934094, -38.74634676501045760, 13.79999999999999893 ) ) ;
#12809=CARTESIAN_POINT ( 'NONE',  ( -23.07454441928563682, -2.431172533959871096, 13.33570496075367728 ) ) ;
#12811=LINE ( 'NONE', #4330, #7519 ) ;
#12812=EDGE_LOOP ( 'NONE', ( #17592, #11941, #16555, #4626 ) ) ;
#12814=DIRECTION ( 'NONE',  ( 0.000000000000000000, 0.000000000000000000, -1.000000000000000000 ) ) ;
#12816=ORIENTED_EDGE ( 'NONE', *, *, #4061, .F. ) ;
#12817=CARTESIAN_POINT ( 'NONE',  ( -9.141460742840918030, 32.11873716947361856, 68.00000000000000000 ) ) ;
#12821=AXIS2_PLACEMENT_3D ( 'NONE', #17658, #15651, #2333 ) ;
#12828=CARTESIAN_POINT ( 'NONE',  ( -25.37540678000427263, 63.74634676501045050, 13.50000000000000000 ) ) ;
#12830=DIRECTION ( 'NONE',  ( 0.000000000000000000, -1.000000000000000000, 0.000000000000000000 ) ) ;
#12834=DIRECTION ( 'NONE',  ( -0.000000000000000000, -1.000000000000000000, -0.000000000000000000 ) ) ;
#12836=ORIENTED_EDGE ( 'NONE', *, *, #1768, .F. ) ;
#12837=DIRECTION ( 'NONE',  ( 0.000000000000000000, 0.000000000000000000, 1.000000000000000000 ) ) ;
#12841=LINE ( 'NONE', #6273, #21730 ) ;
#12843=ORIENTED_EDGE ( 'NONE', *, *, #14455, .T. ) ;
#12844=DIRECTION ( 'NONE',  ( -0.000000000000000000, -0.000000000000000000, 1.000000000000000000 ) ) ;
#12848=ORIENTED_EDGE ( 'NONE', *, *, #6935, .F. ) ;
#12853=VERTEX_POINT ( 'NONE', #7480 ) ;
#12854=DIRECTION ( 'NONE',  ( -1.000000000000000000, -0.000000000000000000, -0.000000000000000000 ) ) ;
#12860=CIRCLE ( 'NONE', #7531, 2.500000000000002220 ) ;
#12863=CARTESIAN_POINT ( 'NONE',  ( 3.127054932750481964, -32.11873716947361856, 109.6002446535588319 ) ) ;
#12866=DIRECTION ( 'NONE',  ( 1.000000000000000000, 0.000000000000000000, 0.000000000000000000 ) ) ;
#12867=VERTEX_POINT ( 'NONE', #17740 ) ;
#12868=LINE ( 'NONE', #12639, #221 ) ;
#12871=ORIENTED_EDGE ( 'NONE', *, *, #14245, .F. ) ;
#12873=EDGE_CURVE ( 'NONE', #12977, #15569, #7488, .T. ) ;
#12875=EDGE_CURVE ( 'NONE', #18789, #10528, #21409, .T. ) ;
#12877=VERTEX_POINT ( 'NONE', #21341 ) ;
#12879=VECTOR ( 'NONE', #11256, 1000.000000000000000 ) ;
#12880=DIRECTION ( 'NONE',  ( -1.000000000000000000, 0.000000000000000000, 0.000000000000000000 ) ) ;
#12881=CARTESIAN_POINT ( 'NONE',  ( -27.37540678000427974, -5.683640910026986681, 42.50000000000000000 ) ) ;
#12883=DIRECTION ( 'NONE',  ( 0.000000000000000000, 1.000000000000000000, -0.000000000000000000 ) ) ;
#12884=EDGE_CURVE ( 'NONE', #17036, #1458, #16054, .T. ) ;
#12886=CARTESIAN_POINT ( 'NONE',  ( 23.32398829872514057, 7.118794219358020148E-15, 13.79999999999999893 ) ) ;
#12887=CIRCLE ( 'NONE', #1839, 0.2999999999999999334 ) ;
#12889=DIRECTION ( 'NONE',  ( -0.000000000000000000, -0.000000000000000000, -1.000000000000000000 ) ) ;
#12890=CARTESIAN_POINT ( 'NONE',  ( -17.95292532278785913, 0.000000000000000000, 109.6002446535588319 ) ) ;
#12895=EDGE_LOOP ( 'NONE', ( #19410, #15538, #1503, #16570, #12335, #18119 ) ) ;
#12898=DIRECTION ( 'NONE',  ( 0.000000000000000000, -1.000000000000000000, 0.000000000000000000 ) ) ;
#12900=EDGE_CURVE ( 'NONE', #10497, #18203, #7256, .T. ) ;
#12903=EDGE_CURVE ( 'NONE', #18309, #16692, #670, .T. ) ;
#12911=DIRECTION ( 'NONE',  ( -1.000000000000000000, 0.000000000000000000, 0.000000000000000000 ) ) ;
#12912=FACE_OUTER_BOUND ( 'NONE', #13122, .T. ) ;
#12913=CARTESIAN_POINT ( 'NONE',  ( -3.127054932750481964, -32.61873716947361856, 109.6002446535588319 ) ) ;
#12914=DIRECTION ( 'NONE',  ( 0.000000000000000000, -1.000000000000000000, 0.000000000000000000 ) ) ;
#12919=CARTESIAN_POINT ( 'NONE',  ( 3.627054932750481964, -32.93424481021354921, 68.00000000000000000 ) ) ;
#12920=CYLINDRICAL_SURFACE ( 'NONE', #6867, 0.2999999999999999334 ) ;
#12921=ORIENTED_EDGE ( 'NONE', *, *, #17329, .T. ) ;
#12922=DIRECTION ( 'NONE',  ( 1.000000000000000000, -3.052134192567374827E-16, 0.000000000000000000 ) ) ;
#12924=AXIS2_PLACEMENT_3D ( 'NONE', #5855, #12301, #19154 ) ;
#12927=VECTOR ( 'NONE', #16752, 1000.000000000000000 ) ;
#12931=CYLINDRICAL_SURFACE ( 'NONE', #20270, 0.2999999999999999889 ) ;
#12932=CARTESIAN_POINT ( 'NONE',  ( 25.37540678000427263, -63.74634676501045050, 3.799999999999999822 ) ) ;
#12933=EDGE_CURVE ( 'NONE', #15453, #18705, #19826, .T. ) ;
#12936=ORIENTED_EDGE ( 'NONE', *, *, #5532, .T. ) ;
#12937=DIRECTION ( 'NONE',  ( -0.000000000000000000, -0.000000000000000000, -1.000000000000000000 ) ) ;
#12938=DIRECTION ( 'NONE',  ( 0.000000000000000000, 0.000000000000000000, 1.000000000000000000 ) ) ;
#12939=CARTESIAN_POINT ( 'NONE',  ( -23.02398829872514341, -2.245853328535781124, 13.29652846991536030 ) ) ;
#12940=AXIS2_PLACEMENT_3D ( 'NONE', #13796, #10365, #10028 ) ;
#12941=CARTESIAN_POINT ( 'NONE',  ( 0.000000000000000000, 71.70000000000001705, 1.500000000000000000 ) ) ;
#12942=CARTESIAN_POINT ( 'NONE',  ( -27.37540678000427619, 5.683640910026986681, 42.50000000000000000 ) ) ;
#12943=CARTESIAN_POINT ( 'NONE',  ( 30.07540678000427548, 0.000000000000000000, 7.500000000000000000 ) ) ;
#12945=DIRECTION ( 'NONE',  ( 0.000000000000000000, -0.000000000000000000, -1.000000000000000000 ) ) ;
#12952=ORIENTED_EDGE ( 'NONE', *, *, #4293, .T. ) ;
#12953=DIRECTION ( 'NONE',  ( -0.000000000000000000, -0.000000000000000000, -1.000000000000000000 ) ) ;
#12963=VERTEX_POINT ( 'NONE', #14158 ) ;
#12965=FACE_OUTER_BOUND ( 'NONE', #20758, .T. ) ;
#12966=DIRECTION ( 'NONE',  ( 0.000000000000000000, 0.000000000000000000, 1.000000000000000000 ) ) ;
#12967=CARTESIAN_POINT ( 'NONE',  ( -3.627054932750481964, -32.93424481021354921, 13.50000000000000000 ) ) ;
#12969=EDGE_CURVE ( 'NONE', #12793, #16058, #15799, .T. ) ;
#12972=EDGE_CURVE ( 'NONE', #1711, #2078, #11102, .T. ) ;
#12973=DIRECTION ( 'NONE',  ( 0.000000000000000000, -1.000000000000000000, -0.000000000000000000 ) ) ;
#12974=ORIENTED_EDGE ( 'NONE', *, *, #640, .F. ) ;
#12976=DIRECTION ( 'NONE',  ( 1.000000000000000000, 0.000000000000000000, 0.000000000000000000 ) ) ;
#12977=VERTEX_POINT ( 'NONE', #9586 ) ;
#12981=VERTEX_POINT ( 'NONE', #16265 ) ;
#12982=CARTESIAN_POINT ( 'NONE',  ( 27.37540678000427619, 5.683640910026986681, 13.79999999999999893 ) ) ;
#12984=EDGE_CURVE ( 'NONE', #3099, #18098, #14716, .T. ) ;
#12985=ORIENTED_EDGE ( 'NONE', *, *, #504, .F. ) ;
#12986=CARTESIAN_POINT ( 'NONE',  ( 25.37540678000427263, -63.74634676501045050, 13.19999999999999929 ) ) ;
#12989=TOROIDAL_SURFACE ( 'NONE', #20533, 4.700000000000004619, 0.2999999999999999889 ) ;
#12994=DIRECTION ( 'NONE',  ( 0.000000000000000000, 0.000000000000000000, 1.000000000000000000 ) ) ;
#12995=DIRECTION ( 'NONE',  ( 0.000000000000000000, 0.000000000000000000, 1.000000000000000000 ) ) ;
#12996=VERTEX_POINT ( 'NONE', #21789 ) ;
#12997=DIRECTION ( 'NONE',  ( 1.000000000000000000, 0.000000000000000000, 0.000000000000000000 ) ) ;
#12998=DIRECTION ( 'NONE',  ( 0.000000000000000000, -1.000000000000000000, 0.000000000000000000 ) ) ;
#13001=ORIENTED_EDGE ( 'NONE', *, *, #12229, .T. ) ;
#13003=EDGE_LOOP ( 'NONE', ( #2840, #14807, #17898, #8750 ) ) ;
#13004=DIRECTION ( 'NONE',  ( -0.000000000000000000, -0.000000000000000000, -1.000000000000000000 ) ) ;
#13005=VECTOR ( 'NONE', #9195, 1000.000000000000000 ) ;
#13007=EDGE_LOOP ( 'NONE', ( #3804, #19858, #21913, #20850 ) ) ;
#13012=DIRECTION ( 'NONE',  ( -0.000000000000000000, 1.000000000000000000, 0.000000000000000000 ) ) ;
#13013=CARTESIAN_POINT ( 'NONE',  ( 29.37540678000427619, -6.000000000000000000, 7.500000000000000000 ) ) ;
#13022=CARTESIAN_POINT ( 'NONE',  ( -23.32398829872514057, 3.528912754968630328, 13.79999999999999893 ) ) ;
#13023=ORIENTED_EDGE ( 'NONE', *, *, #19626, .T. ) ;
#13026=LINE ( 'NONE', #1279, #2528 ) ;
#13028=DIRECTION ( 'NONE',  ( 0.000000000000000000, 0.000000000000000000, -1.000000000000000000 ) ) ;
#13031=ORIENTED_EDGE ( 'NONE', *, *, #6402, .T. ) ;
#13034=DIRECTION ( 'NONE',  ( 1.000000000000000000, 0.000000000000000000, 0.000000000000000000 ) ) ;
#13036=VERTEX_POINT ( 'NONE', #8239 ) ;
#13037=VECTOR ( 'NONE', #1196, 1000.000000000000000 ) ;
#13039=ORIENTED_EDGE ( 'NONE', *, *, #18160, .F. ) ;
#13041=AXIS2_PLACEMENT_3D ( 'NONE', #16406, #6243, #13028 ) ;
#13042=CIRCLE ( 'NONE', #22019, 0.2999999999999999334 ) ;
#13044=CARTESIAN_POINT ( 'NONE',  ( -28.57540678000427548, 0.000000000000000000, 13.19999999999999929 ) ) ;
#13049=ADVANCED_FACE ( 'NONE', ( #15051 ), #12920, .T. ) ;
#13050=EDGE_CURVE ( 'NONE', #4630, #20393, #12216, .T. ) ;
#13051=CARTESIAN_POINT ( 'NONE',  ( 0.000000000000000000, 5.000000000000000000, 3.799999999999999822 ) ) ;
#13052=DIRECTION ( 'NONE',  ( 0.000000000000000000, 0.000000000000000000, 1.000000000000000000 ) ) ;
#13055=VECTOR ( 'NONE', #14424, 1000.000000000000000 ) ;
#13058=DIRECTION ( 'NONE',  ( 1.000000000000000000, 0.000000000000000000, 0.000000000000000000 ) ) ;
#13059=VERTEX_POINT ( 'NONE', #4429 ) ;
#13060=VECTOR ( 'NONE', #12629, 1000.000000000000000 ) ;
#13066=ORIENTED_EDGE ( 'NONE', *, *, #925, .T. ) ;
#13069=ORIENTED_EDGE ( 'NONE', *, *, #10048, .T. ) ;
#13076=AXIS2_PLACEMENT_3D ( 'NONE', #12220, #15695, #2047 ) ;
#13077=DIRECTION ( 'NONE',  ( 0.000000000000000000, 0.000000000000000000, 1.000000000000000000 ) ) ;
#13079=DIRECTION ( 'NONE',  ( 0.000000000000000000, 0.000000000000000000, 1.000000000000000000 ) ) ;
#13080=DIRECTION ( 'NONE',  ( 0.000000000000000000, 1.000000000000000000, 0.000000000000000000 ) ) ;
#13090=ORIENTED_EDGE ( 'NONE', *, *, #21972, .T. ) ;
#13091=FACE_OUTER_BOUND ( 'NONE', #8646, .T. ) ;
#13092=FACE_OUTER_BOUND ( 'NONE', #895, .T. ) ;
#13094=AXIS2_PLACEMENT_3D ( 'NONE', #1243, #14680, #6312 ) ;
#13098=DIRECTION ( 'NONE',  ( 0.000000000000000000, 0.000000000000000000, 1.000000000000000000 ) ) ;
#13102=CIRCLE ( 'NONE', #1674, 5.000000000000004441 ) ;
#13104=EDGE_CURVE ( 'NONE', #20783, #2503, #16835, .T. ) ;
#13105=TOROIDAL_SURFACE ( 'NONE', #7066, 2.800000000000002043, 0.2999999999999999889 ) ;
#13109=CARTESIAN_POINT ( 'NONE',  ( 23.02398829872513986, 5.683640910026983128, 42.50000000000000000 ) ) ;
#13112=CARTESIAN_POINT ( 'NONE',  ( -15.95292532278785913, -51.61873716947361856, 68.00000000000000000 ) ) ;
#13114=ORIENTED_EDGE ( 'NONE', *, *, #19201, .F. ) ;
#13117=CARTESIAN_POINT ( 'NONE',  ( 25.37540678000427263, 63.74634676501045050, 13.50000000000000000 ) ) ;
#13118=CARTESIAN_POINT ( 'NONE',  ( -23.04273156199907291, 2.261510999192719584, 13.21476795433022033 ) ) ;
#13119=ORIENTED_EDGE ( 'NONE', *, *, #12099, .T. ) ;
#13120=CYLINDRICAL_SURFACE ( 'NONE', #2187, 0.5000000000000004441 ) ;
#13121=VECTOR ( 'NONE', #16624, 1000.000000000000000 ) ;
#13122=EDGE_LOOP ( 'NONE', ( #2315, #2116, #5172, #17929 ) ) ;
#13124=VECTOR ( 'NONE', #6390, 1000.000000000000000 ) ;
#13127=ORIENTED_EDGE ( 'NONE', *, *, #20069, .T. ) ;
#13128=DIRECTION ( 'NONE',  ( 1.000000000000000000, 0.000000000000000000, 0.000000000000000000 ) ) ;
#13135=VERTEX_POINT ( 'NONE', #12124 ) ;
#13137=EDGE_CURVE ( 'NONE', #18691, #4007, #10062, .T. ) ;
#13138=DIRECTION ( 'NONE',  ( 1.000000000000000000, 0.000000000000000000, 0.000000000000000000 ) ) ;
#13139=DIRECTION ( 'NONE',  ( -1.000000000000000000, 0.000000000000000000, 0.000000000000000000 ) ) ;
#13142=DIRECTION ( 'NONE',  ( 3.052134192567367925E-16, -1.000000000000000000, 0.000000000000000000 ) ) ;
#13143=ORIENTED_EDGE ( 'NONE', *, *, #13382, .F. ) ;
#13144=DIRECTION ( 'NONE',  ( 0.000000000000000000, 0.000000000000000000, 1.000000000000000000 ) ) ;
#13145=DIRECTION ( 'NONE',  ( 1.000000000000000000, 0.000000000000000000, 0.000000000000000000 ) ) ;
#13146=CIRCLE ( 'NONE', #21030, 0.5000000000000004441 ) ;
#13151=VECTOR ( 'NONE', #6299, 1000.000000000000000 ) ;
#13154=ORIENTED_EDGE ( 'NONE', *, *, #66, .T. ) ;
#13156=CARTESIAN_POINT ( 'NONE',  ( -26.56227312273159313, 9.958410664601840878, 42.50000000000000000 ) ) ;
#13159=VERTEX_POINT ( 'NONE', #7006 ) ;
#13160=ORIENTED_EDGE ( 'NONE', *, *, #4196, .T. ) ;
#13164=AXIS2_PLACEMENT_3D ( 'NONE', #20405, #16806, #1477 ) ;
#13166=EDGE_CURVE ( 'NONE', #13756, #7310, #18622, .T. ) ;
#13170=VECTOR ( 'NONE', #17596, 1000.000000000000000 ) ;
#13171=VECTOR ( 'NONE', #18588, 1000.000000000000000 ) ;
#13173=CYLINDRICAL_SURFACE ( 'NONE', #3863, 0.3000000000000016542 ) ;
#13174=CARTESIAN_POINT ( 'NONE',  ( -23.02398829872513986, -2.191402100636986816, 13.32997043993373332 ) ) ;
#13175=DIRECTION ( 'NONE',  ( 0.000000000000000000, 0.000000000000000000, -1.000000000000000000 ) ) ;
#13177=CARTESIAN_POINT ( 'NONE',  ( 0.000000000000000000, 5.000000000000000000, 7.500000000000000000 ) ) ;
#13182=VERTEX_POINT ( 'NONE', #1847 ) ;
#13185=EDGE_CURVE ( 'NONE', #12411, #11808, #3309, .T. ) ;
#13189=EDGE_LOOP ( 'NONE', ( #14185, #1017, #11788, #14081 ) ) ;
#13190=CARTESIAN_POINT ( 'NONE',  ( -3.127054932750481964, -32.61873716947361856, 68.50000000000000000 ) ) ;
#13191=ORIENTED_EDGE ( 'NONE', *, *, #16045, .T. ) ;
#13192=ORIENTED_EDGE ( 'NONE', *, *, #8509, .T. ) ;
#13193=CARTESIAN_POINT ( 'NONE',  ( 26.37540678000427619, -10.94079601157914716, 13.79999999999999893 ) ) ;
#13195=EDGE_CURVE ( 'NONE', #3729, #4334, #3201, .T. ) ;
#13196=ADVANCED_FACE ( 'NONE', ( #4990 ), #8982, .T. ) ;
#13197=VERTEX_POINT ( 'NONE', #17060 ) ;
#13198=EDGE_CURVE ( 'NONE', #19361, #18032, #13595, .T. ) ;
#13202=AXIS2_PLACEMENT_3D ( 'NONE', #3927, #19247, #17657 ) ;
#13203=DIRECTION ( 'NONE',  ( 1.000000000000000000, 0.000000000000000000, 0.000000000000000000 ) ) ;
#13206=CARTESIAN_POINT ( 'NONE',  ( -8.641460742840918030, -33.43424481021354921, 13.50000000000000000 ) ) ;
#13207=ADVANCED_FACE ( 'NONE', ( #3412 ), #1738, .F. ) ;
#13208=CARTESIAN_POINT ( 'NONE',  ( -3.127054932750481964, 32.61873716947361856, 68.00000000000000000 ) ) ;
#13209=CARTESIAN_POINT ( 'NONE',  ( -27.37540678000427974, -10.94079601157914716, 42.50000000000000000 ) ) ;
#13210=CARTESIAN_POINT ( 'NONE',  ( 29.09616827897941249, -6.500357068115323322, 7.499999999998635758 ) ) ;
#13211=DIRECTION ( 'NONE',  ( -0.000000000000000000, -0.000000000000000000, -1.000000000000000000 ) ) ;
#13212=ORIENTED_EDGE ( 'NONE', *, *, #17436, .T. ) ;
#13213=CARTESIAN_POINT ( 'NONE',  ( -0.000000000000000000, 69.00000000000000000, 1.500000000000000000 ) ) ;
#13215=AXIS2_PLACEMENT_3D ( 'NONE', #16021, #7652, #10681 ) ;
#13216=AXIS2_PLACEMENT_3D ( 'NONE', #18533, #8355, #22012 ) ;
#13218=ORIENTED_EDGE ( 'NONE', *, *, #6661, .F. ) ;
#13219=ORIENTED_EDGE ( 'NONE', *, *, #198, .T. ) ;
#13221=EDGE_LOOP ( 'NONE', ( #20307, #9528, #17338, #3237, #5166 ) ) ;
#13222=EDGE_CURVE ( 'NONE', #6030, #8329, #5919, .T. ) ;
#13224=ORIENTED_EDGE ( 'NONE', *, *, #16173, .F. ) ;
#13227=ORIENTED_EDGE ( 'NONE', *, *, #14701, .F. ) ;
#13228=CIRCLE ( 'NONE', #20040, 0.2999999999999999334 ) ;
#13229=CARTESIAN_POINT ( 'NONE',  ( 14.98586301832698808, -51.95135570414442583, 13.85537332152988554 ) ) ;
#13230=AXIS2_PLACEMENT_3D ( 'NONE', #5539, #21096, #12651 ) ;
#13231=DIRECTION ( 'NONE',  ( -0.000000000000000000, -0.000000000000000000, -1.000000000000000000 ) ) ;
#13234=FACE_OUTER_BOUND ( 'NONE', #9040, .T. ) ;
#13236=EDGE_CURVE ( 'NONE', #20218, #4038, #14740, .T. ) ;
#13238=VERTEX_POINT ( 'NONE', #17706 ) ;
#13239=VERTEX_POINT ( 'NONE', #9106 ) ;
#13241=CARTESIAN_POINT ( 'NONE',  ( -23.04273156199908357, 2.261510999192738680, 13.50000000000000000 ) ) ;
#13243=CARTESIAN_POINT ( 'NONE',  ( -29.13662752439705272, 0.000000000000000000, 3.799999999999999822 ) ) ;
#13244=ORIENTED_EDGE ( 'NONE', *, *, #21073, .T. ) ;
#13246=DIRECTION ( 'NONE',  ( 1.000000000000000000, 0.000000000000000000, 0.000000000000000000 ) ) ;
#13247=EDGE_CURVE ( 'NONE', #15670, #21768, #21902, .T. ) ;
#13250=CARTESIAN_POINT ( 'NONE',  ( -14.96174975910705207, 51.61873716947361856, 14.00000000000000000 ) ) ;
#13251=CARTESIAN_POINT ( 'NONE',  ( 23.02398829872513986, -2.157133568460768203, 13.26806292639400908 ) ) ;
#13252=CARTESIAN_POINT ( 'NONE',  ( 15.95292532278785913, 52.39333383871510108, 13.79999999999999716 ) ) ;
#13253=VERTEX_POINT ( 'NONE', #589 ) ;
#13254=DIRECTION ( 'NONE',  ( 0.000000000000000000, -0.000000000000000000, -1.000000000000000000 ) ) ;
#13255=CARTESIAN_POINT ( 'NONE',  ( 27.37540678000426908, 36.74634676501047181, 13.79999999999999893 ) ) ;
#13257=DIRECTION ( 'NONE',  ( 1.000000000000000000, 0.000000000000000000, 0.000000000000000000 ) ) ;
#13259=VERTEX_POINT ( 'NONE', #2386 ) ;
#13260=DIRECTION ( 'NONE',  ( 1.000000000000000000, 0.000000000000000000, 0.000000000000000000 ) ) ;
#13262=ORIENTED_EDGE ( 'NONE', *, *, #10143, .T. ) ;
#13263=DIRECTION ( 'NONE',  ( 1.000000000000000000, 0.000000000000000000, 0.000000000000000000 ) ) ;
#13265=CARTESIAN_POINT ( 'NONE',  ( -17.95292532278785913, 0.000000000000000000, 13.99999999999999822 ) ) ;
#13269=ORIENTED_EDGE ( 'NONE', *, *, #5423, .T. ) ;
#13273=DIRECTION ( 'NONE',  ( 1.000000000000000000, 0.000000000000000000, 0.000000000000000000 ) ) ;
#13276=VERTEX_POINT ( 'NONE', #704 ) ;
#13278=DIRECTION ( 'NONE',  ( 1.000000000000000000, -0.000000000000000000, -0.000000000000000000 ) ) ;
#13280=DIRECTION ( 'NONE',  ( 0.000000000000000000, 0.000000000000000000, 1.000000000000000000 ) ) ;
#13281=ADVANCED_FACE ( 'NONE', ( #5873 ), #19299, .F. ) ;
#13286=DIRECTION ( 'NONE',  ( -0.000000000000000000, -1.000000000000000000, 0.000000000000000000 ) ) ;
#13287=AXIS2_PLACEMENT_3D ( 'NONE', #19600, #2480, #9647 ) ;
#13297=DIRECTION ( 'NONE',  ( 0.000000000000000000, 0.000000000000000000, 1.000000000000000000 ) ) ;
#13301=CARTESIAN_POINT ( 'NONE',  ( 29.42156510615627596, -2.562837254968982403, 0.09431619747333748471 ) ) ;
#13305=CARTESIAN_POINT ( 'NONE',  ( 29.20000000000002061, 0.000000000000000000, 0.2999999999999947153 ) ) ;
#13307=DIRECTION ( 'NONE',  ( 1.000000000000000000, 0.000000000000000000, 0.000000000000000000 ) ) ;
#13308=AXIS2_PLACEMENT_3D ( 'NONE', #6649, #3174, #6769 ) ;
#13309=FACE_OUTER_BOUND ( 'NONE', #3882, .T. ) ;
#13310=CARTESIAN_POINT ( 'NONE',  ( 17.95292532278785913, 0.000000000000000000, 42.50000000000000711 ) ) ;
#13311=DIRECTION ( 'NONE',  ( -0.000000000000000000, 0.000000000000000000, 1.000000000000000000 ) ) ;
#13314=ADVANCED_FACE ( 'NONE', ( #2500 ), #1837, .T. ) ;
#13315=DIRECTION ( 'NONE',  ( -1.000000000000000000, -0.000000000000000000, 0.000000000000000000 ) ) ;
#13317=FACE_OUTER_BOUND ( 'NONE', #2009, .T. ) ;
#13319=PLANE ( 'NONE',  #17390 ) ;
#13321=LINE ( 'NONE', #4823, #15602 ) ;
#13322=CARTESIAN_POINT ( 'NONE',  ( -31.50000000000002132, -71.00000000000001421, 3.200000000000000178 ) ) ;
#13323=ORIENTED_EDGE ( 'NONE', *, *, #15798, .T. ) ;
#13325=FACE_OUTER_BOUND ( 'NONE', #7317, .T. ) ;
#13326=VERTEX_POINT ( 'NONE', #2716 ) ;
#13329=ORIENTED_EDGE ( 'NONE', *, *, #5750, .T. ) ;
#13330=CARTESIAN_POINT ( 'NONE',  ( 0.000000000000000000, -39.04634676501046187, 13.79999999999999893 ) ) ;
#13331=CARTESIAN_POINT ( 'NONE',  ( 0.000000000000000000, 32.11873716947361856, 109.6002446535588319 ) ) ;
#13332=ORIENTED_EDGE ( 'NONE', *, *, #13453, .F. ) ;
#13333=CARTESIAN_POINT ( 'NONE',  ( 29.37540678000427619, 6.000000000000000000, 7.200000000000000178 ) ) ;
#13336=EDGE_CURVE ( 'NONE', #16692, #10531, #10784, .T. ) ;
#13337=DIRECTION ( 'NONE',  ( 0.000000000000000000, 0.000000000000000000, 1.000000000000000000 ) ) ;
#13340=EDGE_CURVE ( 'NONE', #11153, #14847, #5788, .T. ) ;
#13341=LINE ( 'NONE', #16239, #17912 ) ;
#13344=ORIENTED_EDGE ( 'NONE', *, *, #9675, .T. ) ;
#13350=EDGE_CURVE ( 'NONE', #14858, #19370, #7991, .T. ) ;
#13352=ORIENTED_EDGE ( 'NONE', *, *, #15131, .T. ) ;
#13353=AXIS2_PLACEMENT_3D ( 'NONE', #5772, #9550, #9217 ) ;
#13354=PLANE ( 'NONE',  #1797 ) ;
#13358=DIRECTION ( 'NONE',  ( 0.000000000000000000, 1.000000000000000000, 0.000000000000000000 ) ) ;
#13361=FACE_OUTER_BOUND ( 'NONE', #18819, .T. ) ;
#13362=CARTESIAN_POINT ( 'NONE',  ( -26.56227312273159313, -9.958410664601842655, 42.50000000000000000 ) ) ;
#13363=FACE_OUTER_BOUND ( 'NONE', #598, .T. ) ;
#13366=VERTEX_POINT ( 'NONE', #21310 ) ;
#13368=EDGE_CURVE ( 'NONE', #6358, #5647, #7770, .T. ) ;
#13369=ORIENTED_EDGE ( 'NONE', *, *, #493, .T. ) ;
#13370=DIRECTION ( 'NONE',  ( 1.000000000000000000, 0.000000000000000000, 0.000000000000000000 ) ) ;
#13374=ORIENTED_EDGE ( 'NONE', *, *, #6338, .F. ) ;
#13375=CARTESIAN_POINT ( 'NONE',  ( -15.06704456860866870, 51.94509779313090547, 13.50000000000000000 ) ) ;
#13376=CARTESIAN_POINT ( 'NONE',  ( 17.95292532278785913, -50.11873716947361856, 109.6002446535588319 ) ) ;
#13378=FACE_OUTER_BOUND ( 'NONE', #3060, .T. ) ;
#13379=ORIENTED_EDGE ( 'NONE', *, *, #7049, .T. ) ;
#13381=DIRECTION ( 'NONE',  ( 1.000000000000000000, 0.000000000000000000, 0.000000000000000000 ) ) ;
#13382=EDGE_CURVE ( 'NONE', #18442, #1357, #19716, .T. ) ;
#13384=LINE ( 'NONE', #10051, #4580 ) ;
#13385=ADVANCED_FACE ( 'NONE', ( #11215 ), #14794, .T. ) ;
#13388=AXIS2_PLACEMENT_3D ( 'NONE', #15209, #8075, #19945 ) ;
#13390=AXIS2_PLACEMENT_3D ( 'NONE', #20846, #11985, #20516 ) ;
#13391=CARTESIAN_POINT ( 'NONE',  ( 14.96174975910705918, -51.61873716947361856, 14.00000000000000000 ) ) ;
#13393=LINE ( 'NONE', #10057, #5335 ) ;
#13396=DIRECTION ( 'NONE',  ( -1.000000000000000000, 0.000000000000000000, 0.000000000000000000 ) ) ;
#13397=ORIENTED_EDGE ( 'NONE', *, *, #2585, .F. ) ;
#13400=ORIENTED_EDGE ( 'NONE', *, *, #16946, .F. ) ;
#13401=LINE ( 'NONE', #18779, #11734 ) ;
#13403=VERTEX_POINT ( 'NONE', #6317 ) ;
#13405=AXIS2_PLACEMENT_3D ( 'NONE', #17506, #4077, #2173 ) ;
#13406=ORIENTED_EDGE ( 'NONE', *, *, #11637, .T. ) ;
#13407=AXIS2_PLACEMENT_3D ( 'NONE', #16164, #4104, #7810 ) ;
#13408=DIRECTION ( 'NONE',  ( 0.000000000000000000, 0.000000000000000000, 1.000000000000000000 ) ) ;
#13409=ORIENTED_EDGE ( 'NONE', *, *, #20786, .F. ) ;
#13412=ORIENTED_EDGE ( 'NONE', *, *, #5145, .F. ) ;
#13413=CARTESIAN_POINT ( 'NONE',  ( -15.95292532278785913, -34.11873716947361856, 42.50000000000000711 ) ) ;
#13417=CARTESIAN_POINT ( 'NONE',  ( -9.641460742840918030, -33.43424481021354921, 68.50000000000000000 ) ) ;
#13422=CARTESIAN_POINT ( 'NONE',  ( -15.16859876043988464, -52.00603549157913363, 13.50000000000000000 ) ) ;
#13423=CARTESIAN_POINT ( 'NONE',  ( 0.000000000000000000, -4.700000000000000178, 3.799999999999999822 ) ) ;
#13428=ORIENTED_EDGE ( 'NONE', *, *, #1147, .F. ) ;
#13429=CIRCLE ( 'NONE', #9508, 0.2999999999999999334 ) ;
#13432=ORIENTED_EDGE ( 'NONE', *, *, #20197, .F. ) ;
#13436=EDGE_CURVE ( 'NONE', #17256, #20393, #17572, .T. ) ;
#13446=ORIENTED_EDGE ( 'NONE', *, *, #19707, .F. ) ;
#13447=DIRECTION ( 'NONE',  ( 0.000000000000000000, 0.000000000000000000, 1.000000000000000000 ) ) ;
#13451=DIRECTION ( 'NONE',  ( 1.000000000000000000, 0.000000000000000000, -0.000000000000000000 ) ) ;
#13452=CIRCLE ( 'NONE', #939, 0.5000000000000004441 ) ;
#13453=EDGE_CURVE ( 'NONE', #18309, #6576, #11842, .T. ) ;
#13457=ORIENTED_EDGE ( 'NONE', *, *, #1983, .F. ) ;
#13459=CARTESIAN_POINT ( 'NONE',  ( -15.21174975910705207, -41.81054587065082728, 68.50000000000000000 ) ) ;
#13460=ORIENTED_EDGE ( 'NONE', *, *, #20087, .F. ) ;
#13462=AXIS2_PLACEMENT_3D ( 'NONE', #11675, #18180, #14707 ) ;
#13463=AXIS2_PLACEMENT_3D ( 'NONE', #11410, #21837, #20144 ) ;
#13466=CIRCLE ( 'NONE', #11671, 0.5000000000000004441 ) ;
#13467=ADVANCED_FACE ( 'NONE', ( #1705 ), #4843, .T. ) ;
#13468=ORIENTED_EDGE ( 'NONE', *, *, #10981, .T. ) ;
#13469=CARTESIAN_POINT ( 'NONE',  ( -15.21174975910705207, 41.81054587065082728, 68.50000000000000000 ) ) ;
#13471=ADVANCED_FACE ( 'NONE', ( #18830 ), #16810, .F. ) ;
#13472=CARTESIAN_POINT ( 'NONE',  ( -15.21174975910705207, 32.10873716947361345, 68.25000000000000000 ) ) ;
#13477=CARTESIAN_POINT ( 'NONE',  ( 14.66174975910705847, 0.000000000000000000, 13.79999999999999893 ) ) ;
#13481=CIRCLE ( 'NONE', #12396, 5.299999999999998934 ) ;
#13482=VECTOR ( 'NONE', #18781, 1000.000000000000000 ) ;
#13483=DIRECTION ( 'NONE',  ( 1.000000000000000000, 0.000000000000000000, 0.000000000000000000 ) ) ;
#13484=ADVANCED_FACE ( 'NONE', ( #11654 ), #20175, .F. ) ;
#13486=FACE_OUTER_BOUND ( 'NONE', #6870, .T. ) ;
#13488=CARTESIAN_POINT ( 'NONE',  ( 28.57540678000427548, 0.000000000000000000, 13.19999999999999929 ) ) ;
#13489=EDGE_LOOP ( 'NONE', ( #7484, #9665, #10136, #7515 ) ) ;
#13492=DIRECTION ( 'NONE',  ( 0.000000000000000000, 0.000000000000000000, 1.000000000000000000 ) ) ;
#13495=ORIENTED_EDGE ( 'NONE', *, *, #15199, .T. ) ;
#13497=ORIENTED_EDGE ( 'NONE', *, *, #842, .T. ) ;
#13498=AXIS2_PLACEMENT_3D ( 'NONE', #15195, #3350, #11517 ) ;
#13500=CIRCLE ( 'NONE', #8513, 0.2999999999999999334 ) ;
#13504=DIRECTION ( 'NONE',  ( -1.000000000000000000, -0.000000000000000000, 0.000000000000000000 ) ) ;
#13507=AXIS2_PLACEMENT_3D ( 'NONE', #11757, #3371, #15013 ) ;
#13508=CARTESIAN_POINT ( 'NONE',  ( 29.37540678000427619, 5.299999999999999822, 7.500000000000000000 ) ) ;
#13511=CIRCLE ( 'NONE', #7109, 2.299999999999993161 ) ;
#13516=CIRCLE ( 'NONE', #6755, 0.2500000000000002220 ) ;
#13519=DIRECTION ( 'NONE',  ( 0.000000000000000000, 1.000000000000000000, -0.000000000000000000 ) ) ;
#13521=CARTESIAN_POINT ( 'NONE',  ( 8.641460742840918030, 32.93424481021354921, 68.00000000000000000 ) ) ;
#13522=ORIENTED_EDGE ( 'NONE', *, *, #3746, .T. ) ;
#13528=CARTESIAN_POINT ( 'NONE',  ( 29.44760881811060926, -2.533476707129126204, 0.1250364218578007836 ) ) ;
#13533=VERTEX_POINT ( 'NONE', #10338 ) ;
#13534=DIRECTION ( 'NONE',  ( 1.000000000000000000, 0.000000000000000000, 0.000000000000000000 ) ) ;
#13536=CARTESIAN_POINT ( 'NONE',  ( 15.95292532278785913, -34.11873716947361856, 109.6002446535588319 ) ) ;
#13537=CARTESIAN_POINT ( 'NONE',  ( -15.95292532278785913, 32.11873716947361856, 68.00000000000000000 ) ) ;
#13539=AXIS2_PLACEMENT_3D ( 'NONE', #10362, #18972, #8682 ) ;
#13540=CARTESIAN_POINT ( 'NONE',  ( -3.127054932750481964, -33.43424481021354921, 68.00000000000000000 ) ) ;
#13541=CARTESIAN_POINT ( 'NONE',  ( -32.50000000000002132, -71.00000000000001421, 3.200000000000000178 ) ) ;
#13543=CARTESIAN_POINT ( 'NONE',  ( 30.37540678000427619, 6.000000000000000000, 7.200000000000000178 ) ) ;
#13546=EDGE_CURVE ( 'NONE', #10096, #5643, #12102, .T. ) ;
#13548=ORIENTED_EDGE ( 'NONE', *, *, #3600, .T. ) ;
#13550=EDGE_CURVE ( 'NONE', #2930, #21381, #21975, .T. ) ;
#13551=ORIENTED_EDGE ( 'NONE', *, *, #14276, .F. ) ;
#13555=ORIENTED_EDGE ( 'NONE', *, *, #1292, .T. ) ;
#13558=PRODUCT_DEFINITION_CONTEXT ( 'detailed design', #14566, 'design' ) ;
#13560=CARTESIAN_POINT ( 'NONE',  ( 0.000000000000000000, -67.54634676501045476, 7.500000000000000000 ) ) ;
#13561=CARTESIAN_POINT ( 'NONE',  ( -32.20000000000001705, 72.00000000000001421, 3.200000000000000178 ) ) ;
#13562=ADVANCED_FACE ( 'NONE', ( #6882 ), #5184, .F. ) ;
#13563=FACE_OUTER_BOUND ( 'NONE', #10147, .T. ) ;
#13566=AXIS2_PLACEMENT_3D ( 'NONE', #6788, #13586, #48 ) ;
#13567=MECHANICAL_DESIGN_GEOMETRIC_PRESENTATION_REPRESENTATION('',(#10722),#16040);
#13568=CARTESIAN_POINT ( 'NONE',  ( -23.02398829872514341, 3.297363125858272070, 13.54387027667929289 ) ) ;
#13569=AXIS2_PLACEMENT_3D ( 'NONE', #3879, #20990, #602 ) ;
#13570=CARTESIAN_POINT ( 'NONE',  ( 30.37540678000427619, 0.000000000000000000, 7.200000000000000178 ) ) ;
#13571=CYLINDRICAL_SURFACE ( 'NONE', #21626, 2.500000000000002220 ) ;
#13572=ADVANCED_FACE ( 'NONE', ( #3286 ), #20290, .F. ) ;
#13573=FACE_OUTER_BOUND ( 'NONE', #16100, .T. ) ;
#13574=ORIENTED_EDGE ( 'NONE', *, *, #6447, .F. ) ;
#13578=DIRECTION ( 'NONE',  ( 1.000000000000000000, 0.000000000000000000, 0.000000000000000000 ) ) ;
#13581=CIRCLE ( 'NONE', #3273, 0.5000000000000004441 ) ;
#13582=CIRCLE ( 'NONE', #12497, 0.4999999999999995559 ) ;
#13583=CIRCLE ( 'NONE', #15009, 5.299999999999998934 ) ;
#13585=CARTESIAN_POINT ( 'NONE',  ( 31.50000000000002132, 71.70000000000001705, 3.200000000000000178 ) ) ;
#13586=DIRECTION ( 'NONE',  ( 0.000000000000000000, 0.000000000000000000, -1.000000000000000000 ) ) ;
#13590=ORIENTED_EDGE ( 'NONE', *, *, #20953, .F. ) ;
#13591=FACE_OUTER_BOUND ( 'NONE', #2980, .T. ) ;
#13592=CARTESIAN_POINT ( 'NONE',  ( 14.66174975910705847, -32.10873716947361345, 13.79999999999999893 ) ) ;
#13593=DIRECTION ( 'NONE',  ( -1.000000000000000000, 0.000000000000000000, 0.000000000000000000 ) ) ;
#13595=LINE ( 'NONE', #20436, #3991 ) ;
#13598=CIRCLE ( 'NONE', #3243, 0.5000000000000004441 ) ;
#13599=EDGE_CURVE ( 'NONE', #8047, #3329, #16920, .T. ) ;
#13600=VERTEX_POINT ( 'NONE', #8218 ) ;
#13603=DIRECTION ( 'NONE',  ( 1.000000000000000000, 0.000000000000000000, -0.000000000000000000 ) ) ;
#13604=EDGE_CURVE ( 'NONE', #12457, #14923, #7216, .T. ) ;
#13606=ORIENTED_EDGE ( 'NONE', *, *, #20598, .T. ) ;
#13607=ORIENTED_EDGE ( 'NONE', *, *, #2131, .T. ) ;
#13608=ORIENTED_EDGE ( 'NONE', *, *, #386, .T. ) ;
#13609=CYLINDRICAL_SURFACE ( 'NONE', #17398, 0.2999999999999999334 ) ;
#13613=LINE ( 'NONE', #4894, #11468 ) ;
#13618=CARTESIAN_POINT ( 'NONE',  ( -9.641460742840918030, 32.61873716947361856, 68.00000000000000000 ) ) ;
#13619=CARTESIAN_POINT ( 'NONE',  ( 4.127054932750481520, 32.93424481021354921, 42.50000000000000000 ) ) ;
#13620=LINE ( 'NONE', #18547, #193 ) ;
#13621=ORIENTED_EDGE ( 'NONE', *, *, #13050, .T. ) ;
#13622=CYLINDRICAL_SURFACE ( 'NONE', #11630, 0.2999999999999999334 ) ;
#13624=CARTESIAN_POINT ( 'NONE',  ( 26.56227312273159313, 9.958410664601840878, 13.79999999999999893 ) ) ;
#13627=ADVANCED_FACE ( 'NONE', ( #7304 ), #21187, .F. ) ;
#13630=EDGE_CURVE ( 'NONE', #19361, #11011, #15885, .T. ) ;
#13631=ORIENTED_EDGE ( 'NONE', *, *, #11151, .T. ) ;
#13636=LINE ( 'NONE', #22046, #17760 ) ;
#13638=AXIS2_PLACEMENT_3D ( 'NONE', #16696, #12994, #11105 ) ;
#13639=DIRECTION ( 'NONE',  ( -0.000000000000000000, -1.000000000000000000, -0.000000000000000000 ) ) ;
#13641=AXIS2_PLACEMENT_3D ( 'NONE', #10114, #18717, #16923 ) ;
#13642=CYLINDRICAL_SURFACE ( 'NONE', #1874, 4.351418481279133665 ) ;
#13645=DIRECTION ( 'NONE',  ( 0.000000000000000000, -1.000000000000000000, 0.000000000000000000 ) ) ;
#13648=DIRECTION ( 'NONE',  ( 0.000000000000000000, 0.000000000000000000, -1.000000000000000000 ) ) ;
#13649=CARTESIAN_POINT ( 'NONE',  ( -3.627054932750481964, -32.93424481021354921, 42.50000000000000000 ) ) ;
#13651=ORIENTED_EDGE ( 'NONE', *, *, #1419, .F. ) ;
#13654=CARTESIAN_POINT ( 'NONE',  ( 0.000000000000000000, -38.74634676501045760, 42.50000000000000000 ) ) ;
#13657=VERTEX_POINT ( 'NONE', #19053 ) ;
#13660=ORIENTED_EDGE ( 'NONE', *, *, #19001, .F. ) ;
#13663=ORIENTED_EDGE ( 'NONE', *, *, #6432, .T. ) ;
#13670=CARTESIAN_POINT ( 'NONE',  ( -23.02398829872513986, 3.004888651530577715, 13.74579066068641708 ) ) ;
#13671=CARTESIAN_POINT ( 'NONE',  ( 0.000000000000000000, -52.39333383871510108, 13.79999999999999893 ) ) ;
#13672=DIRECTION ( 'NONE',  ( -0.000000000000000000, 0.000000000000000000, 1.000000000000000000 ) ) ;
#13673=CARTESIAN_POINT ( 'NONE',  ( -29.13662752439705272, 0.000000000000000000, 13.50000000000000000 ) ) ;
#13674=ORIENTED_EDGE ( 'NONE', *, *, #13198, .T. ) ;
#13676=ORIENTED_EDGE ( 'NONE', *, *, #8718, .T. ) ;
#13677=CARTESIAN_POINT ( 'NONE',  ( 14.96174975910705918, 41.81054587065082728, 13.80000000000001315 ) ) ;
#13679=DIRECTION ( 'NONE',  ( 0.000000000000000000, 0.000000000000000000, 1.000000000000000000 ) ) ;
#13683=DIRECTION ( 'NONE',  ( 1.000000000000000000, 0.000000000000000000, 0.000000000000000000 ) ) ;
#13687=EDGE_LOOP ( 'NONE', ( #6639, #3397, #3751, #6672 ) ) ;
#13689=FACE_OUTER_BOUND ( 'NONE', #19211, .T. ) ;
#13690=CYLINDRICAL_SURFACE ( 'NONE', #16128, 0.2999999999999999334 ) ;
#13693=LINE ( 'NONE', #17172, #19868 ) ;
#13695=ORIENTED_EDGE ( 'NONE', *, *, #11664, .F. ) ;
#13697=DIRECTION ( 'NONE',  ( 1.000000000000000000, -0.000000000000000000, 0.000000000000000000 ) ) ;
#13700=ORIENTED_EDGE ( 'NONE', *, *, #15498, .T. ) ;
#13701=EDGE_LOOP ( 'NONE', ( #4593, #15978, #21538, #17283 ) ) ;
#13703=EDGE_CURVE ( 'NONE', #15847, #13894, #16508, .T. ) ;
#13704=DIRECTION ( 'NONE',  ( 1.000000000000000000, 0.000000000000000000, 0.000000000000000000 ) ) ;
#13708=EDGE_CURVE ( 'NONE', #9069, #5223, #352, .T. ) ;
#13713=DIRECTION ( 'NONE',  ( -1.000000000000000000, 0.000000000000000000, 0.000000000000000000 ) ) ;
#13716=CARTESIAN_POINT ( 'NONE',  ( 23.02398829872513986, 3.297879325581059451, 13.54382403646204480 ) ) ;
#13719=DIRECTION ( 'NONE',  ( 1.000000000000000000, 0.000000000000000000, 0.000000000000000000 ) ) ;
#13721=ORIENTED_EDGE ( 'NONE', *, *, #8726, .F. ) ;
#13722=FACE_OUTER_BOUND ( 'NONE', #17082, .T. ) ;
#13726=EDGE_CURVE ( 'NONE', #11031, #5468, #17217, .T. ) ;
#13729=ORIENTED_EDGE ( 'NONE', *, *, #9215, .F. ) ;
#13731=EDGE_CURVE ( 'NONE', #11808, #10741, #6898, .T. ) ;
#13732=FACE_OUTER_BOUND ( 'NONE', #6606, .T. ) ;
#13733=VERTEX_POINT ( 'NONE', #455 ) ;
#13734=CARTESIAN_POINT ( 'NONE',  ( -29.48732477999263679, 2.488184282963944671, 0.2032176586593637813 ) ) ;
#13735=ADVANCED_FACE ( 'NONE', ( #10658 ), #3720, .T. ) ;
#13737=ADVANCED_FACE ( 'NONE', ( #19383 ), #4052, .T. ) ;
#13738=DIRECTION ( 'NONE',  ( 1.000000000000000000, 0.000000000000000000, 0.000000000000000000 ) ) ;
#13739=LINE ( 'NONE', #11618, #10356 ) ;
#13740=CARTESIAN_POINT ( 'NONE',  ( -14.66174975910705136, -51.76873716947361714, 13.50000000000000000 ) ) ;
#13742=CIRCLE ( 'NONE', #18766, 0.2999999999999999334 ) ;
#13743=ORIENTED_EDGE ( 'NONE', *, *, #18942, .F. ) ;
#13745=DIRECTION ( 'NONE',  ( 0.000000000000000000, 0.000000000000000000, -1.000000000000000000 ) ) ;
#13748=VERTEX_POINT ( 'NONE', #1121 ) ;
#13749=VERTEX_POINT ( 'NONE', #7864 ) ;
#13752=EDGE_CURVE ( 'NONE', #4126, #3783, #3296, .T. ) ;
#13754=( LENGTH_UNIT ( ) NAMED_UNIT ( * ) SI_UNIT ( .MILLI., .METRE. ) );
#13756=VERTEX_POINT ( 'NONE', #18015 ) ;
#13757=AXIS2_PLACEMENT_3D ( 'NONE', #7125, #20660, #1943 ) ;
#13759=AXIS2_PLACEMENT_3D ( 'NONE', #14474, #21335, #9579 ) ;
#13761=EDGE_CURVE ( 'NONE', #17, #18889, #6076, .T. ) ;
#13762=DIRECTION ( 'NONE',  ( -0.000000000000000000, -0.000000000000000000, 1.000000000000000000 ) ) ;
#13763=CARTESIAN_POINT ( 'NONE',  ( -9.141460742840918030, 33.43424481021354921, 7.321391277662001151 ) ) ;
#13769=DIRECTION ( 'NONE',  ( -0.000000000000000000, 1.000000000000000000, -0.000000000000000000 ) ) ;
#13771=VECTOR ( 'NONE', #21967, 1000.000000000000000 ) ;
#13772=CARTESIAN_POINT ( 'NONE',  ( -30.67540678000428045, -63.74634676501045050, 3.500000000000000000 ) ) ;
#13773=VECTOR ( 'NONE', #17345, 1000.000000000000000 ) ;
#13774=ORIENTED_EDGE ( 'NONE', *, *, #8552, .T. ) ;
#13775=CIRCLE ( 'NONE', #19895, 0.2999999999999999334 ) ;
#13776=EDGE_LOOP ( 'NONE', ( #16459, #20014, #16938, #21547 ) ) ;
#13777=DIRECTION ( 'NONE',  ( -1.000000000000000000, 0.000000000000000000, 0.000000000000000000 ) ) ;
#13781=EDGE_CURVE ( 'NONE', #1826, #14518, #89, .T. ) ;
#13785=AXIS2_PLACEMENT_3D ( 'NONE', #7965, #12966, #17901 ) ;
#13786=CIRCLE ( 'NONE', #2732, 0.2999999999999999889 ) ;
#13787=CIRCLE ( 'NONE', #6313, 0.2999999999999999334 ) ;
#13790=CIRCLE ( 'NONE', #13094, 0.5000000000000004441 ) ;
#13792=DIRECTION ( 'NONE',  ( 1.000000000000000000, 0.000000000000000000, 0.000000000000000000 ) ) ;
#13793=DIRECTION ( 'NONE',  ( 2.388292521039847891E-16, 0.000000000000000000, 1.000000000000000000 ) ) ;
#13796=CARTESIAN_POINT ( 'NONE',  ( 26.37540678000427619, 10.94079601157914539, 13.50000000000000000 ) ) ;
#13798=CARTESIAN_POINT ( 'NONE',  ( 15.95292532278785913, -32.61873716947361856, 68.00000000000000000 ) ) ;
#13799=DIRECTION ( 'NONE',  ( 0.000000000000000000, 0.000000000000000000, 1.000000000000000000 ) ) ;
#13800=PLANE ( 'NONE',  #2685 ) ;
#13802=CIRCLE ( 'NONE', #9897, 0.2500000000000002220 ) ;
#13803=EDGE_LOOP ( 'NONE', ( #9164, #9784, #5481, #10673 ) ) ;
#13805=AXIS2_PLACEMENT_3D ( 'NONE', #11693, #7126, #10370 ) ;
#13807=ORIENTED_EDGE ( 'NONE', *, *, #4083, .T. ) ;
#13809=DIRECTION ( 'NONE',  ( 1.000000000000000000, -3.052134192567367925E-16, 0.000000000000000000 ) ) ;
#13810=EDGE_CURVE ( 'NONE', #21351, #10680, #21736, .T. ) ;
#13811=CARTESIAN_POINT ( 'NONE',  ( -15.95292532278785913, 32.61873716947361856, 68.50000000000000000 ) ) ;
#13818=VERTEX_POINT ( 'NONE', #13209 ) ;
#13820=DIRECTION ( 'NONE',  ( 0.000000000000000000, 0.000000000000000000, 1.000000000000000000 ) ) ;
#13822=AXIS2_PLACEMENT_3D ( 'NONE', #13193, #18786, #14984 ) ;
#13823=AXIS2_PLACEMENT_3D ( 'NONE', #15490, #7012, #20662 ) ;
#13825=DIRECTION ( 'NONE',  ( 0.000000000000000000, 1.000000000000000000, 0.000000000000000000 ) ) ;
#13827=CARTESIAN_POINT ( 'NONE',  ( 23.02398829872514341, 2.388551872609025573, 13.39771463486666470 ) ) ;
#13828=CARTESIAN_POINT ( 'NONE',  ( 17.95292532278785913, 50.11873716947361856, 68.00000000000000000 ) ) ;
#13830=SPHERICAL_SURFACE ( 'NONE', #1202, 0.5000000000000000000 ) ;
#13833=ADVANCED_FACE ( 'NONE', ( #4717 ), #12567, .F. ) ;
#13836=DIRECTION ( 'NONE',  ( 2.832483164223434527E-16, -1.000000000000000000, 0.000000000000000000 ) ) ;
#13837=( BOUNDED_CURVE ( )  B_SPLINE_CURVE ( 3, ( #11164, #7610, #2780, #4454 ),
 .UNSPECIFIED., .F., .T. ) 
 B_SPLINE_CURVE_WITH_KNOTS ( ( 4, 4 ),
 ( 1.570796326794896558, 3.141592653589793116 ),
 .UNSPECIFIED. ) 
 CURVE ( )  GEOMETRIC_REPRESENTATION_ITEM ( )  RATIONAL_B_SPLINE_CURVE ( ( 1.000000000000000000, 0.8047378541243649375, 0.8047378541243649375, 1.000000000000000000 ) ) 
 REPRESENTATION_ITEM ( '' )  );
#13840=DIRECTION ( 'NONE',  ( -1.000000000000000000, 0.000000000000000000, 0.000000000000000000 ) ) ;
#13842=VECTOR ( 'NONE', #11612, 1000.000000000000000 ) ;
#13843=AXIS2_PLACEMENT_3D ( 'NONE', #17118, #15640, #18913 ) ;
#13844=AXIS2_PLACEMENT_3D ( 'NONE', #10748, #10633, #19256 ) ;
#13851=DIRECTION ( 'NONE',  ( 0.000000000000000000, 0.000000000000000000, 1.000000000000000000 ) ) ;
#13853=DIRECTION ( 'NONE',  ( 0.000000000000000000, 0.000000000000000000, 1.000000000000000000 ) ) ;
#13855=DIRECTION ( 'NONE',  ( -1.000000000000000000, 0.000000000000000000, 0.000000000000000000 ) ) ;
#13857=AXIS2_PLACEMENT_3D ( 'NONE', #8363, #15295, #20346 ) ;
#13858=VECTOR ( 'NONE', #11603, 1000.000000000000000 ) ;
#13859=CARTESIAN_POINT ( 'NONE',  ( 29.50000000000002132, 2.512390033608338236, 0.2999999999999947153 ) ) ;
#13860=CARTESIAN_POINT ( 'NONE',  ( 0.000000000000000000, 0.000000000000000000, 1.500000000000000000 ) ) ;
#13861=TOROIDAL_SURFACE ( 'NONE', #15297, 2.800000000000002043, 0.2999999999999999889 ) ;
#13862=DIRECTION ( 'NONE',  ( -1.000000000000000000, 0.000000000000000000, 0.000000000000000000 ) ) ;
#13863=VECTOR ( 'NONE', #21058, 1000.000000000000000 ) ;
#13865=ORIENTED_EDGE ( 'NONE', *, *, #19492, .F. ) ;
#13867=DIRECTION ( 'NONE',  ( 0.000000000000000000, 0.000000000000000000, -1.000000000000000000 ) ) ;
#13868=CARTESIAN_POINT ( 'NONE',  ( 0.000000000000000000, -71.70000000000001705, 1.800000000000000044 ) ) ;
#13869=EDGE_CURVE ( 'NONE', #2970, #9771, #20811, .T. ) ;
#13871=ORIENTED_EDGE ( 'NONE', *, *, #13869, .F. ) ;
#13873=EDGE_CURVE ( 'NONE', #16490, #2211, #5958, .T. ) ;
#13875=EDGE_LOOP ( 'NONE', ( #17854, #15314, #8099 ) ) ;
#13876=AXIS2_PLACEMENT_3D ( 'NONE', #8163, #21818, #9731 ) ;
#13877=CARTESIAN_POINT ( 'NONE',  ( 23.02398829872514341, -2.334689865870722691, 13.36916081092389241 ) ) ;
#13880=ORIENTED_EDGE ( 'NONE', *, *, #10868, .F. ) ;
#13881=CIRCLE ( 'NONE', #22129, 0.6999999999999992895 ) ;
#13882=DIRECTION ( 'NONE',  ( 0.000000000000000000, -1.000000000000000000, 0.000000000000000000 ) ) ;
#13883=PLANE ( 'NONE',  #18075 ) ;
#13884=ADVANCED_FACE ( 'NONE', ( #7970 ), #16454, .F. ) ;
#13885=FACE_OUTER_BOUND ( 'NONE', #275, .T. ) ;
#13886=CARTESIAN_POINT ( 'NONE',  ( 23.02398829872513986, 3.528912754968628551, 13.79999999999999893 ) ) ;
#13887=DIRECTION ( 'NONE',  ( 0.000000000000000000, 0.000000000000000000, -1.000000000000000000 ) ) ;
#13888=CARTESIAN_POINT ( 'NONE',  ( -29.37540678000427619, -5.299999999999999822, 7.200000000000000178 ) ) ;
#13890=CARTESIAN_POINT ( 'NONE',  ( -9.641460742840918030, -32.11873716947361856, 68.00000000000000000 ) ) ;
#13891=CARTESIAN_POINT ( 'NONE',  ( -14.96174975910705207, -51.86873716947361856, 68.00000000000000000 ) ) ;
#13894=VERTEX_POINT ( 'NONE', #11960 ) ;
#13896=DIRECTION ( 'NONE',  ( 0.000000000000000000, 0.000000000000000000, 1.000000000000000000 ) ) ;
#13900=DIRECTION ( 'NONE',  ( -0.000000000000000000, -1.000000000000000000, -0.000000000000000000 ) ) ;
#13902=PLANE ( 'NONE',  #20951 ) ;
#13904=AXIS2_PLACEMENT_3D ( 'NONE', #12828, #7702, #14505 ) ;
#13905=CARTESIAN_POINT ( 'NONE',  ( -31.50000000000002132, 72.00000000000001421, 3.200000000000000178 ) ) ;
#13906=CIRCLE ( 'NONE', #17144, 2.000000000000001776 ) ;
#13907=AXIS2_PLACEMENT_3D ( 'NONE', #15066, #5228, #6585 ) ;
#13908=CARTESIAN_POINT ( 'NONE',  ( 8.641460742840918030, -32.93424481021354921, 68.00000000000000000 ) ) ;
#13909=VERTEX_POINT ( 'NONE', #6961 ) ;
#13911=CARTESIAN_POINT ( 'NONE',  ( 30.67540678000428045, -6.000000000000000000, 3.799999999999999822 ) ) ;
#13912=EDGE_CURVE ( 'NONE', #9447, #2103, #16124, .T. ) ;
#13913=DIRECTION ( 'NONE',  ( 0.000000000000000000, 0.000000000000000000, -1.000000000000000000 ) ) ;
#13917=EDGE_LOOP ( 'NONE', ( #15696, #3609, #21800, #4831 ) ) ;
#13918=FACE_OUTER_BOUND ( 'NONE', #142, .T. ) ;
#13919=DIRECTION ( 'NONE',  ( -0.000000000000000000, -0.000000000000000000, -1.000000000000000000 ) ) ;
#13920=DIRECTION ( 'NONE',  ( 1.000000000000000000, 0.000000000000000000, 0.000000000000000000 ) ) ;
#13923=CARTESIAN_POINT ( 'NONE',  ( -28.87540678000427619, -6.494748934539263274, 7.799999999999999822 ) ) ;
#13925=EDGE_CURVE ( 'NONE', #2722, #11031, #10187, .T. ) ;
#13927=FACE_OUTER_BOUND ( 'NONE', #21232, .T. ) ;
#13928=AXIS2_PLACEMENT_3D ( 'NONE', #6824, #6375, #10153 ) ;
#13931=ORIENTED_EDGE ( 'NONE', *, *, #12682, .T. ) ;
#13933=ORIENTED_EDGE ( 'NONE', *, *, #9818, .F. ) ;
#13935=DIRECTION ( 'NONE',  ( -0.000000000000000000, -0.000000000000000000, -1.000000000000000000 ) ) ;
#13937=ORIENTED_EDGE ( 'NONE', *, *, #250, .T. ) ;
#13938=DIRECTION ( 'NONE',  ( 1.000000000000000000, -0.000000000000000000, 0.000000000000000000 ) ) ;
#13939=PLANE ( 'NONE',  #17450 ) ;
#13940=VECTOR ( 'NONE', #10018, 1000.000000000000000 ) ;
#13941=EDGE_CURVE ( 'NONE', #5643, #3983, #20384, .T. ) ;
#13945=VERTEX_POINT ( 'NONE', #10087 ) ;
#13948=VERTEX_POINT ( 'NONE', #1558 ) ;
#13949=DIRECTION ( 'NONE',  ( 0.000000000000000000, -0.000000000000000000, 1.000000000000000000 ) ) ;
#13951=ORIENTED_EDGE ( 'NONE', *, *, #7051, .T. ) ;
#13953=DIRECTION ( 'NONE',  ( -1.000000000000000000, 0.000000000000000000, 0.000000000000000000 ) ) ;
#13954=ORIENTED_EDGE ( 'NONE', *, *, #14882, .F. ) ;
#13957=EDGE_CURVE ( 'NONE', #1047, #2085, #1497, .T. ) ;
#13960=CARTESIAN_POINT ( 'NONE',  ( -3.127054932750481964, -32.61873716947361856, 42.50000000000000711 ) ) ;
#13962=ADVANCED_FACE ( 'NONE', ( #3257 ), #2408, .F. ) ;
#13966=VERTEX_POINT ( 'NONE', #11525 ) ;
#13967=DIRECTION ( 'NONE',  ( 0.000000000000000000, 0.000000000000000000, -1.000000000000000000 ) ) ;
#13972=CYLINDRICAL_SURFACE ( 'NONE', #13844, 0.3000000000000003775 ) ;
#13973=CARTESIAN_POINT ( 'NONE',  ( -14.96174975910705207, 51.83071861726173779, 13.82019355104894309 ) ) ;
#13974=AXIS2_PLACEMENT_3D ( 'NONE', #11103, #7768, #14571 ) ;
#13976=VERTEX_POINT ( 'NONE', #20495 ) ;
#13983=ORIENTED_EDGE ( 'NONE', *, *, #12644, .F. ) ;
#13984=LINE ( 'NONE', #14320, #20093 ) ;
#13985=VERTEX_POINT ( 'NONE', #13649 ) ;
#13986=ORIENTED_EDGE ( 'NONE', *, *, #18893, .F. ) ;
#13989=ADVANCED_FACE ( 'NONE', ( #13317 ), #5090, .T. ) ;
#13991=DIRECTION ( 'NONE',  ( 0.000000000000000000, 0.000000000000000000, 1.000000000000000000 ) ) ;
#13993=B_SPLINE_CURVE_WITH_KNOTS ( 'NONE', 3,
 ( #4509, #11216, #11329, #19503, #4183, #9328, #7656, #11448, #9779, #6318, #18275, #6772, #13118, #8423 ),
 .UNSPECIFIED., .F., .F.,
 ( 4, 2, 2, 2, 2, 2, 4 ),
 ( 0.000000000000000000, 0.0006835338044177908991, 0.001025300706626684722, 0.001196184157731131200, 0.001281625883283354006, 0.001324346746059462589, 0.001367067608835571173 ),
 .UNSPECIFIED. ) ;
#13994=AXIS2_PLACEMENT_3D ( 'NONE', #500, #13713, #3667 ) ;
#13996=VECTOR ( 'NONE', #11297, 1000.000000000000000 ) ;
#13998=CIRCLE ( 'NONE', #10457, 0.2999999999999999334 ) ;
#14001=DIRECTION ( 'NONE',  ( 1.000000000000000000, 0.000000000000000000, 0.000000000000000000 ) ) ;
#14004=ORIENTED_EDGE ( 'NONE', *, *, #9536, .F. ) ;
#14009=EDGE_LOOP ( 'NONE', ( #15918, #17997, #10572, #15639 ) ) ;
#14012=AXIS2_PLACEMENT_3D ( 'NONE', #13022, #21896, #19766 ) ;
#14013=EDGE_CURVE ( 'NONE', #16038, #124, #7600, .T. ) ;
#14017=ORIENTED_EDGE ( 'NONE', *, *, #7546, .T. ) ;
#14019=AXIS2_PLACEMENT_3D ( 'NONE', #22092, #1820, #8658 ) ;
#14020=EDGE_CURVE ( 'NONE', #6249, #1178, #5274, .T. ) ;
#14021=DIRECTION ( 'NONE',  ( 0.000000000000000000, 1.000000000000000000, 0.000000000000000000 ) ) ;
#14022=CARTESIAN_POINT ( 'NONE',  ( 25.37540678000427263, 67.54634676501045476, 7.799999999999999822 ) ) ;
#14023=DIRECTION ( 'NONE',  ( -0.000000000000000000, 0.000000000000000000, -1.000000000000000000 ) ) ;
#14026=DIRECTION ( 'NONE',  ( -1.000000000000000000, -0.000000000000000000, -0.000000000000000000 ) ) ;
#14029=DIRECTION ( 'NONE',  ( 0.000000000000000000, 0.000000000000000000, 1.000000000000000000 ) ) ;
#14030=DIRECTION ( 'NONE',  ( 0.000000000000000000, 0.000000000000000000, 1.000000000000000000 ) ) ;
#14034=DIRECTION ( 'NONE',  ( -0.000000000000000000, -1.000000000000000000, 0.000000000000000000 ) ) ;
#14036=DIRECTION ( 'NONE',  ( 1.000000000000000000, 0.000000000000000000, 0.000000000000000000 ) ) ;
#14037=ADVANCED_FACE ( 'NONE', ( #10417 ), #17226, .T. ) ;
#14038=ORIENTED_EDGE ( 'NONE', *, *, #15, .T. ) ;
#14039=DIRECTION ( 'NONE',  ( 1.000000000000000000, 0.000000000000000000, 0.000000000000000000 ) ) ;
#14040=EDGE_CURVE ( 'NONE', #15569, #8198, #658, .T. ) ;
#14045=FACE_OUTER_BOUND ( 'NONE', #4822, .T. ) ;
#14046=CARTESIAN_POINT ( 'NONE',  ( 17.45292532278785913, -50.11873716947361856, 68.00000000000000000 ) ) ;
#14047=DIRECTION ( 'NONE',  ( -1.000000000000000000, -3.052134192567367925E-16, 0.000000000000000000 ) ) ;
#14049=CARTESIAN_POINT ( 'NONE',  ( -27.37540678000427619, 7.754037881813018962E-15, 42.50000000000000000 ) ) ;
#14050=EDGE_CURVE ( 'NONE', #14759, #16038, #2231, .T. ) ;
#14054=VERTEX_POINT ( 'NONE', #10745 ) ;
#14057=DIRECTION ( 'NONE',  ( 1.000000000000000000, 0.000000000000000000, 0.000000000000000000 ) ) ;
#14058=DIRECTION ( 'NONE',  ( -0.000000000000000000, -0.000000000000000000, -1.000000000000000000 ) ) ;
#14063=DIRECTION ( 'NONE',  ( -0.000000000000000000, 1.000000000000000000, -0.000000000000000000 ) ) ;
#14064=ORIENTED_EDGE ( 'NONE', *, *, #19707, .T. ) ;
#14066=VECTOR ( 'NONE', #5364, 1000.000000000000000 ) ;
#14070=CARTESIAN_POINT ( 'NONE',  ( -31.50000000000002132, -71.70000000000001705, 3.500000000000000000 ) ) ;
#14071=DIRECTION ( 'NONE',  ( 0.000000000000000000, 0.000000000000000000, 1.000000000000000000 ) ) ;
#14072=CIRCLE ( 'NONE', #19089, 0.2999999999999999334 ) ;
#14074=FACE_OUTER_BOUND ( 'NONE', #10095, .T. ) ;
#14078=DIRECTION ( 'NONE',  ( -0.000000000000000000, -0.000000000000000000, -1.000000000000000000 ) ) ;
#14079=DIRECTION ( 'NONE',  ( 1.000000000000000000, 0.000000000000000000, 0.000000000000000000 ) ) ;
#14080=DIRECTION ( 'NONE',  ( 1.000000000000000000, 0.000000000000000000, 0.000000000000000000 ) ) ;
#14081=ORIENTED_EDGE ( 'NONE', *, *, #11469, .F. ) ;
#14082=ORIENTED_EDGE ( 'NONE', *, *, #10824, .F. ) ;
#14083=EDGE_LOOP ( 'NONE', ( #9774, #8619, #554, #14647, #9270, #18500, #10043, #13937, #6421, #15069 ) ) ;
#14084=EDGE_CURVE ( 'NONE', #4893, #5864, #20713, .T. ) ;
#14085=ORIENTED_EDGE ( 'NONE', *, *, #20359, .F. ) ;
#14087=CARTESIAN_POINT ( 'NONE',  ( 23.02398829872513986, -2.928406208502775776, 13.54172988673462896 ) ) ;
#14090=CARTESIAN_POINT ( 'NONE',  ( 17.95292532278785913, -50.11873716947361856, 14.00000000000000000 ) ) ;
#14091=CARTESIAN_POINT ( 'NONE',  ( 29.05186365738250842, 0.05288320938007240457, -150.0833101980363722 ) ) ;
#14099=DIRECTION ( 'NONE',  ( 0.000000000000000000, 0.000000000000000000, -1.000000000000000000 ) ) ;
#14101=ORIENTED_EDGE ( 'NONE', *, *, #1281, .F. ) ;
#14106=DIRECTION ( 'NONE',  ( 1.000000000000000000, 0.000000000000000000, 0.000000000000000000 ) ) ;
#14109=EDGE_LOOP ( 'NONE', ( #11308, #3934, #93, #4535 ) ) ;
#14110=CIRCLE ( 'NONE', #20204, 1.000000000000000888 ) ;
#14111=AXIS2_PLACEMENT_3D ( 'NONE', #2425, #16506, #12922 ) ;
#14114=DIRECTION ( 'NONE',  ( -0.000000000000000000, -0.000000000000000000, 1.000000000000000000 ) ) ;
#14116=ORIENTED_EDGE ( 'NONE', *, *, #17949, .F. ) ;
#14118=CARTESIAN_POINT ( 'NONE',  ( 15.95292532278785913, -52.39333383871510108, 13.79999999999999893 ) ) ;
#14120=CARTESIAN_POINT ( 'NONE',  ( 27.37540678000427974, -5.683640910026986681, 13.79999999999999893 ) ) ;
#14121=DIRECTION ( 'NONE',  ( -0.000000000000000000, -0.000000000000000000, -1.000000000000000000 ) ) ;
#14123=CARTESIAN_POINT ( 'NONE',  ( -3.127054932750481964, 32.11873716947361856, 109.6002446535588319 ) ) ;
#14124=CIRCLE ( 'NONE', #20596, 0.2999999999999999334 ) ;
#14125=CIRCLE ( 'NONE', #20939, 0.2999999999999999334 ) ;
#14126=AXIS2_PLACEMENT_3D ( 'NONE', #17095, #18767, #16970 ) ;
#14127=VERTEX_POINT ( 'NONE', #10521 ) ;
#14128=CARTESIAN_POINT ( 'NONE',  ( 29.37540678000427619, 6.000000000000000000, 3.799999999999999822 ) ) ;
#14129=DIRECTION ( 'NONE',  ( 0.000000000000000000, -0.000000000000000000, -1.000000000000000000 ) ) ;
#14132=ORIENTED_EDGE ( 'NONE', *, *, #4055, .T. ) ;
#14133=ORIENTED_EDGE ( 'NONE', *, *, #13599, .F. ) ;
#14135=CARTESIAN_POINT ( 'NONE',  ( -17.92752199202934094, -38.74634676501045760, 13.79999999999999893 ) ) ;
#14137=ORIENTED_EDGE ( 'NONE', *, *, #13873, .F. ) ;
#14143=ADVANCED_FACE ( 'NONE', ( #5833 ), #7711, .T. ) ;
#14144=ORIENTED_EDGE ( 'NONE', *, *, #3078, .F. ) ;
#14146=AXIS2_PLACEMENT_3D ( 'NONE', #6434, #1142, #21422 ) ;
#14147=CARTESIAN_POINT ( 'NONE',  ( -25.37540678000427263, 67.24634676501045760, 7.799999999999999822 ) ) ;
#14148=EDGE_LOOP ( 'NONE', ( #16815, #18719, #15458, #17510 ) ) ;
#14149=DIRECTION ( 'NONE',  ( 0.000000000000000000, 0.000000000000000000, 1.000000000000000000 ) ) ;
#14150=CARTESIAN_POINT ( 'NONE',  ( -26.56227312273159313, -9.958410664601842655, 42.50000000000000000 ) ) ;
#14152=CARTESIAN_POINT ( 'NONE',  ( 25.37540678000427263, 69.04634676501045476, 3.799999999999999822 ) ) ;
#14153=ORIENTED_EDGE ( 'NONE', *, *, #2625, .T. ) ;
#14155=LINE ( 'NONE', #19102, #20318 ) ;
#14156=ADVANCED_FACE ( 'NONE', ( #19916 ), #1102, .T. ) ;
#14157=CARTESIAN_POINT ( 'NONE',  ( -30.67540678000427690, -6.000000000000000000, 3.500000000000000000 ) ) ;
#14158=CARTESIAN_POINT ( 'NONE',  ( -23.04273156199908357, -2.261510999192740901, 7.500000000000000000 ) ) ;
#14160=CIRCLE ( 'NONE', #6328, 0.2500000000000002220 ) ;
#14161=AXIS2_PLACEMENT_3D ( 'NONE', #1078, #7591, #12814 ) ;
#14163=TOROIDAL_SURFACE ( 'NONE', #2734, 0.7000000000000000666, 0.2999999999999999889 ) ;
#14165=CARTESIAN_POINT ( 'NONE',  ( 4.127054932750481520, -32.93424481021354921, 68.00000000000000000 ) ) ;
#14166=FACE_OUTER_BOUND ( 'NONE', #1395, .T. ) ;
#14168=AXIS2_PLACEMENT_3D ( 'NONE', #20268, #14885, #20156 ) ;
#14172=ORIENTED_EDGE ( 'NONE', *, *, #11157, .F. ) ;
#14174=AXIS2_PLACEMENT_3D ( 'NONE', #16125, #2493, #2946 ) ;
#14175=EDGE_LOOP ( 'NONE', ( #16728, #19618, #4462, #12221 ) ) ;
#14176=AXIS2_PLACEMENT_3D ( 'NONE', #1944, #67, #14030 ) ;
#14178=VERTEX_POINT ( 'NONE', #2565 ) ;
#14180=VECTOR ( 'NONE', #2513, 1000.000000000000000 ) ;
#14181=CIRCLE ( 'NONE', #5287, 0.2999999999999999334 ) ;
#14182=DIRECTION ( 'NONE',  ( 0.000000000000000000, 0.000000000000000000, -1.000000000000000000 ) ) ;
#14185=ORIENTED_EDGE ( 'NONE', *, *, #11025, .T. ) ;
#14186=CARTESIAN_POINT ( 'NONE',  ( -14.96174975910705207, 51.86873716947361856, 14.00000000000000000 ) ) ;
#14188=CARTESIAN_POINT ( 'NONE',  ( -27.37540678000427974, -5.683640910026986681, 42.50000000000000000 ) ) ;
#14189=EDGE_CURVE ( 'NONE', #4651, #7158, #7968, .T. ) ;
#14191=VECTOR ( 'NONE', #21036, 1000.000000000000000 ) ;
#14192=AXIS2_PLACEMENT_3D ( 'NONE', #7937, #4348, #6151 ) ;
#14199=CIRCLE ( 'NONE', #14547, 5.300000000000006040 ) ;
#14201=CIRCLE ( 'NONE', #11347, 4.351418481279133665 ) ;
#14204=ORIENTED_EDGE ( 'NONE', *, *, #20302, .F. ) ;
#14206=CARTESIAN_POINT ( 'NONE',  ( 23.32398829872514057, -3.528912754968634324, 13.50000000000000000 ) ) ;
#14207=ORIENTED_EDGE ( 'NONE', *, *, #17932, .T. ) ;
#14208=CARTESIAN_POINT ( 'NONE',  ( -0.000000000000000000, 51.61873716947361856, 68.50000000000000000 ) ) ;
#14209=CIRCLE ( 'NONE', #17083, 0.5000000000000004441 ) ;
#14210=CIRCLE ( 'NONE', #12068, 0.5000000000000004441 ) ;
#14215=CARTESIAN_POINT ( 'NONE',  ( 30.37540678000427619, 6.000000000000000000, 3.799999999999999822 ) ) ;
#14217=AXIS2_PLACEMENT_3D ( 'NONE', #14668, #2826, #17916 ) ;
#14221=CARTESIAN_POINT ( 'NONE',  ( -23.02398829872513986, 2.501891433834999567, 13.57888791970315445 ) ) ;
#14227=VERTEX_POINT ( 'NONE', #4360 ) ;
#14231=ORIENTED_EDGE ( 'NONE', *, *, #11652, .T. ) ;
#14237=ADVANCED_FACE ( 'NONE', ( #6270 ), #4129, .F. ) ;
#14240=DIRECTION ( 'NONE',  ( -1.000000000000000000, 0.000000000000000000, 0.000000000000000000 ) ) ;
#14242=CARTESIAN_POINT ( 'NONE',  ( 15.95292532278785913, -34.11873716947361856, 68.50000000000000000 ) ) ;
#14245=EDGE_CURVE ( 'NONE', #11756, #9769, #985, .T. ) ;
#14246=DIRECTION ( 'NONE',  ( -0.000000000000000000, -0.000000000000000000, -1.000000000000000000 ) ) ;
#14248=CARTESIAN_POINT ( 'NONE',  ( 14.98281217233416562, 51.83338592095527275, 13.50000000000000000 ) ) ;
#14250=DIRECTION ( 'NONE',  ( 1.000000000000000000, 0.000000000000000000, 0.000000000000000000 ) ) ;
#14252=DIRECTION ( 'NONE',  ( 1.000000000000000000, 0.000000000000000000, 0.000000000000000000 ) ) ;
#14254=DIRECTION ( 'NONE',  ( 0.000000000000000000, 0.000000000000000000, 1.000000000000000000 ) ) ;
#14258=LINE ( 'NONE', #16036, #18870 ) ;
#14259=DIRECTION ( 'NONE',  ( 0.000000000000000000, 0.000000000000000000, 1.000000000000000000 ) ) ;
#14261=CYLINDRICAL_SURFACE ( 'NONE', #22085, 0.3000000000000003775 ) ;
#14262=ADVANCED_FACE ( 'NONE', ( #14637 ), #21184, .T. ) ;
#14263=VECTOR ( 'NONE', #14998, 1000.000000000000000 ) ;
#14265=CARTESIAN_POINT ( 'NONE',  ( -9.641460742840918030, -32.11873716947361856, 42.50000000000000711 ) ) ;
#14267=ORIENTED_EDGE ( 'NONE', *, *, #13236, .T. ) ;
#14273=FACE_OUTER_BOUND ( 'NONE', #16117, .T. ) ;
#14274=DIRECTION ( 'NONE',  ( -0.000000000000000000, -0.000000000000000000, -1.000000000000000000 ) ) ;
#14276=EDGE_CURVE ( 'NONE', #4860, #421, #2906, .T. ) ;
#14277=DIRECTION ( 'NONE',  ( 0.000000000000000000, 0.000000000000000000, 1.000000000000000000 ) ) ;
#14278=CARTESIAN_POINT ( 'NONE',  ( 31.50000000000002132, -71.00000000000001421, 3.200000000000000178 ) ) ;
#14281=ORIENTED_EDGE ( 'NONE', *, *, #371, .T. ) ;
#14283=CIRCLE ( 'NONE', #17839, 0.3000000000000003775 ) ;
#14284=DIRECTION ( 'NONE',  ( 1.000000000000000000, 0.000000000000000000, 0.000000000000000000 ) ) ;
#14288=ORIENTED_EDGE ( 'NONE', *, *, #20383, .F. ) ;
#14289=CARTESIAN_POINT ( 'NONE',  ( -9.141460742840918030, 32.93424481021354921, 42.50000000000000000 ) ) ;
#14290=CARTESIAN_POINT ( 'NONE',  ( 0.000000000000000000, -4.700000000000000178, 3.799999999999999822 ) ) ;
#14297=AXIS2_PLACEMENT_3D ( 'NONE', #17701, #3739, #2270 ) ;
#14298=CARTESIAN_POINT ( 'NONE',  ( -15.95292532278785913, -34.11873716947361856, 109.6002446535588319 ) ) ;
#14299=LINE ( 'NONE', #18919, #10652 ) ;
#14301=ADVANCED_FACE ( 'NONE', ( #13918 ), #20767, .T. ) ;
#14302=CARTESIAN_POINT ( 'NONE',  ( -27.37540678000427974, -10.94079601157914716, 13.79999999999999893 ) ) ;
#14305=EDGE_CURVE ( 'NONE', #5089, #21686, #389, .T. ) ;
#14308=VECTOR ( 'NONE', #16606, 1000.000000000000000 ) ;
#14312=ORIENTED_EDGE ( 'NONE', *, *, #18700, .F. ) ;
#14313=ORIENTED_EDGE ( 'NONE', *, *, #17047, .T. ) ;
#14314=VERTEX_POINT ( 'NONE', #4695 ) ;
#14315=CYLINDRICAL_SURFACE ( 'NONE', #21050, 0.2999999999999999334 ) ;
#14317=ORIENTED_EDGE ( 'NONE', *, *, #9755, .T. ) ;
#14320=CARTESIAN_POINT ( 'NONE',  ( 15.95292532278785913, 32.61873716947361856, 68.50000000000000000 ) ) ;
#14325=DIRECTION ( 'NONE',  ( 0.000000000000000000, 0.000000000000000000, 1.000000000000000000 ) ) ;
#14329=CARTESIAN_POINT ( 'NONE',  ( -23.04273161205373910, 2.261511134070790074, 13.23413512703648820 ) ) ;
#14330=AXIS2_PLACEMENT_3D ( 'NONE', #702, #16022, #7117 ) ;
#14334=AXIS2_PLACEMENT_3D ( 'NONE', #13117, #9676, #917 ) ;
#14335=DIRECTION ( 'NONE',  ( 0.000000000000000000, 0.000000000000000000, -1.000000000000000000 ) ) ;
#14339=FACE_OUTER_BOUND ( 'NONE', #14435, .T. ) ;
#14341=ORIENTED_EDGE ( 'NONE', *, *, #6545, .F. ) ;
#14343=EDGE_CURVE ( 'NONE', #9447, #13326, #1745, .T. ) ;
#14346=CARTESIAN_POINT ( 'NONE',  ( 15.21174975910707161, -51.61873716947361856, 68.25000000000000000 ) ) ;
#14351=CARTESIAN_POINT ( 'NONE',  ( -23.02398829872513986, 2.157133568460765538, 42.50000000000000000 ) ) ;
#14352=DIRECTION ( 'NONE',  ( 0.000000000000000000, 0.000000000000000000, 1.000000000000000000 ) ) ;
#14353=CARTESIAN_POINT ( 'NONE',  ( 18.22752199202934520, -50.11873716947361856, 13.79999999999999716 ) ) ;
#14354=CARTESIAN_POINT ( 'NONE',  ( -23.02398829872514341, 2.624937972534823860, 13.63083126556637126 ) ) ;
#14356=CARTESIAN_POINT ( 'NONE',  ( 28.87540678000428329, -6.494748934539265051, 13.24746166461178554 ) ) ;
#14358=CARTESIAN_POINT ( 'NONE',  ( 0.000000000000000000, 5.000000000000000000, 3.799999999999999822 ) ) ;
#14359=EDGE_CURVE ( 'NONE', #8930, #4773, #10250, .T. ) ;
#14360=ORIENTED_EDGE ( 'NONE', *, *, #10604, .F. ) ;
#14361=ORIENTED_EDGE ( 'NONE', *, *, #5619, .F. ) ;
#14364=CARTESIAN_POINT ( 'NONE',  ( 17.92752199202933738, 38.74634676501045760, 13.62426406871192874 ) ) ;
#14367=LINE ( 'NONE', #1054, #5652 ) ;
#14368=EDGE_CURVE ( 'NONE', #2212, #16494, #16637, .T. ) ;
#14372=AXIS2_PLACEMENT_3D ( 'NONE', #559, #3952, #2358 ) ;
#14373=FACE_OUTER_BOUND ( 'NONE', #1027, .T. ) ;
#14375=CARTESIAN_POINT ( 'NONE',  ( 3.627054932750481964, -33.43424481021354921, 68.00000000000000000 ) ) ;
#14376=ORIENTED_EDGE ( 'NONE', *, *, #2668, .T. ) ;
#14377=DIRECTION ( 'NONE',  ( -0.000000000000000000, -0.000000000000000000, -1.000000000000000000 ) ) ;
#14382=SURFACE_STYLE_USAGE ( .BOTH. , #4545 ) ;
#14383=EDGE_CURVE ( 'NONE', #15453, #3099, #12887, .T. ) ;
#14388=ORIENTED_EDGE ( 'NONE', *, *, #224, .T. ) ;
#14391=DIRECTION ( 'NONE',  ( -0.000000000000000000, -0.000000000000000000, -1.000000000000000000 ) ) ;
#14394=EDGE_CURVE ( 'NONE', #4119, #2536, #5219, .T. ) ;
#14399=DIRECTION ( 'NONE',  ( 0.000000000000000000, 0.000000000000000000, 1.000000000000000000 ) ) ;
#14400=DIRECTION ( 'NONE',  ( 0.000000000000000000, -1.000000000000000000, 0.000000000000000000 ) ) ;
#14402=CARTESIAN_POINT ( 'NONE',  ( -29.37540678000427619, -6.000000000000000000, 3.799999999999999822 ) ) ;
#14404=ORIENTED_EDGE ( 'NONE', *, *, #7526, .T. ) ;
#14405=DIRECTION ( 'NONE',  ( 1.000000000000000000, 0.000000000000000000, 0.000000000000000000 ) ) ;
#14409=DIRECTION ( 'NONE',  ( 0.000000000000000000, -1.000000000000000000, 0.000000000000000000 ) ) ;
#14410=CARTESIAN_POINT ( 'NONE',  ( -18.22752199202934520, -39.04634676501046187, 13.50000000000000000 ) ) ;
#14412=ORIENTED_EDGE ( 'NONE', *, *, #12873, .F. ) ;
#14413=FACE_OUTER_BOUND ( 'NONE', #7521, .T. ) ;
#14416=EDGE_CURVE ( 'NONE', #8846, #11165, #3268, .T. ) ;
#14417=ORIENTED_EDGE ( 'NONE', *, *, #6398, .T. ) ;
#14418=LINE ( 'NONE', #21934, #1677 ) ;
#14422=DIRECTION ( 'NONE',  ( 0.000000000000000000, 0.000000000000000000, -1.000000000000000000 ) ) ;
#14423=CARTESIAN_POINT ( 'NONE',  ( -15.21174975910705207, 51.61873716947361856, 68.00000000000000000 ) ) ;
#14424=DIRECTION ( 'NONE',  ( 0.000000000000000000, -1.000000000000000000, 0.000000000000000000 ) ) ;
#14426=CARTESIAN_POINT ( 'NONE',  ( 29.37540678000427619, -6.000000000000000000, 3.500000000000000000 ) ) ;
#14427=EDGE_CURVE ( 'NONE', #19370, #11890, #5609, .T. ) ;
#14428=FACE_OUTER_BOUND ( 'NONE', #20714, .T. ) ;
#14432=DIRECTION ( 'NONE',  ( 1.000000000000000000, 0.000000000000000000, 0.000000000000000000 ) ) ;
#14435=EDGE_LOOP ( 'NONE', ( #14522, #21106, #19176, #21765 ) ) ;
#14437=ORIENTED_EDGE ( 'NONE', *, *, #6695, .T. ) ;
#14442=AXIS2_PLACEMENT_3D ( 'NONE', #15886, #11192, #16215 ) ;
#14447=CARTESIAN_POINT ( 'NONE',  ( 32.50000000000002132, 71.00000000000001421, 3.500000000000000000 ) ) ;
#14448=CARTESIAN_POINT ( 'NONE',  ( -28.87540678000427619, 6.494748934539263274, 13.19999999999999929 ) ) ;
#14451=EDGE_CURVE ( 'NONE', #16854, #1657, #17206, .T. ) ;
#14453=CARTESIAN_POINT ( 'NONE',  ( 28.87540678000427619, -6.494748934539263274, 13.19999999999999929 ) ) ;
#14455=EDGE_CURVE ( 'NONE', #5434, #3729, #5547, .T. ) ;
#14456=DIRECTION ( 'NONE',  ( 1.000000000000000000, 3.587913079599239526E-15, 0.000000000000000000 ) ) ;
#14458=CIRCLE ( 'NONE', #16242, 0.5000000000000004441 ) ;
#14459=ORIENTED_EDGE ( 'NONE', *, *, #11958, .F. ) ;
#14461=ORIENTED_EDGE ( 'NONE', *, *, #15226, .T. ) ;
#14463=CARTESIAN_POINT ( 'NONE',  ( -28.57540678000427548, -63.74634676501045050, 13.19999999999999929 ) ) ;
#14465=CARTESIAN_POINT ( 'NONE',  ( -17.95292532278785913, 50.11873716947361856, 13.99999999999999822 ) ) ;
#14469=CARTESIAN_POINT ( 'NONE',  ( -25.37540678000427263, 63.74634676501045050, 7.200000000000000178 ) ) ;
#14471=AXIS2_PLACEMENT_3D ( 'NONE', #15158, #11800, #5548 ) ;
#14474=CARTESIAN_POINT ( 'NONE',  ( 0.000000000000000000, 32.11873716947361856, 109.6002446535588319 ) ) ;
#14476=ORIENTED_EDGE ( 'NONE', *, *, #20274, .F. ) ;
#14477=CARTESIAN_POINT ( 'NONE',  ( -29.37540678000427619, -6.000000000000000000, 3.799999999999999822 ) ) ;
#14480=CARTESIAN_POINT ( 'NONE',  ( -23.26721486835118569, -3.307416615798745685, 13.50000000000000355 ) ) ;
#14483=ORIENTED_EDGE ( 'NONE', *, *, #9475, .F. ) ;
#14485=FACE_OUTER_BOUND ( 'NONE', #7818, .T. ) ;
#14486=EDGE_CURVE ( 'NONE', #4912, #3263, #15705, .T. ) ;
#14490=AXIS2_PLACEMENT_3D ( 'NONE', #3496, #10332, #5952 ) ;
#14492=CARTESIAN_POINT ( 'NONE',  ( -29.13662752439705272, -5.299999999999999822, 7.200000000000000178 ) ) ;
#14493=CARTESIAN_POINT ( 'NONE',  ( 15.95292532278785913, -51.61873716947361856, 14.00000000000000000 ) ) ;
#14495=AXIS2_PLACEMENT_3D ( 'NONE', #6181, #6071, #13077 ) ;
#14496=ORIENTED_EDGE ( 'NONE', *, *, #2404, .T. ) ;
#14497=AXIS2_PLACEMENT_3D ( 'NONE', #13013, #11132, #2630 ) ;
#14500=ORIENTED_EDGE ( 'NONE', *, *, #21645, .F. ) ;
#14501=FACE_OUTER_BOUND ( 'NONE', #18836, .T. ) ;
#14502=EDGE_CURVE ( 'NONE', #14785, #10729, #3978, .T. ) ;
#14503=AXIS2_PLACEMENT_3D ( 'NONE', #2971, #16721, #1066 ) ;
#14505=DIRECTION ( 'NONE',  ( 1.000000000000000000, 0.000000000000000000, 0.000000000000000000 ) ) ;
#14506=AXIS2_PLACEMENT_3D ( 'NONE', #1117, #4047, #2355 ) ;
#14507=CARTESIAN_POINT ( 'NONE',  ( 29.09616841400578124, 6.500357067309672665, 7.499999999999999112 ) ) ;
#14509=DIRECTION ( 'NONE',  ( 0.000000000000000000, 0.000000000000000000, 1.000000000000000000 ) ) ;
#14511=LINE ( 'NONE', #19913, #10206 ) ;
#14512=AXIS2_PLACEMENT_3D ( 'NONE', #7974, #2931, #14335 ) ;
#14513=EDGE_CURVE ( 'NONE', #21455, #8790, #21209, .T. ) ;
#14516=DIRECTION ( 'NONE',  ( -1.000000000000000000, 0.000000000000000000, 0.000000000000000000 ) ) ;
#14518=VERTEX_POINT ( 'NONE', #10690 ) ;
#14519=VECTOR ( 'NONE', #4981, 1000.000000000000000 ) ;
#14521=CIRCLE ( 'NONE', #18463, 0.5000000000000004441 ) ;
#14522=ORIENTED_EDGE ( 'NONE', *, *, #13703, .T. ) ;
#14523=DIRECTION ( 'NONE',  ( 0.000000000000000000, 0.000000000000000000, 1.000000000000000000 ) ) ;
#14525=EDGE_LOOP ( 'NONE', ( #11480, #19795, #16383, #17528 ) ) ;
#14526=ORIENTED_EDGE ( 'NONE', *, *, #10081, .F. ) ;
#14527=AXIS2_PLACEMENT_3D ( 'NONE', #11915, #3321, #17076 ) ;
#14532=ORIENTED_EDGE ( 'NONE', *, *, #15959, .T. ) ;
#14534=CARTESIAN_POINT ( 'NONE',  ( 28.57540678000427548, 63.74634676501045050, 13.50000000000000000 ) ) ;
#14535=LINE ( 'NONE', #9518, #20233 ) ;
#14539=DIRECTION ( 'NONE',  ( 1.000000000000000000, 0.000000000000000000, 0.000000000000000000 ) ) ;
#14546=DIRECTION ( 'NONE',  ( -0.000000000000000000, -1.000000000000000000, -0.000000000000000000 ) ) ;
#14547=AXIS2_PLACEMENT_3D ( 'NONE', #9114, #12458, #19085 ) ;
#14551=CYLINDRICAL_SURFACE ( 'NONE', #2737, 5.000000000000000888 ) ;
#14552=DIRECTION ( 'NONE',  ( 0.000000000000000000, 0.000000000000000000, -1.000000000000000000 ) ) ;
#14553=ORIENTED_EDGE ( 'NONE', *, *, #1756, .F. ) ;
#14555=DIRECTION ( 'NONE',  ( 0.000000000000000000, 1.000000000000000000, 0.000000000000000000 ) ) ;
#14556=CARTESIAN_POINT ( 'NONE',  ( 15.95292532278785913, -32.11873716947361856, 68.50000000000000000 ) ) ;
#14558=AXIS2_PLACEMENT_3D ( 'NONE', #20223, #11711, #14839 ) ;
#14562=ADVANCED_FACE ( 'NONE', ( #7332 ), #1467, .F. ) ;
#14566=APPLICATION_CONTEXT ( 'automotive_design' ) ;
#14567=CARTESIAN_POINT ( 'NONE',  ( -17.93704824106378837, -38.74634676501045760, 13.87500000000000000 ) ) ;
#14568=DIRECTION ( 'NONE',  ( -0.000000000000000000, -0.000000000000000000, -1.000000000000000000 ) ) ;
#14570=CARTESIAN_POINT ( 'NONE',  ( 18.22752199202934520, -39.04634676501046187, 13.50000000000000000 ) ) ;
#14571=DIRECTION ( 'NONE',  ( 1.000000000000000000, 0.000000000000000000, 0.000000000000000000 ) ) ;
#14573=CARTESIAN_POINT ( 'NONE',  ( -17.45292532278785913, 50.11873716947361856, 14.00000000000000000 ) ) ;
#14574=DIRECTION ( 'NONE',  ( 0.000000000000000000, 0.000000000000000000, 1.000000000000000000 ) ) ;
#14575=VECTOR ( 'NONE', #19647, 1000.000000000000000 ) ;
#14576=CARTESIAN_POINT ( 'NONE',  ( -23.02398829872514341, 3.262290859344318950, 13.79999999999999893 ) ) ;
#14578=EDGE_LOOP ( 'NONE', ( #8334, #21558, #17014, #16316, #459, #9230, #15375, #17504, #9148, #10249, #16196, #10983, #15443, #15129, #20576, #5836, #7719, #6166, #11835, #3334, #10828, #3875, #19260, #9260, #1617, #19306, #12558, #16648, #3044, #18486, #21848, #18366, #12077, #883, #18427, #2067, #15771, #19987, #7524, #1244, #3933, #1995, #4753, #11007, #20808, #1984, #14101, #14717, #11545, #1613, #2578, #2735, #3374, #6890, #13660, #10403, #19339, #17337, #19100, #19244, #21057, #102, #1880, #18399 ) ) ;
#14582=ORIENTED_EDGE ( 'NONE', *, *, #6505, .T. ) ;
#14583=ORIENTED_EDGE ( 'NONE', *, *, #3254, .F. ) ;
#14584=AXIS2_PLACEMENT_3D ( 'NONE', #5839, #2463, #21268 ) ;
#14586=FACE_OUTER_BOUND ( 'NONE', #20329, .T. ) ;
#14588=CARTESIAN_POINT ( 'NONE',  ( 17.92752199202934094, 38.74634676501045760, 13.79999999999999893 ) ) ;
#14589=ORIENTED_EDGE ( 'NONE', *, *, #9818, .T. ) ;
#14591=ORIENTED_EDGE ( 'NONE', *, *, #2365, .T. ) ;
#14592=DIRECTION ( 'NONE',  ( -0.000000000000000000, 0.000000000000000000, 1.000000000000000000 ) ) ;
#14596=DIRECTION ( 'NONE',  ( -1.000000000000000000, 0.000000000000000000, 0.000000000000000000 ) ) ;
#14599=CARTESIAN_POINT ( 'NONE',  ( -30.37540678000427619, -6.000000000000000000, 3.799999999999999822 ) ) ;
#14600=DIRECTION ( 'NONE',  ( 0.000000000000000000, 0.000000000000000000, -1.000000000000000000 ) ) ;
#14602=CYLINDRICAL_SURFACE ( 'NONE', #10600, 0.5000000000000004441 ) ;
#14603=CIRCLE ( 'NONE', #977, 1.974596669241483804 ) ;
#14604=DIRECTION ( 'NONE',  ( 0.000000000000000000, 0.000000000000000000, -1.000000000000000000 ) ) ;
#14607=EDGE_LOOP ( 'NONE', ( #22022, #2441, #15193, #6686 ) ) ;
#14608=CARTESIAN_POINT ( 'NONE',  ( 15.95292532278785913, -32.61873716947361856, 68.50000000000000000 ) ) ;
#14610=EDGE_CURVE ( 'NONE', #8484, #13135, #21763, .T. ) ;
#14614=ORIENTED_EDGE ( 'NONE', *, *, #7176, .F. ) ;
#14615=EDGE_LOOP ( 'NONE', ( #2575, #2561, #16139, #16912 ) ) ;
#14617=DIRECTION ( 'NONE',  ( 0.000000000000000000, -1.000000000000000000, 0.000000000000000000 ) ) ;
#14618=FACE_OUTER_BOUND ( 'NONE', #20214, .T. ) ;
#14619=VECTOR ( 'NONE', #18574, 1000.000000000000000 ) ;
#14620=ORIENTED_EDGE ( 'NONE', *, *, #8966, .F. ) ;
#14624=DIRECTION ( 'NONE',  ( 0.000000000000000000, 0.000000000000000000, -1.000000000000000000 ) ) ;
#14625=CARTESIAN_POINT ( 'NONE',  ( -23.04273166366764514, -2.261511273150494716, 13.23427437508502358 ) ) ;
#14626=ADVANCED_FACE ( 'NONE', ( #1373 ), #13120, .T. ) ;
#14628=FACE_OUTER_BOUND ( 'NONE', #516, .T. ) ;
#14629=PLANE ( 'NONE',  #21536 ) ;
#14630=CARTESIAN_POINT ( 'NONE',  ( -14.66174975910705136, 51.76873716947361714, 13.50000000000000000 ) ) ;
#14631=AXIS2_PLACEMENT_3D ( 'NONE', #15559, #14001, #15680 ) ;
#14633=DIRECTION ( 'NONE',  ( -0.000000000000000000, -0.000000000000000000, -1.000000000000000000 ) ) ;
#14634=ORIENTED_EDGE ( 'NONE', *, *, #13185, .F. ) ;
#14637=FACE_OUTER_BOUND ( 'NONE', #4776, .T. ) ;
#14638=CARTESIAN_POINT ( 'NONE',  ( -29.13662752439705272, 0.000000000000000000, 3.799999999999999822 ) ) ;
#14642=EDGE_LOOP ( 'NONE', ( #19574, #8763, #19093, #4829 ) ) ;
#14644=TOROIDAL_SURFACE ( 'NONE', #10734, 4.700000000000004619, 0.2999999999999999889 ) ;
#14646=CIRCLE ( 'NONE', #10393, 2.500000000000002220 ) ;
#14647=ORIENTED_EDGE ( 'NONE', *, *, #6545, .T. ) ;
#14650=ORIENTED_EDGE ( 'NONE', *, *, #21017, .T. ) ;
#14652=CARTESIAN_POINT ( 'NONE',  ( 8.641460742840918030, 32.93424481021354921, 68.00000000000000000 ) ) ;
#14653=LINE ( 'NONE', #21511, #17358 ) ;
#14655=CARTESIAN_POINT ( 'NONE',  ( -14.66174975910705136, 0.000000000000000000, 13.50000000000000000 ) ) ;
#14656=DIRECTION ( 'NONE',  ( 1.000000000000000000, -0.000000000000000000, -0.000000000000000000 ) ) ;
#14657=TOROIDAL_SURFACE ( 'NONE', #5038, 2.299999999999993161, 0.2999999999999999889 ) ;
#14661=DIRECTION ( 'NONE',  ( 0.000000000000000000, 0.000000000000000000, -1.000000000000000000 ) ) ;
#14664=CARTESIAN_POINT ( 'NONE',  ( -25.37540678000427263, -63.74634676501045050, 13.50000000000000000 ) ) ;
#14665=CARTESIAN_POINT ( 'NONE',  ( -17.45292532278785913, 39.04634676501046187, 13.50000000000000000 ) ) ;
#14666=EDGE_LOOP ( 'NONE', ( #4369, #6443, #5138, #19745 ) ) ;
#14667=VERTEX_POINT ( 'NONE', #6554 ) ;
#14668=CARTESIAN_POINT ( 'NONE',  ( 31.50000000000002132, -71.70000000000001705, 3.200000000000000178 ) ) ;
#14672=CARTESIAN_POINT ( 'NONE',  ( -3.627054932750481964, 33.43424481021354921, 42.50000000000000000 ) ) ;
#14673=ORIENTED_EDGE ( 'NONE', *, *, #8738, .T. ) ;
#14676=AXIS2_PLACEMENT_3D ( 'NONE', #79, #5353, #13381 ) ;
#14677=EDGE_CURVE ( 'NONE', #5889, #16679, #6321, .T. ) ;
#14679=CARTESIAN_POINT ( 'NONE',  ( 15.16923466928735742, -52.00603548408893317, 13.50000000000000000 ) ) ;
#14680=DIRECTION ( 'NONE',  ( 0.000000000000000000, 0.000000000000000000, 1.000000000000000000 ) ) ;
#14684=DIRECTION ( 'NONE',  ( 1.000000000000000000, 3.052134192567374827E-16, 0.000000000000000000 ) ) ;
#14685=VECTOR ( 'NONE', #12128, 1000.000000000000000 ) ;
#14687=( BOUNDED_SURFACE ( )  B_SPLINE_SURFACE ( 3, 2, ( 
 ( #11159, #2655, #21810 ),
 ( #971, #14739, #14625 ),
 ( #13174, #12939, #4682 ),
 ( #9722, #11386, #19787 ),
 ( #4447, #21590, #4566 ),
 ( #14961, #2995, #18212 ),
 ( #16524, #2895, #16625 ),
 ( #1300, #6487, #4787 ),
 ( #3558, #5238, #12032 ),
 ( #22149, #4897, #18883 ),
 ( #20224, #22023, #8805 ),
 ( #11712, #1762, #11926 ) ),
 .UNSPECIFIED., .F., .F., .F. ) 
 B_SPLINE_SURFACE_WITH_KNOTS ( ( 4, 2, 2, 2, 2, 4 ),
 ( 3, 3 ),
 ( 0.0007953085288493463639, 0.0009951922240469452709, 0.001195075919244544069, 0.001594843309639741667, 0.001994610700034939264, 0.002394378090430136861 ),
 ( 0.000000000000000000, 1.000000000000000000 ),
 .UNSPECIFIED. ) 
 GEOMETRIC_REPRESENTATION_ITEM ( )  RATIONAL_B_SPLINE_SURFACE ( (
 ( 1.000000000000000000, 0.9842566880020464648, 1.000000000000000000),
 ( 1.000000000000000000, 0.9842682545141110406, 1.000000000000000000),
 ( 1.000000000000000000, 0.9790935905989442967, 1.000000000000000000),
 ( 1.000000000000000000, 0.9652215946044103712, 1.000000000000000000),
 ( 1.000000000000000000, 0.9566241109334496784, 1.000000000000000000),
 ( 1.000000000000000000, 0.9283687200450407850, 1.000000000000000000),
 ( 1.000000000000000000, 0.9065874062052604598, 1.000000000000000000),
 ( 1.000000000000000000, 0.8577429740253560420, 1.000000000000000000),
 ( 1.000000000000000000, 0.8312249658972131749, 1.000000000000000000),
 ( 1.000000000000000000, 0.7732701221514807211, 1.000000000000000000),
 ( 1.000000000000000000, 0.7418345472257018569, 1.000000000000000000),
 ( 1.000000000000000000, 0.7071067811865475727, 1.000000000000000000) ) ) 
 REPRESENTATION_ITEM ( '' )  SURFACE ( )  );
#14689=EDGE_CURVE ( 'NONE', #8961, #12734, #3658, .T. ) ;
#14690=EDGE_LOOP ( 'NONE', ( #484, #13555, #20394 ) ) ;
#14692=CARTESIAN_POINT ( 'NONE',  ( -30.37540678000427619, 0.000000000000000000, 7.200000000000000178 ) ) ;
#14694=ORIENTED_EDGE ( 'NONE', *, *, #13925, .F. ) ;
#14697=CARTESIAN_POINT ( 'NONE',  ( 31.50000000000002132, 72.00000000000001421, 3.200000000000000178 ) ) ;
#14699=AXIS2_PLACEMENT_3D ( 'NONE', #12121, #18973, #261 ) ;
#14701=EDGE_CURVE ( 'NONE', #11864, #21336, #4638, .T. ) ;
#14703=CIRCLE ( 'NONE', #13641, 4.699999999999999289 ) ;
#14705=ORIENTED_EDGE ( 'NONE', *, *, #11112, .T. ) ;
#14707=DIRECTION ( 'NONE',  ( 0.000000000000000000, 0.000000000000000000, 1.000000000000000000 ) ) ;
#14708=EDGE_CURVE ( 'NONE', #7686, #1621, #13341, .T. ) ;
#14709=DIRECTION ( 'NONE',  ( 1.000000000000000000, 0.000000000000000000, 0.000000000000000000 ) ) ;
#14710=DIRECTION ( 'NONE',  ( 0.000000000000000000, 0.000000000000000000, 1.000000000000000000 ) ) ;
#14713=CARTESIAN_POINT ( 'NONE',  ( 15.95292532278785913, -34.11873716947361856, 68.00000000000000000 ) ) ;
#14714=CARTESIAN_POINT ( 'NONE',  ( 26.61833302554978786, -9.663695060508651125, 13.79999999999999893 ) ) ;
#14716=LINE ( 'NONE', #2873, #20827 ) ;
#14717=ORIENTED_EDGE ( 'NONE', *, *, #1509, .T. ) ;
#14718=CARTESIAN_POINT ( 'NONE',  ( -15.21174975910705207, -52.11873716947361856, 14.00000000000000000 ) ) ;
#14721=ADVANCED_FACE ( 'NONE', ( #21545 ), #18642, .T. ) ;
#14722=ORIENTED_EDGE ( 'NONE', *, *, #17306, .F. ) ;
#14725=EDGE_CURVE ( 'NONE', #20218, #11552, #4512, .T. ) ;
#14729=CARTESIAN_POINT ( 'NONE',  ( -15.95292532278785913, 52.11873716947361856, 13.99999999999999822 ) ) ;
#14733=ORIENTED_EDGE ( 'NONE', *, *, #10731, .T. ) ;
#14737=AXIS2_PLACEMENT_3D ( 'NONE', #8843, #17326, #14080 ) ;
#14739=CARTESIAN_POINT ( 'NONE',  ( -23.02398829872489827, -2.211005466174399636, 13.25091654438544531 ) ) ;
#14740=CIRCLE ( 'NONE', #9381, 0.2999999999999999334 ) ;
#14743=LINE ( 'NONE', #12943, #12927 ) ;
#14744=VERTEX_POINT ( 'NONE', #18277 ) ;
#14746=CARTESIAN_POINT ( 'NONE',  ( 9.641460742840918030, 32.11873716947361856, 68.50000000000000000 ) ) ;
#14747=CARTESIAN_POINT ( 'NONE',  ( -8.641460742840918030, 33.43424481021354921, 42.50000000000000000 ) ) ;
#14748=ORIENTED_EDGE ( 'NONE', *, *, #345, .T. ) ;
#14750=CARTESIAN_POINT ( 'NONE',  ( -3.127054932750481964, 32.11873716947361856, 68.50000000000000000 ) ) ;
#14752=ORIENTED_EDGE ( 'NONE', *, *, #19222, .T. ) ;
#14756=ORIENTED_EDGE ( 'NONE', *, *, #12284, .T. ) ;
#14759=VERTEX_POINT ( 'NONE', #6773 ) ;
#14760=CARTESIAN_POINT ( 'NONE',  ( 25.37540678000427263, -66.94634676501046044, 13.50000000000000000 ) ) ;
#14769=LINE ( 'NONE', #13206, #6844 ) ;
#14771=CARTESIAN_POINT ( 'NONE',  ( 29.13662752439705272, 0.000000000000000000, 13.50000000000000000 ) ) ;
#14772=CARTESIAN_POINT ( 'NONE',  ( 25.37540678000429395, -38.74634676501045760, 42.50000000000000000 ) ) ;
#14774=ORIENTED_EDGE ( 'NONE', *, *, #7022, .T. ) ;
#14777=ADVANCED_FACE ( 'NONE', ( #13573 ), #20094, .T. ) ;
#14780=EDGE_LOOP ( 'NONE', ( #9874, #9797, #13244, #12350 ) ) ;
#14785=VERTEX_POINT ( 'NONE', #5080 ) ;
#14787=CARTESIAN_POINT ( 'NONE',  ( -14.90262739788949098, -52.32122552996407450, 13.50000000000000000 ) ) ;
#14788=AXIS2_PLACEMENT_3D ( 'NONE', #4715, #6740, #16783 ) ;
#14789=EDGE_LOOP ( 'NONE', ( #20439, #21423, #12564, #8174 ) ) ;
#14790=CYLINDRICAL_SURFACE ( 'NONE', #1998, 0.2999999999999999334 ) ;
#14791=AXIS2_PLACEMENT_3D ( 'NONE', #19654, #4326, #17964 ) ;
#14792=ORIENTED_EDGE ( 'NONE', *, *, #4443, .T. ) ;
#14793=DIRECTION ( 'NONE',  ( -0.000000000000000000, -0.000000000000000000, -1.000000000000000000 ) ) ;
#14794=SPHERICAL_SURFACE ( 'NONE', #18640, 0.5000000000000000000 ) ;
#14795=DIRECTION ( 'NONE',  ( 1.000000000000000000, 0.000000000000000000, 0.000000000000000000 ) ) ;
#14796=ADVANCED_FACE ( 'NONE', ( #5417 ), #19009, .F. ) ;
#14797=ORIENTED_EDGE ( 'NONE', *, *, #17052, .T. ) ;
#14800=ORIENTED_EDGE ( 'NONE', *, *, #19738, .T. ) ;
#14801=VERTEX_POINT ( 'NONE', #13891 ) ;
#14802=CARTESIAN_POINT ( 'NONE',  ( 15.21174975910705918, 52.10286008774954780, 13.87500000000000000 ) ) ;
#14803=DIRECTION ( 'NONE',  ( 1.000000000000000000, 0.000000000000000000, 0.000000000000000000 ) ) ;
#14804=ORIENTED_EDGE ( 'NONE', *, *, #12703, .T. ) ;
#14807=ORIENTED_EDGE ( 'NONE', *, *, #19646, .F. ) ;
#14808=CARTESIAN_POINT ( 'NONE',  ( 29.37540678000427619, -6.000000000000000000, 3.799999999999999822 ) ) ;
#14809=CARTESIAN_POINT ( 'NONE',  ( 15.95292532278785913, 34.11873716947361856, 68.50000000000000000 ) ) ;
#14810=ADVANCED_FACE ( 'NONE', ( #10342 ), #15469, .F. ) ;
#14811=CARTESIAN_POINT ( 'NONE',  ( -28.57540678000427548, 63.74634676501045050, 13.50000000000000000 ) ) ;
#14812=DIRECTION ( 'NONE',  ( 0.000000000000000000, 0.000000000000000000, -1.000000000000000000 ) ) ;
#14813=EDGE_LOOP ( 'NONE', ( #8223, #6496, #6589, #8463, #5286, #14004 ) ) ;
#14814=CYLINDRICAL_SURFACE ( 'NONE', #15944, 0.5000000000000004441 ) ;
#14828=ORIENTED_EDGE ( 'NONE', *, *, #18754, .T. ) ;
#14830=DIRECTION ( 'NONE',  ( -1.000000000000000000, 0.000000000000000000, 0.000000000000000000 ) ) ;
#14831=EDGE_CURVE ( 'NONE', #7888, #2103, #18493, .T. ) ;
#14833=ORIENTED_EDGE ( 'NONE', *, *, #12229, .F. ) ;
#14835=LINE ( 'NONE', #21693, #18979 ) ;
#14837=AXIS2_PLACEMENT_3D ( 'NONE', #3768, #10915, #11030 ) ;
#14839=DIRECTION ( 'NONE',  ( 0.000000000000000000, 0.000000000000000000, -1.000000000000000000 ) ) ;
#14840=LINE ( 'NONE', #11491, #16327 ) ;
#14843=CARTESIAN_POINT ( 'NONE',  ( -18.22752199202934520, 50.11873716947361856, 13.50000000000000000 ) ) ;
#14844=DIRECTION ( 'NONE',  ( -0.000000000000000000, -0.000000000000000000, -1.000000000000000000 ) ) ;
#14845=DIRECTION ( 'NONE',  ( 1.000000000000000000, 0.000000000000000000, 0.000000000000000000 ) ) ;
#14846=DIRECTION ( 'NONE',  ( -0.000000000000000000, 1.000000000000000000, -0.000000000000000000 ) ) ;
#14847=VERTEX_POINT ( 'NONE', #5187 ) ;
#14850=ADVANCED_FACE ( 'NONE', ( #15562 ), #11989, .T. ) ;
#14855=CYLINDRICAL_SURFACE ( 'NONE', #9972, 2.000000000000001776 ) ;
#14858=VERTEX_POINT ( 'NONE', #1485 ) ;
#14860=CARTESIAN_POINT ( 'NONE',  ( 29.50000000000002132, -2.473451120191013430, 0.2999999999999947153 ) ) ;
#14862=ORIENTED_EDGE ( 'NONE', *, *, #10767, .F. ) ;
#14865=CARTESIAN_POINT ( 'NONE',  ( 27.61238352468048518, -2.348761424523157615, 0.000000000000000000 ) ) ;
#14867=VECTOR ( 'NONE', #11529, 1000.000000000000000 ) ;
#14869=EDGE_CURVE ( 'NONE', #14314, #1350, #14703, .T. ) ;
#14870=CARTESIAN_POINT ( 'NONE',  ( 15.95292532278785913, -50.11873716947361856, 68.00000000000000000 ) ) ;
#14871=CARTESIAN_POINT ( 'NONE',  ( 23.02398829872513986, 3.419159475692122196, 13.52813170334708914 ) ) ;
#14872=EDGE_CURVE ( 'NONE', #19359, #2691, #17037, .T. ) ;
#14875=DIRECTION ( 'NONE',  ( 0.000000000000000000, -0.000000000000000000, 1.000000000000000000 ) ) ;
#14877=AXIS2_PLACEMENT_3D ( 'NONE', #2190, #3996, #2519 ) ;
#14879=AXIS2_PLACEMENT_3D ( 'NONE', #8573, #20650, #5206 ) ;
#14881=AXIS2_PLACEMENT_3D ( 'NONE', #17273, #5546, #3867 ) ;
#14882=EDGE_CURVE ( 'NONE', #12488, #17779, #10078, .T. ) ;
#14883=FACE_OUTER_BOUND ( 'NONE', #16409, .T. ) ;
#14885=DIRECTION ( 'NONE',  ( 0.000000000000000000, 0.000000000000000000, 1.000000000000000000 ) ) ;
#14886=LINE ( 'NONE', #7750, #18135 ) ;
#14887=ORIENTED_EDGE ( 'NONE', *, *, #2653, .F. ) ;
#14890=CARTESIAN_POINT ( 'NONE',  ( 29.50000000000002132, 0.000000000000000000, 0.2999999999999947153 ) ) ;
#14892=VERTEX_POINT ( 'NONE', #13772 ) ;
#14894=ORIENTED_EDGE ( 'NONE', *, *, #16528, .T. ) ;
#14896=AXIS2_PLACEMENT_3D ( 'NONE', #10071, #20367, #3458 ) ;
#14900=DIRECTION ( 'NONE',  ( -0.000000000000000000, -0.000000000000000000, 1.000000000000000000 ) ) ;
#14903=DIRECTION ( 'NONE',  ( 1.000000000000000000, 0.000000000000000000, 0.000000000000000000 ) ) ;
#14905=CARTESIAN_POINT ( 'NONE',  ( 0.000000000000000000, 68.44634676501046044, 7.200000000000000178 ) ) ;
#14907=FACE_OUTER_BOUND ( 'NONE', #2646, .T. ) ;
#14910=EDGE_LOOP ( 'NONE', ( #15166, #4511, #1541, #16644 ) ) ;
#14915=FACE_OUTER_BOUND ( 'NONE', #18431, .T. ) ;
#14916=DIRECTION ( 'NONE',  ( -0.000000000000000000, 1.000000000000000000, 0.000000000000000000 ) ) ;
#14919=EDGE_CURVE ( 'NONE', #22137, #1525, #8269, .T. ) ;
#14921=AXIS2_PLACEMENT_3D ( 'NONE', #8110, #929, #3061 ) ;
#14923=VERTEX_POINT ( 'NONE', #3956 ) ;
#14926=EDGE_CURVE ( 'NONE', #5550, #8429, #16850, .T. ) ;
#14931=CARTESIAN_POINT ( 'NONE',  ( -25.37540678000427263, -63.74634676501045050, 3.799999999999999822 ) ) ;
#14934=DIRECTION ( 'NONE',  ( 0.000000000000000000, 0.000000000000000000, 1.000000000000000000 ) ) ;
#14935=AXIS2_PLACEMENT_3D ( 'NONE', #19563, #12830, #12606 ) ;
#14936=DIRECTION ( 'NONE',  ( 1.000000000000000000, 0.000000000000000000, 0.000000000000000000 ) ) ;
#14940=CIRCLE ( 'NONE', #20666, 1.000000000000000888 ) ;
#14942=CIRCLE ( 'NONE', #9591, 0.5000000000000004441 ) ;
#14944=CYLINDRICAL_SURFACE ( 'NONE', #11257, 0.5000000000000004441 ) ;
#14945=DIRECTION ( 'NONE',  ( 0.000000000000000000, 1.000000000000000000, 0.000000000000000000 ) ) ;
#14951=DIRECTION ( 'NONE',  ( -0.000000000000000000, -0.000000000000000000, -1.000000000000000000 ) ) ;
#14955=ORIENTED_EDGE ( 'NONE', *, *, #21073, .F. ) ;
#14956=DIRECTION ( 'NONE',  ( 0.000000000000000000, 1.000000000000000000, 0.000000000000000000 ) ) ;
#14958=EDGE_CURVE ( 'NONE', #20211, #2381, #8876, .T. ) ;
#14961=CARTESIAN_POINT ( 'NONE',  ( -23.02398829872513986, -2.502127083158335541, 13.57904421648012949 ) ) ;
#14966=DIRECTION ( 'NONE',  ( -0.000000000000000000, -1.000000000000000000, 0.000000000000000000 ) ) ;
#14967=VECTOR ( 'NONE', #16833, 1000.000000000000000 ) ;
#14969=DIRECTION ( 'NONE',  ( 0.000000000000000000, -0.000000000000000000, -1.000000000000000000 ) ) ;
#14970=ORIENTED_EDGE ( 'NONE', *, *, #20359, .T. ) ;
#14972=DIRECTION ( 'NONE',  ( 0.000000000000000000, -0.000000000000000000, -1.000000000000000000 ) ) ;
#14973=EDGE_CURVE ( 'NONE', #5901, #1178, #12549, .T. ) ;
#14976=CARTESIAN_POINT ( 'NONE',  ( 29.13662752439705272, 0.000000000000000000, 7.500000000000000000 ) ) ;
#14977=VERTEX_POINT ( 'NONE', #10180 ) ;
#14978=DIRECTION ( 'NONE',  ( 1.000000000000000000, 0.000000000000000000, 0.000000000000000000 ) ) ;
#14981=CARTESIAN_POINT ( 'NONE',  ( -9.641460742840918030, 32.11873716947361856, 109.6002446535588319 ) ) ;
#14982=VERTEX_POINT ( 'NONE', #15198 ) ;
#14984=DIRECTION ( 'NONE',  ( 1.000000000000000000, 0.000000000000000000, 0.000000000000000000 ) ) ;
#14987=DIRECTION ( 'NONE',  ( 1.000000000000000000, 0.000000000000000000, -0.000000000000000000 ) ) ;
#14989=ORIENTED_EDGE ( 'NONE', *, *, #17216, .F. ) ;
#14994=LINE ( 'NONE', #10179, #19860 ) ;
#14995=ADVANCED_FACE ( 'NONE', ( #16992 ), #15435, .F. ) ;
#14998=DIRECTION ( 'NONE',  ( 0.000000000000000000, -1.000000000000000000, 0.000000000000000000 ) ) ;
#14999=DIRECTION ( 'NONE',  ( -1.000000000000000000, -0.000000000000000000, 2.388292521039847891E-16 ) ) ;
#15000=DIRECTION ( 'NONE',  ( -0.000000000000000000, -0.000000000000000000, 1.000000000000000000 ) ) ;
#15001=CARTESIAN_POINT ( 'NONE',  ( -14.66895121610833463, -51.92349730072803027, 13.50000000000000000 ) ) ;
#15006=ORIENTED_EDGE ( 'NONE', *, *, #17986, .T. ) ;
#15007=DIRECTION ( 'NONE',  ( -1.000000000000000000, 0.000000000000000000, 0.000000000000000000 ) ) ;
#15009=AXIS2_PLACEMENT_3D ( 'NONE', #6436, #18268, #11326 ) ;
#15012=EDGE_LOOP ( 'NONE', ( #13219, #690, #9254, #5082 ) ) ;
#15013=DIRECTION ( 'NONE',  ( 1.000000000000000000, 0.000000000000000000, 0.000000000000000000 ) ) ;
#15017=ORIENTED_EDGE ( 'NONE', *, *, #446, .T. ) ;
#15020=ADVANCED_FACE ( 'NONE', ( #3589 ), #18288, .T. ) ;
#15022=CARTESIAN_POINT ( 'NONE',  ( 14.96174975910705918, -51.83053110199097091, 13.82013245744073160 ) ) ;
#15024=CARTESIAN_POINT ( 'NONE',  ( -3.127054932750481964, -32.93424481021354921, 68.50000000000000000 ) ) ;
#15025=ORIENTED_EDGE ( 'NONE', *, *, #250, .F. ) ;
#15028=DIRECTION ( 'NONE',  ( 1.000000000000000000, 0.000000000000000000, -0.000000000000000000 ) ) ;
#15030=ORIENTED_EDGE ( 'NONE', *, *, #14020, .T. ) ;
#15031=ORIENTED_EDGE ( 'NONE', *, *, #14486, .T. ) ;
#15033=LINE ( 'NONE', #40, #18134 ) ;
#15036=ADVANCED_FACE ( 'NONE', ( #17222 ), #5381, .T. ) ;
#15037=ORIENTED_EDGE ( 'NONE', *, *, #9076, .F. ) ;
#15039=ADVANCED_FACE ( 'NONE', ( #3468 ), #8837, .F. ) ;
#15041=ORIENTED_EDGE ( 'NONE', *, *, #1442, .F. ) ;
#15044=VECTOR ( 'NONE', #2059, 1000.000000000000000 ) ;
#15048=CARTESIAN_POINT ( 'NONE',  ( 14.66174975910705847, -51.76873716947361714, 13.79999999999999893 ) ) ;
#15049=VECTOR ( 'NONE', #16857, 1000.000000000000000 ) ;
#15051=FACE_OUTER_BOUND ( 'NONE', #5218, .T. ) ;
#15055=ORIENTED_EDGE ( 'NONE', *, *, #19813, .F. ) ;
#15056=FACE_OUTER_BOUND ( 'NONE', #12230, .T. ) ;
#15057=AXIS2_PLACEMENT_3D ( 'NONE', #17933, #915, #12775 ) ;
#15058=CYLINDRICAL_SURFACE ( 'NONE', #12022, 0.2999999999999999334 ) ;
#15059=ORIENTED_EDGE ( 'NONE', *, *, #8974, .F. ) ;
#15060=AXIS2_PLACEMENT_3D ( 'NONE', #11029, #16156, #4319 ) ;
#15062=ORIENTED_EDGE ( 'NONE', *, *, #2538, .F. ) ;
#15063=CARTESIAN_POINT ( 'NONE',  ( -26.61833302554978786, -9.663695060508651125, 13.79999999999999893 ) ) ;
#15064=ADVANCED_FACE ( 'NONE', ( #15642 ), #13642, .F. ) ;
#15066=CARTESIAN_POINT ( 'NONE',  ( -29.13662752439705272, 0.000000000000000000, 7.200000000000000178 ) ) ;
#15068=EDGE_LOOP ( 'NONE', ( #12438, #15685, #8027, #4645 ) ) ;
#15069=ORIENTED_EDGE ( 'NONE', *, *, #22143, .T. ) ;
#15070=ORIENTED_EDGE ( 'NONE', *, *, #9789, .T. ) ;
#15072=CARTESIAN_POINT ( 'NONE',  ( -14.96174975910705207, -32.10873716947361345, 13.05380965755523448 ) ) ;
#15076=LINE ( 'NONE', #21921, #1141 ) ;
#15077=DIRECTION ( 'NONE',  ( 1.000000000000000000, -0.000000000000000000, -0.000000000000000000 ) ) ;
#15078=VECTOR ( 'NONE', #4815, 1000.000000000000000 ) ;
#15079=AXIS2_PLACEMENT_3D ( 'NONE', #916, #17241, #15773 ) ;
#15081=CARTESIAN_POINT ( 'NONE',  ( 27.37540678000428684, -36.74634676501047181, 42.50000000000000000 ) ) ;
#15083=CYLINDRICAL_SURFACE ( 'NONE', #8057, 5.000000000000000888 ) ;
#15089=ORIENTED_EDGE ( 'NONE', *, *, #19365, .T. ) ;
#15090=FACE_OUTER_BOUND ( 'NONE', #5731, .T. ) ;
#15093=EDGE_LOOP ( 'NONE', ( #20390, #17235, #8460, #9963 ) ) ;
#15098=LINE ( 'NONE', #18454, #6741 ) ;
#15099=EDGE_CURVE ( 'NONE', #13059, #8047, #15784, .T. ) ;
#15102=CARTESIAN_POINT ( 'NONE',  ( -15.05373532783226054, -52.39333378048836920, 13.50000000000000000 ) ) ;
#15103=PLANE ( 'NONE',  #10189 ) ;
#15104=ADVANCED_FACE ( 'NONE', ( #14074 ), #15750, .T. ) ;
#15105=EDGE_CURVE ( 'NONE', #11974, #1458, #5091, .T. ) ;
#15106=DIRECTION ( 'NONE',  ( 0.000000000000000000, 0.000000000000000000, -1.000000000000000000 ) ) ;
#15108=LINE ( 'NONE', #13654, #18453 ) ;
#15109=EDGE_CURVE ( 'NONE', #10741, #15111, #4121, .T. ) ;
#15110=ORIENTED_EDGE ( 'NONE', *, *, #3341, .T. ) ;
#15111=VERTEX_POINT ( 'NONE', #12502 ) ;
#15112=CARTESIAN_POINT ( 'NONE',  ( -15.95292532278785913, 50.11873716947361856, 13.50000000000000000 ) ) ;
#15113=ADVANCED_FACE ( 'NONE', ( #17876 ), #21038, .T. ) ;
#15115=ORIENTED_EDGE ( 'NONE', *, *, #6661, .T. ) ;
#15116=SURFACE_STYLE_FILL_AREA ( #20504 ) ;
#15117=ORIENTED_EDGE ( 'NONE', *, *, #15522, .F. ) ;
#15118=EDGE_LOOP ( 'NONE', ( #20366, #16484, #14144, #11871 ) ) ;
#15122=DIRECTION ( 'NONE',  ( 0.000000000000000000, 0.000000000000000000, -1.000000000000000000 ) ) ;
#15124=DIRECTION ( 'NONE',  ( 1.000000000000000000, 0.000000000000000000, 0.000000000000000000 ) ) ;
#15126=DIRECTION ( 'NONE',  ( -0.000000000000000000, -0.000000000000000000, -1.000000000000000000 ) ) ;
#15128=CYLINDRICAL_SURFACE ( 'NONE', #5181, 3.500000000000003109 ) ;
#15129=ORIENTED_EDGE ( 'NONE', *, *, #18214, .T. ) ;
#15131=EDGE_CURVE ( 'NONE', #2930, #16763, #3297, .T. ) ;
#15132=VERTEX_POINT ( 'NONE', #755 ) ;
#15133=VERTEX_POINT ( 'NONE', #423 ) ;
#15136=ADVANCED_FACE ( 'NONE', ( #7607 ), #9053, .F. ) ;
#15137=DIRECTION ( 'NONE',  ( 0.000000000000000000, -0.000000000000000000, -1.000000000000000000 ) ) ;
#15140=CIRCLE ( 'NONE', #845, 0.3000000000000004885 ) ;
#15142=DIRECTION ( 'NONE',  ( 0.000000000000000000, 0.000000000000000000, -1.000000000000000000 ) ) ;
#15146=PLANE ( 'NONE',  #19505 ) ;
#15149=FACE_OUTER_BOUND ( 'NONE', #13917, .T. ) ;
#15150=EDGE_CURVE ( 'NONE', #4677, #10017, #12605, .T. ) ;
#15151=CARTESIAN_POINT ( 'NONE',  ( -8.641460742840918030, -33.93424481021354921, 68.00000000000000000 ) ) ;
#15153=CARTESIAN_POINT ( 'NONE',  ( 31.50000000000002132, -71.00000000000001421, 1.800000000000000044 ) ) ;
#15154=CARTESIAN_POINT ( 'NONE',  ( -15.95292532278785913, 32.11873716947361856, 109.6002446535588319 ) ) ;
#15155=ORIENTED_EDGE ( 'NONE', *, *, #12243, .T. ) ;
#15157=ORIENTED_EDGE ( 'NONE', *, *, #14701, .T. ) ;
#15158=CARTESIAN_POINT ( 'NONE',  ( -27.37540678000427974, -5.683640910026986681, 13.79999999999999893 ) ) ;
#15162=ORIENTED_EDGE ( 'NONE', *, *, #493, .F. ) ;
#15163=PLANE ( 'NONE',  #7058 ) ;
#15165=SPHERICAL_SURFACE ( 'NONE', #13216, 0.5000000000000000000 ) ;
#15166=ORIENTED_EDGE ( 'NONE', *, *, #15622, .T. ) ;
#15167=FACE_OUTER_BOUND ( 'NONE', #21007, .T. ) ;
#15170=DIRECTION ( 'NONE',  ( 1.000000000000000000, 0.000000000000000000, 0.000000000000000000 ) ) ;
#15179=CARTESIAN_POINT ( 'NONE',  ( -14.96174975910705207, -41.81054587065082728, 13.79999999999999893 ) ) ;
#15186=ORIENTED_EDGE ( 'NONE', *, *, #18918, .F. ) ;
#15189=AXIS2_PLACEMENT_3D ( 'NONE', #7230, #5342, #481 ) ;
#15191=AXIS2_PLACEMENT_3D ( 'NONE', #17745, #5902, #21234 ) ;
#15193=ORIENTED_EDGE ( 'NONE', *, *, #5319, .T. ) ;
#15194=EDGE_CURVE ( 'NONE', #21063, #19665, #9383, .T. ) ;
#15195=CARTESIAN_POINT ( 'NONE',  ( -15.21174975910705207, -51.61873716947361856, 68.00000000000000000 ) ) ;
#15197=CIRCLE ( 'NONE', #6278, 6.499999999999999112 ) ;
#15198=CARTESIAN_POINT ( 'NONE',  ( -14.96174975910705207, 41.81054587065082728, 68.25000000000000000 ) ) ;
#15199=EDGE_CURVE ( 'NONE', #14759, #17313, #15964, .T. ) ;
#15200=CARTESIAN_POINT ( 'NONE',  ( 25.37540678000429395, -38.74634676501045760, 13.79999999999999893 ) ) ;
#15202=DIRECTION ( 'NONE',  ( 0.000000000000000000, 0.000000000000000000, -1.000000000000000000 ) ) ;
#15204=AXIS2_PLACEMENT_3D ( 'NONE', #18630, #1510, #18301 ) ;
#15206=CARTESIAN_POINT ( 'NONE',  ( -14.96174975910705207, 51.61873716947361856, 68.25000000000000000 ) ) ;
#15209=CARTESIAN_POINT ( 'NONE',  ( 29.17540678000427690, 63.74634676501045050, 7.799999999999999822 ) ) ;
#15211=ORIENTED_EDGE ( 'NONE', *, *, #5661, .T. ) ;
#15213=AXIS2_PLACEMENT_3D ( 'NONE', #12250, #6708, #20463 ) ;
#15215=CARTESIAN_POINT ( 'NONE',  ( -25.37540678000427263, -67.24634676501045760, 13.50000000000000000 ) ) ;
#15223=VECTOR ( 'NONE', #14114, 1000.000000000000000 ) ;
#15226=EDGE_CURVE ( 'NONE', #16467, #20699, #9161, .T. ) ;
#15227=CARTESIAN_POINT ( 'NONE',  ( -30.67540678000428045, -63.74634676501045050, 3.799999999999999822 ) ) ;
#15228=CARTESIAN_POINT ( 'NONE',  ( -29.13662752439705272, 5.000000000000000000, 7.200000000000000178 ) ) ;
#15232=AXIS2_PLACEMENT_3D ( 'NONE', #18395, #13254, #16262 ) ;
#15233=CIRCLE ( 'NONE', #1660, 0.6999999999999992895 ) ;
#15234=LINE ( 'NONE', #11875, #21392 ) ;
#15239=CARTESIAN_POINT ( 'NONE',  ( -23.02398829872513986, 3.264233419183502072, 13.78834712654929717 ) ) ;
#15240=DIRECTION ( 'NONE',  ( 2.832483164223434527E-16, -1.000000000000000000, 0.000000000000000000 ) ) ;
#15241=CARTESIAN_POINT ( 'NONE',  ( 3.127054932750481964, 32.61873716947361856, 109.6002446535588319 ) ) ;
#15242=CIRCLE ( 'NONE', #19523, 4.351418481279137218 ) ;
#15245=ORIENTED_EDGE ( 'NONE', *, *, #9780, .F. ) ;
#15246=ORIENTED_EDGE ( 'NONE', *, *, #5403, .F. ) ;
#15248=CARTESIAN_POINT ( 'NONE',  ( 29.37540678000427619, 4.700000000000000178, 3.500000000000000000 ) ) ;
#15251=AXIS2_PLACEMENT_3D ( 'NONE', #2802, #21939, #3021 ) ;
#15257=FACE_OUTER_BOUND ( 'NONE', #20120, .T. ) ;
#15259=EDGE_CURVE ( 'NONE', #5867, #15111, #17926, .T. ) ;
#15260=DIRECTION ( 'NONE',  ( -0.000000000000000000, 0.000000000000000000, -1.000000000000000000 ) ) ;
#15261=EDGE_CURVE ( 'NONE', #11552, #1923, #13998, .T. ) ;
#15262=FACE_OUTER_BOUND ( 'NONE', #20068, .T. ) ;
#15263=ORIENTED_EDGE ( 'NONE', *, *, #12884, .F. ) ;
#15266=CARTESIAN_POINT ( 'NONE',  ( -15.95292532278785913, 52.09333383871509682, 13.79999999999999893 ) ) ;
#15267=DIRECTION ( 'NONE',  ( -0.000000000000000000, 1.000000000000000000, 0.000000000000000000 ) ) ;
#15269=ORIENTED_EDGE ( 'NONE', *, *, #5634, .T. ) ;
#15270=CIRCLE ( 'NONE', #9559, 0.5000000000000004441 ) ;
#15275=CARTESIAN_POINT ( 'NONE',  ( 32.20000000000001705, -71.00000000000001421, 3.200000000000000178 ) ) ;
#15278=AXIS2_PLACEMENT_3D ( 'NONE', #4194, #14034, #5555 ) ;
#15280=CARTESIAN_POINT ( 'NONE',  ( -24.13662752439704917, 0.000000000000000000, 3.799999999999999822 ) ) ;
#15283=CARTESIAN_POINT ( 'NONE',  ( -9.141460742840918030, -33.43424481021354921, 42.50000000000000000 ) ) ;
#15284=( BOUNDED_CURVE ( )  B_SPLINE_CURVE ( 3, ( #6118, #11229, #16253, #7790 ),
 .UNSPECIFIED., .F., .T. ) 
 B_SPLINE_CURVE_WITH_KNOTS ( ( 4, 4 ),
 ( 0.000000000000000000, 1.570796326794896558 ),
 .UNSPECIFIED. ) 
 CURVE ( )  GEOMETRIC_REPRESENTATION_ITEM ( )  RATIONAL_B_SPLINE_CURVE ( ( 1.000000000000000000, 0.8047378541243649375, 0.8047378541243649375, 1.000000000000000000 ) ) 
 REPRESENTATION_ITEM ( '' )  );
#15285=ORIENTED_EDGE ( 'NONE', *, *, #10134, .F. ) ;
#15286=DIRECTION ( 'NONE',  ( -0.000000000000000000, 0.000000000000000000, -1.000000000000000000 ) ) ;
#15289=VECTOR ( 'NONE', #3247, 1000.000000000000000 ) ;
#15290=DIRECTION ( 'NONE',  ( 1.000000000000000000, -0.000000000000000000, 0.000000000000000000 ) ) ;
#15291=CARTESIAN_POINT ( 'NONE',  ( -18.22752199202934520, -50.11873716947361856, 13.79999999999999893 ) ) ;
#15294=ORIENTED_EDGE ( 'NONE', *, *, #12758, .T. ) ;
#15295=DIRECTION ( 'NONE',  ( 0.000000000000000000, 0.000000000000000000, 1.000000000000000000 ) ) ;
#15297=AXIS2_PLACEMENT_3D ( 'NONE', #8186, #3469, #8511 ) ;
#15300=DIRECTION ( 'NONE',  ( 0.000000000000000000, 0.000000000000000000, -1.000000000000000000 ) ) ;
#15302=CARTESIAN_POINT ( 'NONE',  ( 23.02398829872513986, 3.053353875533147299, 13.54966661417621587 ) ) ;
#15304=EDGE_CURVE ( 'NONE', #15586, #19753, #18216, .T. ) ;
#15305=CARTESIAN_POINT ( 'NONE',  ( -28.87540678000427619, 63.74634676501045050, 13.19999999999999929 ) ) ;
#15307=DIRECTION ( 'NONE',  ( 0.000000000000000000, 0.000000000000000000, -1.000000000000000000 ) ) ;
#15308=CARTESIAN_POINT ( 'NONE',  ( 0.000000000000000000, 52.11873716947361856, 68.00000000000000000 ) ) ;
#15314=ORIENTED_EDGE ( 'NONE', *, *, #21424, .T. ) ;
#15316=DIRECTION ( 'NONE',  ( 0.000000000000000000, 0.000000000000000000, 1.000000000000000000 ) ) ;
#15318=VECTOR ( 'NONE', #9446, 1000.000000000000000 ) ;
#15319=VERTEX_POINT ( 'NONE', #14843 ) ;
#15321=ADVANCED_FACE ( 'NONE', ( #16527 ), #14629, .F. ) ;
#15327=DIRECTION ( 'NONE',  ( 1.000000000000000000, -2.832483164223420229E-16, 0.000000000000000000 ) ) ;
#15330=CARTESIAN_POINT ( 'NONE',  ( 29.20000000000002061, -68.70000000000001705, 0.000000000000000000 ) ) ;
#15331=AXIS2_PLACEMENT_3D ( 'NONE', #530, #5606, #20822 ) ;
#15333=CARTESIAN_POINT ( 'NONE',  ( -14.75141515765153954, -52.14252004795846318, 13.50000000000000000 ) ) ;
#15335=EDGE_CURVE ( 'NONE', #11905, #13059, #14743, .T. ) ;
#15336=ORIENTED_EDGE ( 'NONE', *, *, #9385, .T. ) ;
#15340=EDGE_LOOP ( 'NONE', ( #20065, #2259, #5648, #18136 ) ) ;
#15341=EDGE_LOOP ( 'NONE', ( #18264, #17863, #15525, #2155 ) ) ;
#15344=EDGE_LOOP ( 'NONE', ( #15110, #12431, #21906, #21965 ) ) ;
#15345=AXIS2_PLACEMENT_3D ( 'NONE', #20595, #15530, #20149 ) ;
#15348=CARTESIAN_POINT ( 'NONE',  ( 15.95292532278785913, 52.39333383871510108, 13.50000000000000000 ) ) ;
#15349=CARTESIAN_POINT ( 'NONE',  ( 30.07540678000427548, 0.000000000000000000, 7.500000000000000000 ) ) ;
#15351=DIRECTION ( 'NONE',  ( -0.000000000000000000, -0.000000000000000000, 1.000000000000000000 ) ) ;
#15353=ADVANCED_FACE ( 'NONE', ( #9726 ), #10807, .F. ) ;
#15354=AXIS2_PLACEMENT_3D ( 'NONE', #6490, #8263, #21920 ) ;
#15356=DIRECTION ( 'NONE',  ( -3.052134192567367925E-16, -1.000000000000000000, 0.000000000000000000 ) ) ;
#15357=VECTOR ( 'NONE', #16849, 1000.000000000000000 ) ;
#15358=CARTESIAN_POINT ( 'NONE',  ( 4.127054932750481520, -33.43424481021354921, 13.50000000000000000 ) ) ;
#15360=CARTESIAN_POINT ( 'NONE',  ( 14.66918480534031843, -51.92478805997374280, 13.49999999999999645 ) ) ;
#15361=DIRECTION ( 'NONE',  ( -0.000000000000000000, -0.000000000000000000, -1.000000000000000000 ) ) ;
#15364=VERTEX_POINT ( 'NONE', #8264 ) ;
#15365=DIRECTION ( 'NONE',  ( -1.000000000000000000, 0.000000000000000000, -0.000000000000000000 ) ) ;
#15367=CARTESIAN_POINT ( 'NONE',  ( -29.42156627136959557, -2.562835948873662506, 0.09431749384236855216 ) ) ;
#15368=EDGE_CURVE ( 'NONE', #12236, #8942, #15076, .T. ) ;
#15370=EDGE_CURVE ( 'NONE', #1798, #11697, #19680, .T. ) ;
#15371=DIRECTION ( 'NONE',  ( 1.000000000000000000, 0.000000000000000000, 0.000000000000000000 ) ) ;
#15375=ORIENTED_EDGE ( 'NONE', *, *, #4807, .F. ) ;
#15376=DIRECTION ( 'NONE',  ( 1.000000000000000000, 0.000000000000000000, -0.000000000000000000 ) ) ;
#15377=B_SPLINE_CURVE_WITH_KNOTS ( 'NONE', 3,
 ( #7916, #16503, #21230, #7680, #6019, #1168, #6129, #2747 ),
 .UNSPECIFIED., .F., .F.,
 ( 4, 2, 2, 4 ),
 ( 0.000000000000000000, 0.0001191530424135532222, 0.0002383060848271064444, 0.0004766121696541957583 ),
 .UNSPECIFIED. ) ;
#15381=DIRECTION ( 'NONE',  ( -1.000000000000000000, 0.000000000000000000, 0.000000000000000000 ) ) ;
#15384=LINE ( 'NONE', #1845, #14967 ) ;
#15385=CARTESIAN_POINT ( 'NONE',  ( 27.67540678000429111, -36.74634676501047181, 13.50000000000000000 ) ) ;
#15389=ORIENTED_EDGE ( 'NONE', *, *, #15811, .T. ) ;
#15390=DIRECTION ( 'NONE',  ( 0.000000000000000000, 0.000000000000000000, -1.000000000000000000 ) ) ;
#15392=CARTESIAN_POINT ( 'NONE',  ( 29.37573593128808369, -68.87573593128806237, -5.171888261068354354E-15 ) ) ;
#15393=ORIENTED_EDGE ( 'NONE', *, *, #3620, .F. ) ;
#15395=VERTEX_POINT ( 'NONE', #13508 ) ;
#15396=CARTESIAN_POINT ( 'NONE',  ( 3.627054932750481964, -32.11873716947361856, 68.00000000000000000 ) ) ;
#15397=DIRECTION ( 'NONE',  ( 1.000000000000000000, 0.000000000000000000, 0.000000000000000000 ) ) ;
#15399=DIRECTION ( 'NONE',  ( -1.000000000000000000, 0.000000000000000000, 0.000000000000000000 ) ) ;
#15402=CARTESIAN_POINT ( 'NONE',  ( 31.50000000000002132, 71.00000000000001421, 3.500000000000000000 ) ) ;
#15404=VERTEX_POINT ( 'NONE', #16863 ) ;
#15411=DIRECTION ( 'NONE',  ( 1.000000000000000000, 0.000000000000000000, -2.388292521039847891E-16 ) ) ;
#15413=CARTESIAN_POINT ( 'NONE',  ( 23.20993114852208805, 3.065002284660069076, 13.47295189337469878 ) ) ;
#15415=EDGE_CURVE ( 'NONE', #8431, #18168, #22152, .T. ) ;
#15423=EDGE_LOOP ( 'NONE', ( #13631, #9287, #13114, #6932 ) ) ;
#15424=CARTESIAN_POINT ( 'NONE',  ( 24.13662752439704917, 0.000000000000000000, 7.500000000000000000 ) ) ;
#15425=FACE_OUTER_BOUND ( 'NONE', #20397, .T. ) ;
#15428=EDGE_CURVE ( 'NONE', #10963, #1577, #13620, .T. ) ;
#15430=CIRCLE ( 'NONE', #11493, 5.000000000000000888 ) ;
#15431=VECTOR ( 'NONE', #19275, 1000.000000000000000 ) ;
#15432=DIRECTION ( 'NONE',  ( -0.000000000000000000, -0.000000000000000000, -1.000000000000000000 ) ) ;
#15433=ORIENTED_EDGE ( 'NONE', *, *, #7645, .T. ) ;
#15435=CYLINDRICAL_SURFACE ( 'NONE', #6881, 0.2999999999999999334 ) ;
#15436=CARTESIAN_POINT ( 'NONE',  ( 25.37540678000426908, 38.74634676501045760, 42.50000000000000000 ) ) ;
#15437=DIRECTION ( 'NONE',  ( 0.000000000000000000, 1.000000000000000000, 0.000000000000000000 ) ) ;
#15438=EDGE_CURVE ( 'NONE', #20293, #16692, #1531, .T. ) ;
#15439=CARTESIAN_POINT ( 'NONE',  ( 0.000000000000000000, 0.000000000000000000, 68.50000000000000000 ) ) ;
#15441=CARTESIAN_POINT ( 'NONE',  ( -9.141460742840918030, 33.43424481021354921, 42.50000000000000000 ) ) ;
#15443=ORIENTED_EDGE ( 'NONE', *, *, #6618, .F. ) ;
#15445=CARTESIAN_POINT ( 'NONE',  ( 17.93704824106378837, -38.74634676501045760, 13.87500000000000000 ) ) ;
#15449=ORIENTED_EDGE ( 'NONE', *, *, #12984, .T. ) ;
#15453=VERTEX_POINT ( 'NONE', #5241 ) ;
#15454=( NAMED_UNIT ( * ) PLANE_ANGLE_UNIT ( ) SI_UNIT ( $, .RADIAN. ) );
#15458=ORIENTED_EDGE ( 'NONE', *, *, #18114, .T. ) ;
#15459=DIRECTION ( 'NONE',  ( 1.000000000000000000, 0.000000000000000000, 0.000000000000000000 ) ) ;
#15460=DIRECTION ( 'NONE',  ( 0.000000000000000000, -1.000000000000000000, 0.000000000000000000 ) ) ;
#15465=CARTESIAN_POINT ( 'NONE',  ( -9.141460742840918030, 32.61873716947361856, 7.321391277662001151 ) ) ;
#15467=CARTESIAN_POINT ( 'NONE',  ( -15.21174975910705207, -51.86873716947361856, 13.05380965755523448 ) ) ;
#15469=CYLINDRICAL_SURFACE ( 'NONE', #5431, 6.500000000000002665 ) ;
#15471=ORIENTED_EDGE ( 'NONE', *, *, #14427, .T. ) ;
#15474=ORIENTED_EDGE ( 'NONE', *, *, #19492, .T. ) ;
#15476=EDGE_CURVE ( 'NONE', #16066, #17364, #11621, .T. ) ;
#15480=ORIENTED_EDGE ( 'NONE', *, *, #9152, .F. ) ;
#15481=CARTESIAN_POINT ( 'NONE',  ( 28.87540678000427619, -63.74634676501045050, 13.19999999999999929 ) ) ;
#15483=EDGE_CURVE ( 'NONE', #21353, #18406, #6286, .T. ) ;
#15485=CARTESIAN_POINT ( 'NONE',  ( 30.37540678000427619, 6.000000000000000000, 3.499999999999999556 ) ) ;
#15489=DIRECTION ( 'NONE',  ( 1.000000000000000000, 0.000000000000000000, 0.000000000000000000 ) ) ;
#15490=CARTESIAN_POINT ( 'NONE',  ( 29.13662752439705272, -4.700000000000000178, 3.799999999999999822 ) ) ;
#15491=B_SPLINE_CURVE_WITH_KNOTS ( 'NONE', 3,
 ( #21756, #21301, #1140, #4173, #11440, #14787, #9772, #12769 ),
 .UNSPECIFIED., .F., .F.,
 ( 4, 2, 2, 4 ),
 ( 0.000000000000000000, 0.0002312589012449784136, 0.0004625178024899568273, 0.0009250356049798978252 ),
 .UNSPECIFIED. ) ;
#15492=VERTEX_POINT ( 'NONE', #1962 ) ;
#15497=ADVANCED_FACE ( 'NONE', ( #6200 ), #695, .F. ) ;
#15498=EDGE_CURVE ( 'NONE', #11552, #9562, #12679, .T. ) ;
#15499=ORIENTED_EDGE ( 'NONE', *, *, #17904, .T. ) ;
#15501=ORIENTED_EDGE ( 'NONE', *, *, #2668, .F. ) ;
#15503=CARTESIAN_POINT ( 'NONE',  ( 29.13662752439705272, 0.000000000000000000, 13.19999999999999929 ) ) ;
#15511=CARTESIAN_POINT ( 'NONE',  ( 15.95292532278785913, 50.11873716947361856, 68.50000000000000000 ) ) ;
#15515=EDGE_CURVE ( 'NONE', #19461, #21526, #10591, .T. ) ;
#15518=CARTESIAN_POINT ( 'NONE',  ( -29.37540678000427619, 5.299999999999999822, 7.500000000000000000 ) ) ;
#15522=EDGE_CURVE ( 'NONE', #8649, #2930, #501, .T. ) ;
#15523=ORIENTED_EDGE ( 'NONE', *, *, #11504, .T. ) ;
#15524=AXIS2_PLACEMENT_3D ( 'NONE', #20412, #16811, #6651 ) ;
#15525=ORIENTED_EDGE ( 'NONE', *, *, #2653, .T. ) ;
#15526=CARTESIAN_POINT ( 'NONE',  ( -29.50000000000002132, 2.473451120191013430, 0.2999999999999947153 ) ) ;
#15528=CARTESIAN_POINT ( 'NONE',  ( -3.627054932750481964, 33.43424481021354921, 68.00000000000000000 ) ) ;
#15529=EDGE_CURVE ( 'NONE', #12670, #3289, #19099, .T. ) ;
#15530=DIRECTION ( 'NONE',  ( -0.000000000000000000, 0.000000000000000000, 1.000000000000000000 ) ) ;
#15531=ADVANCED_FACE ( 'NONE', ( #397 ), #9855, .T. ) ;
#15532=FACE_OUTER_BOUND ( 'NONE', #20672, .T. ) ;
#15535=AXIS2_PLACEMENT_3D ( 'NONE', #20573, #7040, #12479 ) ;
#15536=ORIENTED_EDGE ( 'NONE', *, *, #17518, .T. ) ;
#15537=DIRECTION ( 'NONE',  ( 1.000000000000000000, 0.000000000000000000, 0.000000000000000000 ) ) ;
#15538=ORIENTED_EDGE ( 'NONE', *, *, #14610, .T. ) ;
#15543=AXIS2_PLACEMENT_3D ( 'NONE', #15291, #19697, #2580 ) ;
#15545=CARTESIAN_POINT ( 'NONE',  ( 23.02398829872514696, -2.388718329487954595, 13.39778868030486869 ) ) ;
#15546=ORIENTED_EDGE ( 'NONE', *, *, #1445, .T. ) ;
#15549=EDGE_LOOP ( 'NONE', ( #9171, #63, #6216, #6826 ) ) ;
#15555=EDGE_CURVE ( 'NONE', #12963, #10963, #5217, .T. ) ;
#15556=CARTESIAN_POINT ( 'NONE',  ( -23.02398829872513986, 2.157133568460911199, 13.19999999999998685 ) ) ;
#15559=CARTESIAN_POINT ( 'NONE',  ( 15.21174975910705918, 42.11054587065083155, 13.79999999999999893 ) ) ;
#15561=AXIS2_PLACEMENT_3D ( 'NONE', #17472, #2019, #6978 ) ;
#15562=FACE_OUTER_BOUND ( 'NONE', #4662, .T. ) ;
#15564=ORIENTED_EDGE ( 'NONE', *, *, #13436, .F. ) ;
#15567=LINE ( 'NONE', #1925, #5676 ) ;
#15569=VERTEX_POINT ( 'NONE', #12472 ) ;
#15573=VECTOR ( 'NONE', #14945, 1000.000000000000000 ) ;
#15577=FACE_OUTER_BOUND ( 'NONE', #6393, .T. ) ;
#15579=VERTEX_POINT ( 'NONE', #5895 ) ;
#15580=CARTESIAN_POINT ( 'NONE',  ( -29.13662752439705272, -4.700000000000000178, 3.500000000000000000 ) ) ;
#15583=CARTESIAN_POINT ( 'NONE',  ( 25.37540678000427263, -68.44634676501046044, 7.500000000000000000 ) ) ;
#15585=CARTESIAN_POINT ( 'NONE',  ( -14.66174975910705136, 51.76873716947361714, 13.79999999999999893 ) ) ;
#15586=VERTEX_POINT ( 'NONE', #20789 ) ;
#15587=DIRECTION ( 'NONE',  ( 0.000000000000000000, -1.000000000000000000, 0.000000000000000000 ) ) ;
#15589=DIRECTION ( 'NONE',  ( -0.000000000000000000, -0.000000000000000000, 1.000000000000000000 ) ) ;
#15594=AXIS2_PLACEMENT_3D ( 'NONE', #11010, #2507, #19408 ) ;
#15595=ORIENTED_EDGE ( 'NONE', *, *, #16006, .T. ) ;
#15597=FACE_OUTER_BOUND ( 'NONE', #2312, .T. ) ;
#15598=B_SPLINE_CURVE_WITH_KNOTS ( 'NONE', 3,
 ( #811, #17820, #2499, #9327, #16133, #11214, #7654, #14448 ),
 .UNSPECIFIED., .F., .F.,
 ( 4, 2, 2, 4 ),
 ( -3.470042892451968281E-06, 0.0002769752510348927397, 0.0004171978979985645165, 0.0005574205449622362391 ),
 .UNSPECIFIED. ) ;
#15600=CARTESIAN_POINT ( 'NONE',  ( 29.37540678000427619, 5.299999999999999822, 7.500000000000000000 ) ) ;
#15602=VECTOR ( 'NONE', #11629, 1000.000000000000000 ) ;
#15605=EDGE_LOOP ( 'NONE', ( #5554, #16771, #8971, #21387 ) ) ;
#15606=DIRECTION ( 'NONE',  ( 0.000000000000000000, 0.000000000000000000, -1.000000000000000000 ) ) ;
#15616=DIRECTION ( 'NONE',  ( -1.000000000000000000, 0.000000000000000000, 0.000000000000000000 ) ) ;
#15618=ORIENTED_EDGE ( 'NONE', *, *, #19273, .F. ) ;
#15620=VECTOR ( 'NONE', #18171, 1000.000000000000000 ) ;
#15621=AXIS2_PLACEMENT_3D ( 'NONE', #1020, #21852, #6533 ) ;
#15622=EDGE_CURVE ( 'NONE', #11436, #2085, #3791, .T. ) ;
#15623=ORIENTED_EDGE ( 'NONE', *, *, #2148, .F. ) ;
#15625=ORIENTED_EDGE ( 'NONE', *, *, #7618, .T. ) ;
#15626=VERTEX_POINT ( 'NONE', #2196 ) ;
#15634=ADVANCED_FACE ( 'NONE', ( #9248 ), #16049, .F. ) ;
#15637=VECTOR ( 'NONE', #5421, 1000.000000000000000 ) ;
#15638=CIRCLE ( 'NONE', #11367, 0.5000000000000004441 ) ;
#15639=ORIENTED_EDGE ( 'NONE', *, *, #2520, .F. ) ;
#15640=DIRECTION ( 'NONE',  ( -0.000000000000000000, -0.000000000000000000, -1.000000000000000000 ) ) ;
#15641=CARTESIAN_POINT ( 'NONE',  ( 27.67540678000427690, 10.94079601157914539, 13.79999999999999893 ) ) ;
#15642=FACE_OUTER_BOUND ( 'NONE', #7911, .T. ) ;
#15643=DIRECTION ( 'NONE',  ( 0.000000000000000000, 0.000000000000000000, 1.000000000000000000 ) ) ;
#15644=LINE ( 'NONE', #649, #3633 ) ;
#15646=ORIENTED_EDGE ( 'NONE', *, *, #20302, .T. ) ;
#15650=ADVANCED_FACE ( 'NONE', ( #2865 ), #11463, .T. ) ;
#15651=DIRECTION ( 'NONE',  ( -0.000000000000000000, 0.000000000000000000, 1.000000000000000000 ) ) ;
#15652=CIRCLE ( 'NONE', #6036, 1.500000000000001332 ) ;
#15653=DIRECTION ( 'NONE',  ( 0.000000000000000000, 0.000000000000000000, 1.000000000000000000 ) ) ;
#15654=AXIS2_PLACEMENT_3D ( 'NONE', #10423, #3483, #4945 ) ;
#15655=ORIENTED_EDGE ( 'NONE', *, *, #8950, .T. ) ;
#15657=CARTESIAN_POINT ( 'NONE',  ( -15.00548668436308830, 51.86811046850819906, 13.49999999999993072 ) ) ;
#15660=CARTESIAN_POINT ( 'NONE',  ( 29.13662752439705272, 0.000000000000000000, 7.200000000000000178 ) ) ;
#15662=EDGE_CURVE ( 'NONE', #20783, #19588, #18785, .T. ) ;
#15665=AXIS2_PLACEMENT_3D ( 'NONE', #1644, #22157, #5026 ) ;
#15666=ADVANCED_FACE ( 'NONE', ( #19761 ), #4655, .F. ) ;
#15667=DIRECTION ( 'NONE',  ( -0.000000000000000000, -1.000000000000000000, -0.000000000000000000 ) ) ;
#15669=VECTOR ( 'NONE', #2812, 1000.000000000000000 ) ;
#15670=VERTEX_POINT ( 'NONE', #3073 ) ;
#15671=AXIS2_PLACEMENT_3D ( 'NONE', #17776, #11171, #14516 ) ;
#15674=CARTESIAN_POINT ( 'NONE',  ( -31.50000000000002132, 71.00000000000001421, 3.500000000000000000 ) ) ;
#15676=ADVANCED_FACE ( 'NONE', ( #8124 ), #22020, .F. ) ;
#15677=CARTESIAN_POINT ( 'NONE',  ( -23.10703542945396194, 2.595685412882489107, 13.38944394804412852 ) ) ;
#15678=DIRECTION ( 'NONE',  ( 0.000000000000000000, 0.000000000000000000, -1.000000000000000000 ) ) ;
#15679=CARTESIAN_POINT ( 'NONE',  ( 23.06007706085599906, -2.355179835980778513, 13.30024289742314814 ) ) ;
#15680=DIRECTION ( 'NONE',  ( 0.000000000000000000, 0.000000000000000000, -1.000000000000000000 ) ) ;
#15682=CARTESIAN_POINT ( 'NONE',  ( -15.21174975910705207, -52.10286008774954780, 13.87500000000000000 ) ) ;
#15683=CIRCLE ( 'NONE', #21803, 2.500000000000002220 ) ;
#15685=ORIENTED_EDGE ( 'NONE', *, *, #17274, .F. ) ;
#15686=LINE ( 'NONE', #5645, #15637 ) ;
#15687=VECTOR ( 'NONE', #9392, 1000.000000000000000 ) ;
#15688=FACE_OUTER_BOUND ( 'NONE', #7543, .T. ) ;
#15690=ORIENTED_EDGE ( 'NONE', *, *, #19273, .T. ) ;
#15692=AXIS2_PLACEMENT_3D ( 'NONE', #15700, #17170, #5336 ) ;
#15694=AXIS2_PLACEMENT_3D ( 'NONE', #12340, #2286, #19087 ) ;
#15695=DIRECTION ( 'NONE',  ( 0.000000000000000000, 1.000000000000000000, -0.000000000000000000 ) ) ;
#15696=ORIENTED_EDGE ( 'NONE', *, *, #12419, .F. ) ;
#15697=DIRECTION ( 'NONE',  ( 0.000000000000000000, 0.000000000000000000, -1.000000000000000000 ) ) ;
#15698=DIRECTION ( 'NONE',  ( 0.000000000000000000, 0.000000000000000000, -1.000000000000000000 ) ) ;
#15699=CARTESIAN_POINT ( 'NONE',  ( 29.37540678000427619, 6.000000000000000000, 3.799999999999999822 ) ) ;
#15700=CARTESIAN_POINT ( 'NONE',  ( 0.000000000000000000, -52.11873716947361856, 109.6002446535588319 ) ) ;
#15705=LINE ( 'NONE', #19508, #7930 ) ;
#15709=EDGE_CURVE ( 'NONE', #19513, #2319, #19870, .T. ) ;
#15713=LINE ( 'NONE', #12237, #7787 ) ;
#15716=TOROIDAL_SURFACE ( 'NONE', #17512, 1.300000000000000044, 0.2999999999999999889 ) ;
#15717=SPHERICAL_SURFACE ( 'NONE', #3938, 0.5000000000000000000 ) ;
#15718=VECTOR ( 'NONE', #10590, 1000.000000000000000 ) ;
#15721=EDGE_LOOP ( 'NONE', ( #20550, #10839, #6247, #19721 ) ) ;
#15722=CYLINDRICAL_SURFACE ( 'NONE', #10068, 0.5000000000000004441 ) ;
#15723=ORIENTED_EDGE ( 'NONE', *, *, #16684, .T. ) ;
#15724=FACE_OUTER_BOUND ( 'NONE', #7682, .T. ) ;
#15727=LINE ( 'NONE', #3892, #7233 ) ;
#15736=ADVANCED_FACE ( 'NONE', ( #17957 ), #7798, .F. ) ;
#15737=ORIENTED_EDGE ( 'NONE', *, *, #13236, .F. ) ;
#15742=CARTESIAN_POINT ( 'NONE',  ( 31.50000000000002132, -71.00000000000001421, 3.500000000000000000 ) ) ;
#15745=ORIENTED_EDGE ( 'NONE', *, *, #15767, .T. ) ;
#15749=DIRECTION ( 'NONE',  ( 0.000000000000000000, 0.000000000000000000, 1.000000000000000000 ) ) ;
#15750=CYLINDRICAL_SURFACE ( 'NONE', #4368, 2.000000000000001776 ) ;
#15751=CARTESIAN_POINT ( 'NONE',  ( 3.627054932750481964, -32.93424481021354921, 42.50000000000000000 ) ) ;
#15752=AXIS2_PLACEMENT_3D ( 'NONE', #5337, #20540, #18975 ) ;
#15753=VECTOR ( 'NONE', #9680, 1000.000000000000000 ) ;
#15755=VERTEX_POINT ( 'NONE', #18294 ) ;
#15756=CARTESIAN_POINT ( 'NONE',  ( 14.90249074642385096, 52.32070855895314310, 13.50000000000000178 ) ) ;
#15761=CARTESIAN_POINT ( 'NONE',  ( 29.13662752439705272, 0.000000000000000000, 7.500000000000000000 ) ) ;
#15762=EDGE_LOOP ( 'NONE', ( #20452, #7542, #15820, #19305 ) ) ;
#15763=DIRECTION ( 'NONE',  ( 1.000000000000000000, 0.000000000000000000, 0.000000000000000000 ) ) ;
#15765=CIRCLE ( 'NONE', #4702, 0.2999999999999999334 ) ;
#15766=ORIENTED_EDGE ( 'NONE', *, *, #15828, .T. ) ;
#15767=EDGE_CURVE ( 'NONE', #17212, #10568, #18817, .T. ) ;
#15771=ORIENTED_EDGE ( 'NONE', *, *, #22021, .T. ) ;
#15772=ADVANCED_FACE ( 'NONE', ( #19869 ), #15146, .F. ) ;
#15773=DIRECTION ( 'NONE',  ( 0.000000000000000000, 0.000000000000000000, 1.000000000000000000 ) ) ;
#15774=EDGE_LOOP ( 'NONE', ( #5624, #3098, #7460, #2601 ) ) ;
#15775=VERTEX_POINT ( 'NONE', #8446 ) ;
#15776=FACE_OUTER_BOUND ( 'NONE', #3664, .T. ) ;
#15779=FACE_OUTER_BOUND ( 'NONE', #13776, .T. ) ;
#15781=VECTOR ( 'NONE', #11624, 1000.000000000000000 ) ;
#15782=EDGE_CURVE ( 'NONE', #9791, #16858, #3453, .T. ) ;
#15784=CIRCLE ( 'NONE', #19382, 0.2999999999999999334 ) ;
#15785=ADVANCED_FACE ( 'NONE', ( #15262 ), #3192, .F. ) ;
#15789=EDGE_CURVE ( 'NONE', #5745, #21866, #10238, .T. ) ;
#15791=ORIENTED_EDGE ( 'NONE', *, *, #1124, .T. ) ;
#15794=LINE ( 'NONE', #12112, #17764 ) ;
#15798=EDGE_CURVE ( 'NONE', #17367, #16560, #20194, .T. ) ;
#15799=CIRCLE ( 'NONE', #4338, 0.2999999999999999334 ) ;
#15800=DIRECTION ( 'NONE',  ( -1.000000000000000000, 0.000000000000000000, 0.000000000000000000 ) ) ;
#15801=CARTESIAN_POINT ( 'NONE',  ( 23.04273156199908357, 2.261510999192739124, 7.500000000000000000 ) ) ;
#15803=CARTESIAN_POINT ( 'NONE',  ( -23.04273156199908357, 2.261510999192739124, 7.500000000000000000 ) ) ;
#15805=PLANE ( 'NONE',  #310 ) ;
#15806=CARTESIAN_POINT ( 'NONE',  ( -29.50000000000002132, -2.473451120191013430, 1.500000000000001332 ) ) ;
#15807=ADVANCED_FACE ( 'NONE', ( #151 ), #4985, .T. ) ;
#15810=DIRECTION ( 'NONE',  ( 0.000000000000000000, 0.000000000000000000, 1.000000000000000000 ) ) ;
#15811=EDGE_CURVE ( 'NONE', #20727, #19232, #13775, .T. ) ;
#15814=DIRECTION ( 'NONE',  ( 0.000000000000000000, 0.000000000000000000, 1.000000000000000000 ) ) ;
#15816=EDGE_LOOP ( 'NONE', ( #5564, #12921, #10320, #927 ) ) ;
#15817=ORIENTED_EDGE ( 'NONE', *, *, #12218, .T. ) ;
#15819=DIRECTION ( 'NONE',  ( 1.000000000000000000, -0.000000000000000000, 0.000000000000000000 ) ) ;
#15820=ORIENTED_EDGE ( 'NONE', *, *, #10242, .T. ) ;
#15821=CARTESIAN_POINT ( 'NONE',  ( 15.21174975910705918, 41.81054587065082728, 13.75000000000000000 ) ) ;
#15822=EDGE_LOOP ( 'NONE', ( #6085, #5374, #6145, #6063 ) ) ;
#15827=CARTESIAN_POINT ( 'NONE',  ( -28.82574430125643516, -6.542305536751587880, 13.37088755551135932 ) ) ;
#15828=EDGE_CURVE ( 'NONE', #1525, #2296, #2718, .T. ) ;
#15830=CARTESIAN_POINT ( 'NONE',  ( -25.37540678000429395, -39.04634676501046187, 13.50000000000000000 ) ) ;
#15831=ORIENTED_EDGE ( 'NONE', *, *, #8938, .T. ) ;
#15832=LINE ( 'NONE', #19323, #20950 ) ;
#15836=ORIENTED_EDGE ( 'NONE', *, *, #8072, .F. ) ;
#15839=ORIENTED_EDGE ( 'NONE', *, *, #19898, .T. ) ;
#15840=CARTESIAN_POINT ( 'NONE',  ( 15.95292532278785913, 34.11873716947361856, 42.50000000000000711 ) ) ;
#15841=LINE ( 'NONE', #5479, #8462 ) ;
#15843=ORIENTED_EDGE ( 'NONE', *, *, #4671, .F. ) ;
#15844=VERTEX_POINT ( 'NONE', #20535 ) ;
#15846=DIRECTION ( 'NONE',  ( -1.000000000000000000, 0.000000000000000000, 0.000000000000000000 ) ) ;
#15847=VERTEX_POINT ( 'NONE', #5096 ) ;
#15848=AXIS2_PLACEMENT_3D ( 'NONE', #9035, #17414, #19003 ) ;
#15849=ORIENTED_EDGE ( 'NONE', *, *, #2502, .F. ) ;
#15854=EDGE_CURVE ( 'NONE', #22008, #20718, #1390, .T. ) ;
#15855=AXIS2_PLACEMENT_3D ( 'NONE', #15153, #17059, #14936 ) ;
#15856=DIRECTION ( 'NONE',  ( 0.000000000000000000, -1.000000000000000000, 0.000000000000000000 ) ) ;
#15863=CARTESIAN_POINT ( 'NONE',  ( 18.22752199202934520, 39.04634676501046187, 13.50000000000000000 ) ) ;
#15866=ORIENTED_EDGE ( 'NONE', *, *, #15304, .T. ) ;
#15872=ORIENTED_EDGE ( 'NONE', *, *, #7666, .F. ) ;
#15873=EDGE_CURVE ( 'NONE', #12188, #13276, #6319, .T. ) ;
#15877=DIRECTION ( 'NONE',  ( -1.000000000000000000, -0.000000000000000000, 0.000000000000000000 ) ) ;
#15878=FACE_OUTER_BOUND ( 'NONE', #7128, .T. ) ;
#15880=CYLINDRICAL_SURFACE ( 'NONE', #17356, 0.3000000000000016542 ) ;
#15881=CIRCLE ( 'NONE', #3752, 0.2999999999999999334 ) ;
#15884=CARTESIAN_POINT ( 'NONE',  ( 28.87540678000428329, 6.494748934539265051, 13.24746166461178554 ) ) ;
#15885=LINE ( 'NONE', #5521, #15431 ) ;
#15886=CARTESIAN_POINT ( 'NONE',  ( 3.127054932750481964, -32.61873716947361856, 68.00000000000000000 ) ) ;
#15891=ORIENTED_EDGE ( 'NONE', *, *, #143, .F. ) ;
#15892=DIRECTION ( 'NONE',  ( -0.000000000000000000, 0.000000000000000000, 1.000000000000000000 ) ) ;
#15899=EDGE_CURVE ( 'NONE', #7824, #8633, #581, .T. ) ;
#15902=DIRECTION ( 'NONE',  ( -1.000000000000000000, 0.000000000000000000, -0.000000000000000000 ) ) ;
#15903=EDGE_LOOP ( 'NONE', ( #13651, #2129, #8319, #2976, #15211, #6691 ) ) ;
#15904=CARTESIAN_POINT ( 'NONE',  ( 15.95292532278785913, -50.11873716947361856, 13.87499999999999822 ) ) ;
#15906=DIRECTION ( 'NONE',  ( -0.000000000000000000, 1.000000000000000000, -0.000000000000000000 ) ) ;
#15908=CARTESIAN_POINT ( 'NONE',  ( -14.71432562863492421, 52.07267296161941061, 13.49999999999999822 ) ) ;
#15909=LINE ( 'NONE', #5213, #18058 ) ;
#15910=AXIS2_PLACEMENT_3D ( 'NONE', #9185, #15877, #5747 ) ;
#15911=AXIS2_PLACEMENT_3D ( 'NONE', #15241, #10003, #20176 ) ;
#15913=EDGE_CURVE ( 'NONE', #2242, #13197, #16019, .T. ) ;
#15915=FACE_OUTER_BOUND ( 'NONE', #5176, .T. ) ;
#15916=CARTESIAN_POINT ( 'NONE',  ( 0.000000000000000000, -32.11873716947361856, 109.6002446535588319 ) ) ;
#15918=ORIENTED_EDGE ( 'NONE', *, *, #21040, .T. ) ;
#15919=EDGE_LOOP ( 'NONE', ( #18464, #1744, #21362, #6471 ) ) ;
#15920=CARTESIAN_POINT ( 'NONE',  ( -15.95292532278785913, -52.11873716947361856, 14.00000000000000000 ) ) ;
#15927=VERTEX_POINT ( 'NONE', #17265 ) ;
#15928=CARTESIAN_POINT ( 'NONE',  ( -9.141460742840918030, 32.93424481021354921, 68.00000000000000000 ) ) ;
#15929=AXIS2_PLACEMENT_3D ( 'NONE', #1840, #16828, #3406 ) ;
#15931=EDGE_CURVE ( 'NONE', #20718, #5997, #257, .T. ) ;
#15933=DIRECTION ( 'NONE',  ( 1.000000000000000000, 0.000000000000000000, 0.000000000000000000 ) ) ;
#15934=DIRECTION ( 'NONE',  ( 1.000000000000000000, 0.000000000000000000, 0.000000000000000000 ) ) ;
#15935=CARTESIAN_POINT ( 'NONE',  ( 23.02398829872514341, 2.157133568460765538, 13.26781970120005560 ) ) ;
#15936=CARTESIAN_POINT ( 'NONE',  ( -23.32398829872514057, -2.157133568460768647, 7.500000000000000000 ) ) ;
#15937=ORIENTED_EDGE ( 'NONE', *, *, #16855, .F. ) ;
#15938=CARTESIAN_POINT ( 'NONE',  ( 29.17540678000427690, -63.74634676501045050, 7.500000000000000000 ) ) ;
#15941=DIRECTION ( 'NONE',  ( -0.000000000000000000, -1.000000000000000000, -0.000000000000000000 ) ) ;
#15943=VECTOR ( 'NONE', #12576, 1000.000000000000000 ) ;
#15944=AXIS2_PLACEMENT_3D ( 'NONE', #4766, #11465, #3076 ) ;
#15945=AXIS2_PLACEMENT_3D ( 'NONE', #3572, #10399, #4108 ) ;
#15946=AXIS2_PLACEMENT_3D ( 'NONE', #4476, #21395, #21181 ) ;
#15947=ORIENTED_EDGE ( 'NONE', *, *, #9724, .F. ) ;
#15948=CARTESIAN_POINT ( 'NONE',  ( -9.641460742840918030, 32.61873716947361856, 109.6002446535588319 ) ) ;
#15950=ORIENTED_EDGE ( 'NONE', *, *, #4895, .T. ) ;
#15952=FACE_OUTER_BOUND ( 'NONE', #4303, .T. ) ;
#15956=AXIS2_PLACEMENT_3D ( 'NONE', #11676, #3302, #3525 ) ;
#15957=ORIENTED_EDGE ( 'NONE', *, *, #20856, .T. ) ;
#15958=AXIS2_PLACEMENT_3D ( 'NONE', #13413, #20252, #18120 ) ;
#15959=EDGE_CURVE ( 'NONE', #18447, #6635, #12444, .T. ) ;
#15962=CARTESIAN_POINT ( 'NONE',  ( -31.50000000000002132, 71.70000000000001705, 1.500000000000000000 ) ) ;
#15963=CIRCLE ( 'NONE', #12386, 0.4999999999999995559 ) ;
#15964=B_SPLINE_CURVE_WITH_KNOTS ( 'NONE', 3,
 ( #7703, #14507, #3800, #3921, #10739, #17553 ),
 .UNSPECIFIED., .F., .F.,
 ( 4, 2, 4 ),
 ( 0.000000000000000000, 0.0002343434414548649890, 0.0004686868829097299780 ),
 .UNSPECIFIED. ) ;
#15967=CARTESIAN_POINT ( 'NONE',  ( 17.45292532278785913, 50.11873716947361856, 68.00000000000000000 ) ) ;
#15969=ORIENTED_EDGE ( 'NONE', *, *, #5862, .T. ) ;
#15970=CARTESIAN_POINT ( 'NONE',  ( 29.50000000000002132, 2.512390033608338680, 0.2497329951907094336 ) ) ;
#15974=VECTOR ( 'NONE', #13867, 1000.000000000000000 ) ;
#15975=ORIENTED_EDGE ( 'NONE', *, *, #11193, .F. ) ;
#15978=ORIENTED_EDGE ( 'NONE', *, *, #4443, .F. ) ;
#15980=ADVANCED_FACE ( 'NONE', ( #15577 ), #9150, .T. ) ;
#15986=VERTEX_POINT ( 'NONE', #12550 ) ;
#15988=CARTESIAN_POINT ( 'NONE',  ( 23.02398829872514341, -2.246571036181248981, 13.29719918165956294 ) ) ;
#15989=ORIENTED_EDGE ( 'NONE', *, *, #996, .F. ) ;
#15990=DIRECTION ( 'NONE',  ( 0.000000000000000000, -1.000000000000000000, 0.000000000000000000 ) ) ;
#15991=AXIS2_PLACEMENT_3D ( 'NONE', #1163, #4654, #13139 ) ;
#15992=CIRCLE ( 'NONE', #19231, 0.5000000000000004441 ) ;
#15993=CARTESIAN_POINT ( 'NONE',  ( -29.13662752439705272, 0.000000000000000000, 1.500000000000001332 ) ) ;
#15995=CARTESIAN_POINT ( 'NONE',  ( -29.37540678000427619, -6.000000000000000000, 7.500000000000000000 ) ) ;
#15996=AXIS2_PLACEMENT_3D ( 'NONE', #2113, #7169, #13853 ) ;
#15997=ADVANCED_FACE ( 'NONE', ( #19395 ), #20757, .T. ) ;
#15998=CIRCLE ( 'NONE', #6394, 2.274596669241483848 ) ;
#16000=CIRCLE ( 'NONE', #3878, 0.5000000000000004441 ) ;
#16002=CARTESIAN_POINT ( 'NONE',  ( -23.04273156199908357, 2.261510999192889670, 13.19999999999999218 ) ) ;
#16004=DIRECTION ( 'NONE',  ( 0.000000000000000000, 0.000000000000000000, 1.000000000000000000 ) ) ;
#16006=EDGE_CURVE ( 'NONE', #4820, #6732, #5433, .T. ) ;
#16007=EDGE_LOOP ( 'NONE', ( #12291, #13323, #16736, #8270 ) ) ;
#16008=ORIENTED_EDGE ( 'NONE', *, *, #5530, .T. ) ;
#16009=DIRECTION ( 'NONE',  ( -0.000000000000000000, -1.000000000000000000, 0.000000000000000000 ) ) ;
#16010=VECTOR ( 'NONE', #15077, 1000.000000000000000 ) ;
#16013=ORIENTED_EDGE ( 'NONE', *, *, #17908, .F. ) ;
#16014=VECTOR ( 'NONE', #17359, 1000.000000000000000 ) ;
#16015=EDGE_CURVE ( 'NONE', #12543, #18168, #4066, .T. ) ;
#16019=LINE ( 'NONE', #10555, #207 ) ;
#16021=CARTESIAN_POINT ( 'NONE',  ( 0.000000000000000000, 0.000000000000000000, 3.500000000000000000 ) ) ;
#16022=DIRECTION ( 'NONE',  ( -0.000000000000000000, -1.000000000000000000, -0.000000000000000000 ) ) ;
#16023=CIRCLE ( 'NONE', #21782, 0.5000000000000004441 ) ;
#16024=CARTESIAN_POINT ( 'NONE',  ( 14.96174975910705918, 51.76873716947361004, 13.79999999999999716 ) ) ;
#16027=ADVANCED_FACE ( 'NONE', ( #17374 ), #2268, .F. ) ;
#16030=CARTESIAN_POINT ( 'NONE',  ( 0.000000000000000000, -52.10286008774954780, 13.87500000000000000 ) ) ;
#16032=DIRECTION ( 'NONE',  ( 0.000000000000000000, 0.000000000000000000, 1.000000000000000000 ) ) ;
#16033=VERTEX_POINT ( 'NONE', #2161 ) ;
#16034=ORIENTED_EDGE ( 'NONE', *, *, #4515, .F. ) ;
#16036=CARTESIAN_POINT ( 'NONE',  ( 31.50000000000002132, 72.00000000000001421, 3.200000000000000178 ) ) ;
#16037=CYLINDRICAL_SURFACE ( 'NONE', #10670, 0.2500000000000002220 ) ;
#16038=VERTEX_POINT ( 'NONE', #15801 ) ;
#16040=( GEOMETRIC_REPRESENTATION_CONTEXT ( 3 ) GLOBAL_UNCERTAINTY_ASSIGNED_CONTEXT ( ( #19830 ) ) GLOBAL_UNIT_ASSIGNED_CONTEXT ( ( #5293, #15454, #11760 ) ) REPRESENTATION_CONTEXT ( 'NONE', 'WORKASPACE' ) );
#16041=AXIS2_PLACEMENT_3D ( 'NONE', #10084, #13311, #3356 ) ;
#16042=ORIENTED_EDGE ( 'NONE', *, *, #21858, .T. ) ;
#16045=EDGE_CURVE ( 'NONE', #4942, #2394, #470, .T. ) ;
#16046=DIRECTION ( 'NONE',  ( -0.000000000000000000, -0.000000000000000000, 1.000000000000000000 ) ) ;
#16047=PLANE ( 'NONE',  #7813 ) ;
#16049=PLANE ( 'NONE',  #7714 ) ;
#16050=ORIENTED_EDGE ( 'NONE', *, *, #640, .T. ) ;
#16052=DIRECTION ( 'NONE',  ( 0.000000000000000000, 0.000000000000000000, 1.000000000000000000 ) ) ;
#16054=LINE ( 'NONE', #4006, #18534 ) ;
#16056=CARTESIAN_POINT ( 'NONE',  ( 14.96174975910707161, 41.81054587065082728, 68.25000000000000000 ) ) ;
#16058=VERTEX_POINT ( 'NONE', #12771 ) ;
#16060=AXIS2_PLACEMENT_3D ( 'NONE', #5870, #12222, #5435 ) ;
#16061=DIRECTION ( 'NONE',  ( 0.000000000000000000, 1.000000000000000000, -0.000000000000000000 ) ) ;
#16062=AXIS2_PLACEMENT_3D ( 'NONE', #486, #14259, #19309 ) ;
#16064=CARTESIAN_POINT ( 'NONE',  ( -23.02398829872514341, -2.157133568460766426, 13.26781970120005738 ) ) ;
#16066=VERTEX_POINT ( 'NONE', #7986 ) ;
#16067=DIRECTION ( 'NONE',  ( -1.000000000000000000, 0.000000000000000000, 0.000000000000000000 ) ) ;
#16068=CARTESIAN_POINT ( 'NONE',  ( -3.627054932750481964, 32.93424481021354921, 68.00000000000000000 ) ) ;
#16070=LINE ( 'NONE', #5911, #9934 ) ;
#16073=ORIENTED_EDGE ( 'NONE', *, *, #6466, .F. ) ;
#16076=VERTEX_POINT ( 'NONE', #21757 ) ;
#16077=FACE_OUTER_BOUND ( 'NONE', #13687, .T. ) ;
#16078=CIRCLE ( 'NONE', #21831, 0.2999999999999999334 ) ;
#16080=DIRECTION ( 'NONE',  ( 1.000000000000000000, -0.000000000000000000, -0.000000000000000000 ) ) ;
#16085=ADVANCED_FACE ( 'NONE', ( #16572 ), #14790, .F. ) ;
#16088=EDGE_CURVE ( 'NONE', #4856, #20038, #21313, .T. ) ;
#16095=LINE ( 'NONE', #20039, #2039 ) ;
#16098=ORIENTED_EDGE ( 'NONE', *, *, #9196, .F. ) ;
#16100=EDGE_LOOP ( 'NONE', ( #20004, #12314, #8257, #13721 ) ) ;
#16102=AXIS2_PLACEMENT_3D ( 'NONE', #21709, #13799, #10368 ) ;
#16104=EDGE_CURVE ( 'NONE', #12460, #6564, #11641, .T. ) ;
#16105=DIRECTION ( 'NONE',  ( 0.000000000000000000, 0.000000000000000000, 1.000000000000000000 ) ) ;
#16106=AXIS2_PLACEMENT_3D ( 'NONE', #4813, #9971, #20257 ) ;
#16108=CARTESIAN_POINT ( 'NONE',  ( 29.50000000000002132, -69.00000000000000000, 0.2999999999999947153 ) ) ;
#16109=CARTESIAN_POINT ( 'NONE',  ( -15.21174975910705207, -41.81054587065082728, 68.50000000000000000 ) ) ;
#16110=AXIS2_PLACEMENT_3D ( 'NONE', #3860, #10683, #17499 ) ;
#16114=AXIS2_PLACEMENT_3D ( 'NONE', #13960, #20705, #5494 ) ;
#16115=( BOUNDED_SURFACE ( )  B_SPLINE_SURFACE ( 3, 2, ( 
 ( #7293, #21062, #14206 ),
 ( #19264, #12191, #12410 ),
 ( #19044, #10529, #7080 ),
 ( #19144, #443, #3708 ),
 ( #12090, #14087, #2015 ),
 ( #20936, #8969, #2348 ),
 ( #340, #7403, #5744 ),
 ( #1908, #15545, #10855 ),
 ( #8748, #13877, #19372 ),
 ( #10758, #15988, #12521 ),
 ( #3822, #2241, #3940 ),
 ( #222, #20726, #10643 ) ),
 .UNSPECIFIED., .F., .F., .F. ) 
 B_SPLINE_SURFACE_WITH_KNOTS ( ( 4, 2, 2, 2, 2, 4 ),
 ( 3, 3 ),
 ( 0.0006083281319963866878, 0.001004469391314930567, 0.001400610650633474664, 0.001796751909952018760, 0.001994822539611290808, 0.002192893169270562857 ),
 ( 0.000000000000000000, 1.000000000000000000 ),
 .UNSPECIFIED. ) 
 GEOMETRIC_REPRESENTATION_ITEM ( )  RATIONAL_B_SPLINE_SURFACE ( (
 ( 1.000000000000000000, 0.7071067811865475727, 1.000000000000000000),
 ( 1.000000000000000000, 0.7419362082869460640, 1.000000000000000000),
 ( 1.000000000000000000, 0.7734000586050232551, 1.000000000000000000),
 ( 1.000000000000000000, 0.8313348272087556223, 1.000000000000000000),
 ( 1.000000000000000000, 0.8578042680912326690, 1.000000000000000000),
 ( 1.000000000000000000, 0.9064979099737223711, 1.000000000000000000),
 ( 1.000000000000000000, 0.9284078965777988746, 1.000000000000000000),
 ( 1.000000000000000000, 0.9565959158316886812, 1.000000000000000000),
 ( 1.000000000000000000, 0.9652268734598682398, 1.000000000000000000),
 ( 1.000000000000000000, 0.9789818400845352597, 1.000000000000000000),
 ( 1.000000000000000000, 0.9843224408025195160, 1.000000000000000000),
 ( 1.000000000000000000, 0.9842566880020492404, 1.000000000000000000) ) ) 
 REPRESENTATION_ITEM ( '' )  SURFACE ( )  );
#16117=EDGE_LOOP ( 'NONE', ( #10825, #9316, #18613, #22013, #21925, #20889 ) ) ;
#16124=CIRCLE ( 'NONE', #2574, 0.5000000000000004441 ) ;
#16125=CARTESIAN_POINT ( 'NONE',  ( 27.37540678000427974, -5.683640910026986681, 13.79999999999999893 ) ) ;
#16126=VECTOR ( 'NONE', #11162, 1000.000000000000000 ) ;
#16128=AXIS2_PLACEMENT_3D ( 'NONE', #13477, #15267, #6796 ) ;
#16133=CARTESIAN_POINT ( 'NONE',  ( -28.82574430125643516, 6.542305536751587880, 13.37088755551135932 ) ) ;
#16134=CARTESIAN_POINT ( 'NONE',  ( -14.66174975910704781, 51.84664399969958737, 13.49999999999999645 ) ) ;
#16136=ORIENTED_EDGE ( 'NONE', *, *, #20246, .T. ) ;
#16137=DIRECTION ( 'NONE',  ( 1.000000000000000000, 0.000000000000000000, 0.000000000000000000 ) ) ;
#16139=ORIENTED_EDGE ( 'NONE', *, *, #4365, .T. ) ;
#16142=LINE ( 'NONE', #15920, #12732 ) ;
#16144=DIRECTION ( 'NONE',  ( 1.000000000000000000, 0.000000000000000000, 0.000000000000000000 ) ) ;
#16147=EDGE_CURVE ( 'NONE', #2496, #20277, #13790, .T. ) ;
#16151=CARTESIAN_POINT ( 'NONE',  ( -28.87540678000427619, 0.000000000000000000, 7.799999999999999822 ) ) ;
#16153=EDGE_CURVE ( 'NONE', #13818, #4728, #582, .T. ) ;
#16154=CARTESIAN_POINT ( 'NONE',  ( -17.45292532278785913, -34.11873716947361856, 68.00000000000000000 ) ) ;
#16156=DIRECTION ( 'NONE',  ( 1.000000000000000000, 0.000000000000000000, -2.388292521039847891E-16 ) ) ;
#16159=DIRECTION ( 'NONE',  ( 0.000000000000000000, -1.000000000000000000, 0.000000000000000000 ) ) ;
#16161=DIRECTION ( 'NONE',  ( -1.000000000000000000, 0.000000000000000000, 0.000000000000000000 ) ) ;
#16162=CARTESIAN_POINT ( 'NONE',  ( -23.04273156199909423, -2.261510999192741345, 13.22936009151389847 ) ) ;
#16163=ORIENTED_EDGE ( 'NONE', *, *, #16798, .F. ) ;
#16164=CARTESIAN_POINT ( 'NONE',  ( -15.21174975910705207, 52.39333383871510108, 13.79999999999999893 ) ) ;
#16165=DIRECTION ( 'NONE',  ( 0.000000000000000000, 0.000000000000000000, -1.000000000000000000 ) ) ;
#16169=EDGE_LOOP ( 'NONE', ( #17971, #13069, #11857, #2150, #4840, #8439 ) ) ;
#16170=ORIENTED_EDGE ( 'NONE', *, *, #15899, .F. ) ;
#16173=EDGE_CURVE ( 'NONE', #15775, #10812, #3467, .T. ) ;
#16174=CARTESIAN_POINT ( 'NONE',  ( 26.37540678000427619, -10.94079601157914716, 13.79999999999999893 ) ) ;
#16175=ORIENTED_EDGE ( 'NONE', *, *, #6878, .F. ) ;
#16178=EDGE_CURVE ( 'NONE', #8747, #4728, #15242, .T. ) ;
#16181=LINE ( 'NONE', #10736, #3848 ) ;
#16182=EDGE_CURVE ( 'NONE', #18705, #12963, #6203, .T. ) ;
#16184=CARTESIAN_POINT ( 'NONE',  ( -3.627054932750481964, 33.93424481021354921, 68.50000000000000000 ) ) ;
#16193=EDGE_CURVE ( 'NONE', #17942, #2242, #12372, .T. ) ;
#16194=CARTESIAN_POINT ( 'NONE',  ( -14.96174975910705207, -41.81054587065082728, 68.25000000000000000 ) ) ;
#16196=ORIENTED_EDGE ( 'NONE', *, *, #12652, .F. ) ;
#16197=EDGE_LOOP ( 'NONE', ( #9662, #15501, #5718, #11755 ) ) ;
#16199=DIRECTION ( 'NONE',  ( 0.000000000000000000, 0.000000000000000000, -1.000000000000000000 ) ) ;
#16201=AXIS2_PLACEMENT_3D ( 'NONE', #3256, #1339, #11854 ) ;
#16204=LINE ( 'NONE', #19466, #2579 ) ;
#16206=DIRECTION ( 'NONE',  ( -0.000000000000000000, 1.000000000000000000, 0.000000000000000000 ) ) ;
#16208=VERTEX_POINT ( 'NONE', #17805 ) ;
#16209=EDGE_CURVE ( 'NONE', #2496, #1170, #12028, .T. ) ;
#16210=DIRECTION ( 'NONE',  ( -0.000000000000000000, 1.000000000000000000, -0.000000000000000000 ) ) ;
#16212=DIRECTION ( 'NONE',  ( 1.000000000000000000, -0.000000000000000000, -0.000000000000000000 ) ) ;
#16215=DIRECTION ( 'NONE',  ( 1.000000000000000000, 0.000000000000000000, 0.000000000000000000 ) ) ;
#16217=CARTESIAN_POINT ( 'NONE',  ( -9.641460742840918030, -32.93424481021354921, 68.50000000000000000 ) ) ;
#16218=LINE ( 'NONE', #4385, #21016 ) ;
#16219=VERTEX_POINT ( 'NONE', #16217 ) ;
#16220=ORIENTED_EDGE ( 'NONE', *, *, #606, .F. ) ;
#16225=ORIENTED_EDGE ( 'NONE', *, *, #5750, .F. ) ;
#16226=DIRECTION ( 'NONE',  ( 1.000000000000000000, 0.000000000000000000, 0.000000000000000000 ) ) ;
#16228=CIRCLE ( 'NONE', #21265, 2.000000000000001776 ) ;
#16229=ADVANCED_FACE ( 'NONE', ( #13091 ), #11195, .T. ) ;
#16234=LINE ( 'NONE', #7891, #5070 ) ;
#16238=ORIENTED_EDGE ( 'NONE', *, *, #5487, .T. ) ;
#16239=CARTESIAN_POINT ( 'NONE',  ( -29.20000000000002061, 50.00000000000000000, 0.000000000000000000 ) ) ;
#16241=VERTEX_POINT ( 'NONE', #2692 ) ;
#16242=AXIS2_PLACEMENT_3D ( 'NONE', #6804, #13603, #16733 ) ;
#16245=VERTEX_POINT ( 'NONE', #4614 ) ;
#16246=DIRECTION ( 'NONE',  ( 1.000000000000000000, 0.000000000000000000, 0.000000000000000000 ) ) ;
#16253=CARTESIAN_POINT ( 'NONE',  ( 14.83748569039512866, -41.93480993936275780, 13.49999999999999822 ) ) ;
#16257=CIRCLE ( 'NONE', #12326, 0.2999999999999999334 ) ;
#16261=ORIENTED_EDGE ( 'NONE', *, *, #3509, .T. ) ;
#16262=DIRECTION ( 'NONE',  ( 1.000000000000000000, 0.000000000000000000, 0.000000000000000000 ) ) ;
#16263=CARTESIAN_POINT ( 'NONE',  ( -30.07540678000427548, 0.000000000000000000, 7.200000000000000178 ) ) ;
#16264=CARTESIAN_POINT ( 'NONE',  ( 25.37540678000429040, -36.74634676501047181, 13.79999999999999893 ) ) ;
#16265=CARTESIAN_POINT ( 'NONE',  ( -26.61833302554978786, 9.663695060508649348, 13.50000000000000000 ) ) ;
#16267=ADVANCED_FACE ( 'NONE', ( #21523 ), #14551, .F. ) ;
#16270=ORIENTED_EDGE ( 'NONE', *, *, #10506, .T. ) ;
#16272=CARTESIAN_POINT ( 'NONE',  ( -29.37540678000427619, 5.000000000000000000, 7.200000000000000178 ) ) ;
#16274=VECTOR ( 'NONE', #10156, 1000.000000000000000 ) ;
#16275=AXIS2_PLACEMENT_3D ( 'NONE', #14976, #18555, #22038 ) ;
#16278=DIRECTION ( 'NONE',  ( 1.000000000000000000, 0.000000000000000000, 0.000000000000000000 ) ) ;
#16280=EDGE_CURVE ( 'NONE', #12981, #1863, #18100, .T. ) ;
#16282=AXIS2_PLACEMENT_3D ( 'NONE', #14652, #21617, #6279 ) ;
#16284=AXIS2_PLACEMENT_3D ( 'NONE', #16937, #11787, #1604 ) ;
#16288=FACE_OUTER_BOUND ( 'NONE', #669, .T. ) ;
#16289=CIRCLE ( 'NONE', #14879, 1.499999999999999556 ) ;
#16292=AXIS2_PLACEMENT_3D ( 'NONE', #11387, #13280, #6374 ) ;
#16293=DIRECTION ( 'NONE',  ( 0.000000000000000000, 1.000000000000000000, 0.000000000000000000 ) ) ;
#16295=EDGE_CURVE ( 'NONE', #19855, #10953, #7748, .T. ) ;
#16296=LINE ( 'NONE', #14746, #21348 ) ;
#16299=DIRECTION ( 'NONE',  ( -0.000000000000000000, -0.000000000000000000, -1.000000000000000000 ) ) ;
#16305=EDGE_CURVE ( 'NONE', #4651, #124, #12868, .T. ) ;
#16313=FACE_OUTER_BOUND ( 'NONE', #22075, .T. ) ;
#16316=ORIENTED_EDGE ( 'NONE', *, *, #19901, .T. ) ;
#16317=CIRCLE ( 'NONE', #12387, 0.3000000000000004885 ) ;
#16318=LINE ( 'NONE', #21389, #12201 ) ;
#16319=ORIENTED_EDGE ( 'NONE', *, *, #21253, .T. ) ;
#16320=FACE_OUTER_BOUND ( 'NONE', #14607, .T. ) ;
#16324=EDGE_CURVE ( 'NONE', #11318, #12310, #2380, .T. ) ;
#16327=VECTOR ( 'NONE', #17981, 1000.000000000000000 ) ;
#16329=CARTESIAN_POINT ( 'NONE',  ( 23.04273156199908357, 2.261510999192738680, 13.19999999999999929 ) ) ;
#16330=FACE_OUTER_BOUND ( 'NONE', #10038, .T. ) ;
#16337=CIRCLE ( 'NONE', #3853, 0.2500000000000002220 ) ;
#16341=EDGE_CURVE ( 'NONE', #19370, #9810, #20969, .T. ) ;
#16342=FACE_OUTER_BOUND ( 'NONE', #16753, .T. ) ;
#16343=VERTEX_POINT ( 'NONE', #5964 ) ;
#16348=ORIENTED_EDGE ( 'NONE', *, *, #1473, .F. ) ;
#16350=CIRCLE ( 'NONE', #4206, 0.2999999999999999334 ) ;
#16351=AXIS2_PLACEMENT_3D ( 'NONE', #11786, #16716, #3636 ) ;
#16353=DIRECTION ( 'NONE',  ( -0.000000000000000000, 1.000000000000000000, -0.000000000000000000 ) ) ;
#16354=ORIENTED_EDGE ( 'NONE', *, *, #20928, .F. ) ;
#16355=CIRCLE ( 'NONE', #7805, 1.499999999999999556 ) ;
#16356=VECTOR ( 'NONE', #20395, 1000.000000000000000 ) ;
#16359=EDGE_CURVE ( 'NONE', #13238, #20804, #11965, .T. ) ;
#16360=CARTESIAN_POINT ( 'NONE',  ( 15.21174975910705918, -52.10286008774955491, 13.87500000000000000 ) ) ;
#16362=ORIENTED_EDGE ( 'NONE', *, *, #14872, .T. ) ;
#16364=EDGE_CURVE ( 'NONE', #17313, #13197, #3481, .T. ) ;
#16365=DIRECTION ( 'NONE',  ( 1.000000000000000000, 0.000000000000000000, -0.000000000000000000 ) ) ;
#16366=CARTESIAN_POINT ( 'NONE',  ( 15.21174975910705918, 52.39333383871510108, 13.50000000000000000 ) ) ;
#16370=ORIENTED_EDGE ( 'NONE', *, *, #2298, .T. ) ;
#16371=CARTESIAN_POINT ( 'NONE',  ( 31.50000000000002132, -71.00000000000001421, 1.500000000000000000 ) ) ;
#16373=AXIS2_PLACEMENT_3D ( 'NONE', #14714, #19873, #19426 ) ;
#16375=CIRCLE ( 'NONE', #10978, 0.2999999999999999334 ) ;
#16376=ORIENTED_EDGE ( 'NONE', *, *, #3505, .T. ) ;
#16377=AXIS2_PLACEMENT_3D ( 'NONE', #15660, #10427, #2236 ) ;
#16378=ORIENTED_EDGE ( 'NONE', *, *, #9485, .T. ) ;
#16380=AXIS2_PLACEMENT_3D ( 'NONE', #8722, #2317, #635 ) ;
#16383=ORIENTED_EDGE ( 'NONE', *, *, #21637, .T. ) ;
#16385=ORIENTED_EDGE ( 'NONE', *, *, #17666, .F. ) ;
#16386=DIRECTION ( 'NONE',  ( 0.000000000000000000, 0.000000000000000000, 1.000000000000000000 ) ) ;
#16387=VECTOR ( 'NONE', #6712, 1000.000000000000000 ) ;
#16388=DIRECTION ( 'NONE',  ( 0.000000000000000000, 0.000000000000000000, 1.000000000000000000 ) ) ;
#16389=LINE ( 'NONE', #11564, #7795 ) ;
#16390=DIRECTION ( 'NONE',  ( -0.000000000000000000, -1.000000000000000000, 0.000000000000000000 ) ) ;
#16391=AXIS2_PLACEMENT_3D ( 'NONE', #13911, #19072, #19178 ) ;
#16393=DIRECTION ( 'NONE',  ( 0.000000000000000000, 0.000000000000000000, 1.000000000000000000 ) ) ;
#16394=ORIENTED_EDGE ( 'NONE', *, *, #17737, .F. ) ;
#16396=FACE_OUTER_BOUND ( 'NONE', #9892, .T. ) ;
#16397=EDGE_CURVE ( 'NONE', #18789, #16208, #15108, .T. ) ;
#16398=EDGE_CURVE ( 'NONE', #10410, #8471, #12005, .T. ) ;
#16401=ORIENTED_EDGE ( 'NONE', *, *, #6956, .T. ) ;
#16402=EDGE_CURVE ( 'NONE', #1165, #6732, #5164, .T. ) ;
#16404=DIRECTION ( 'NONE',  ( 1.000000000000000000, 0.000000000000000000, 0.000000000000000000 ) ) ;
#16406=CARTESIAN_POINT ( 'NONE',  ( -17.45292532278785913, 0.000000000000000000, 13.99999999999999822 ) ) ;
#16407=DIRECTION ( 'NONE',  ( 1.000000000000000000, 0.000000000000000000, 0.000000000000000000 ) ) ;
#16408=ORIENTED_EDGE ( 'NONE', *, *, #20945, .F. ) ;
#16409=EDGE_LOOP ( 'NONE', ( #163, #5869, #6792, #15623 ) ) ;
#16411=LINE ( 'NONE', #12817, #4975 ) ;
#16412=LINE ( 'NONE', #21582, #3865 ) ;
#16413=AXIS2_PLACEMENT_3D ( 'NONE', #7062, #14078, #2225 ) ;
#16414=EDGE_LOOP ( 'NONE', ( #10788, #16376, #10229, #1212 ) ) ;
#16418=DIRECTION ( 'NONE',  ( -0.000000000000000000, -1.000000000000000000, -0.000000000000000000 ) ) ;
#16419=DIRECTION ( 'NONE',  ( 0.000000000000000000, -1.000000000000000000, 0.000000000000000000 ) ) ;
#16420=CYLINDRICAL_SURFACE ( 'NONE', #9527, 0.5000000000000004441 ) ;
#16424=FACE_OUTER_BOUND ( 'NONE', #17978, .T. ) ;
#16428=AXIS2_PLACEMENT_3D ( 'NONE', #18755, #20117, #13704 ) ;
#16429=LINE ( 'NONE', #13051, #11320 ) ;
#16430=CARTESIAN_POINT ( 'NONE',  ( 0.000000000000000000, 32.11873716947361856, 42.50000000000000711 ) ) ;
#16433=DIRECTION ( 'NONE',  ( 1.000000000000000000, 0.000000000000000000, 0.000000000000000000 ) ) ;
#16434=CARTESIAN_POINT ( 'NONE',  ( -15.95292532278785913, -52.09333383871509682, 13.79999999999999893 ) ) ;
#16435=DIRECTION ( 'NONE',  ( 1.000000000000000000, 0.000000000000000000, 0.000000000000000000 ) ) ;
#16436=ORIENTED_EDGE ( 'NONE', *, *, #7123, .F. ) ;
#16437=DIRECTION ( 'NONE',  ( -0.000000000000000000, 0.000000000000000000, 1.000000000000000000 ) ) ;
#16439=ORIENTED_EDGE ( 'NONE', *, *, #4694, .T. ) ;
#16441=DIRECTION ( 'NONE',  ( -1.000000000000000000, -0.000000000000000000, 0.000000000000000000 ) ) ;
#16443=DIRECTION ( 'NONE',  ( 0.000000000000000000, -1.000000000000000000, 0.000000000000000000 ) ) ;
#16444=ADVANCED_FACE ( 'NONE', ( #21955 ), #11656, .T. ) ;
#16445=FACE_OUTER_BOUND ( 'NONE', #194, .T. ) ;
#16446=FACE_OUTER_BOUND ( 'NONE', #12730, .T. ) ;
#16448=EDGE_CURVE ( 'NONE', #16241, #4678, #2367, .T. ) ;
#16449=CARTESIAN_POINT ( 'NONE',  ( 18.22752199202934520, -39.04634676501046187, 13.50000000000000000 ) ) ;
#16452=AXIS2_PLACEMENT_3D ( 'NONE', #19597, #2589, #11189 ) ;
#16454=CYLINDRICAL_SURFACE ( 'NONE', #12199, 6.500000000000002665 ) ;
#16455=CARTESIAN_POINT ( 'NONE',  ( -25.37540678000427263, -63.74634676501045050, 7.799999999999999822 ) ) ;
#16456=ORIENTED_EDGE ( 'NONE', *, *, #21196, .T. ) ;
#16459=ORIENTED_EDGE ( 'NONE', *, *, #19798, .F. ) ;
#16464=UNCERTAINTY_MEASURE_WITH_UNIT (LENGTH_MEASURE( 1.000000000000000082E-05 ), #4219, 'distance_accuracy_value', 'NONE');
#16467=VERTEX_POINT ( 'NONE', #18805 ) ;
#16470=EDGE_CURVE ( 'NONE', #20293, #19133, #13452, .T. ) ;
#16474=CARTESIAN_POINT ( 'NONE',  ( 18.22752199202934520, 0.000000000000000000, 13.79999999999999893 ) ) ;
#16477=EDGE_CURVE ( 'NONE', #9561, #13657, #3366, .T. ) ;
#16479=CYLINDRICAL_SURFACE ( 'NONE', #12181, 0.2999999999999999334 ) ;
#16480=DIRECTION ( 'NONE',  ( -1.000000000000000000, 0.000000000000000000, 0.000000000000000000 ) ) ;
#16484=ORIENTED_EDGE ( 'NONE', *, *, #21260, .F. ) ;
#16487=CARTESIAN_POINT ( 'NONE',  ( 23.32398829872514057, -2.157133568460768647, 13.50000000000000000 ) ) ;
#16488=CARTESIAN_POINT ( 'NONE',  ( 18.22752199202934520, 39.04634676501046187, 13.50000000000000000 ) ) ;
#16489=EDGE_CURVE ( 'NONE', #15404, #2691, #1682, .T. ) ;
#16490=VERTEX_POINT ( 'NONE', #18468 ) ;
#16494=VERTEX_POINT ( 'NONE', #6529 ) ;
#16496=DIRECTION ( 'NONE',  ( 1.000000000000000000, 0.000000000000000000, 0.000000000000000000 ) ) ;
#16497=EDGE_CURVE ( 'NONE', #1863, #13159, #13321, .T. ) ;
#16499=ORIENTED_EDGE ( 'NONE', *, *, #9385, .F. ) ;
#16500=CARTESIAN_POINT ( 'NONE',  ( -23.32398829872514057, -2.157133568460768647, 13.19999999999999929 ) ) ;
#16503=CARTESIAN_POINT ( 'NONE',  ( -14.96174975910705385, 51.80670431852983882, 13.81236938792781643 ) ) ;
#16505=ORIENTED_EDGE ( 'NONE', *, *, #7767, .F. ) ;
#16506=DIRECTION ( 'NONE',  ( -3.052134192567367925E-16, -1.000000000000000000, 0.000000000000000000 ) ) ;
#16508=CIRCLE ( 'NONE', #11498, 0.2999999999999999334 ) ;
#16511=CARTESIAN_POINT ( 'NONE',  ( -23.02398829872513986, -2.623740515231446135, 13.63037280509750637 ) ) ;
#16514=EDGE_LOOP ( 'NONE', ( #7838, #18414, #5014, #9329 ) ) ;
#16515=CARTESIAN_POINT ( 'NONE',  ( -15.00250675241655429, 51.98442790175712247, 13.86082508289638149 ) ) ;
#16516=DIRECTION ( 'NONE',  ( 0.000000000000000000, 0.000000000000000000, 1.000000000000000000 ) ) ;
#16520=ADVANCED_FACE ( 'NONE', ( #7069 ), #3597, .T. ) ;
#16522=CARTESIAN_POINT ( 'NONE',  ( -28.87540678000427619, 6.494748934539263274, 7.799999999999999822 ) ) ;
#16524=CARTESIAN_POINT ( 'NONE',  ( -23.02398829872513986, -2.624244922594602514, 13.63058196926743904 ) ) ;
#16527=FACE_OUTER_BOUND ( 'NONE', #10700, .T. ) ;
#16528=EDGE_CURVE ( 'NONE', #17106, #15492, #14181, .T. ) ;
#16530=DIRECTION ( 'NONE',  ( 1.000000000000000000, -0.000000000000000000, -0.000000000000000000 ) ) ;
#16532=ORIENTED_EDGE ( 'NONE', *, *, #14926, .T. ) ;
#16533=CARTESIAN_POINT ( 'NONE',  ( 9.141460742840918030, 32.11873716947361856, 68.00000000000000000 ) ) ;
#16536=CARTESIAN_POINT ( 'NONE',  ( 27.37540678000427619, 10.94079601157914539, 42.50000000000000000 ) ) ;
#16538=ORIENTED_EDGE ( 'NONE', *, *, #17756, .T. ) ;
#16540=FACE_OUTER_BOUND ( 'NONE', #7808, .T. ) ;
#16545=DIRECTION ( 'NONE',  ( 0.000000000000000000, 0.000000000000000000, 1.000000000000000000 ) ) ;
#16548=CARTESIAN_POINT ( 'NONE',  ( 27.37540678000426908, 36.74634676501047181, 13.79999999999999893 ) ) ;
#16549=LINE ( 'NONE', #14655, #14263 ) ;
#16551=CARTESIAN_POINT ( 'NONE',  ( -23.02398829872513986, -3.528912754968629439, 13.79999999999999893 ) ) ;
#16553=CARTESIAN_POINT ( 'NONE',  ( 29.17540678000427690, -6.499884319688664647, 7.500000000000000000 ) ) ;
#16555=ORIENTED_EDGE ( 'NONE', *, *, #8207, .F. ) ;
#16558=DIRECTION ( 'NONE',  ( 0.000000000000000000, 0.000000000000000000, 1.000000000000000000 ) ) ;
#16559=DIRECTION ( 'NONE',  ( -0.000000000000000000, -0.000000000000000000, -1.000000000000000000 ) ) ;
#16560=VERTEX_POINT ( 'NONE', #9262 ) ;
#16561=ORIENTED_EDGE ( 'NONE', *, *, #5488, .T. ) ;
#16565=ADVANCED_FACE ( 'NONE', ( #20716 ), #10421, .F. ) ;
#16566=ORIENTED_EDGE ( 'NONE', *, *, #19215, .T. ) ;
#16567=CARTESIAN_POINT ( 'NONE',  ( -29.20000000000002061, 50.00000000000000000, 0.000000000000000000 ) ) ;
#16569=VERTEX_POINT ( 'NONE', #5281 ) ;
#16570=ORIENTED_EDGE ( 'NONE', *, *, #20663, .F. ) ;
#16571=DIRECTION ( 'NONE',  ( 0.000000000000000000, 0.000000000000000000, -1.000000000000000000 ) ) ;
#16572=FACE_OUTER_BOUND ( 'NONE', #11464, .T. ) ;
#16573=AXIS2_PLACEMENT_3D ( 'NONE', #10792, #476, #18974 ) ;
#16574=ORIENTED_EDGE ( 'NONE', *, *, #16636, .T. ) ;
#16576=DIRECTION ( 'NONE',  ( 0.000000000000000000, 0.000000000000000000, 1.000000000000000000 ) ) ;
#16580=ORIENTED_EDGE ( 'NONE', *, *, #570, .F. ) ;
#16582=ORIENTED_EDGE ( 'NONE', *, *, #6976, .F. ) ;
#16583=CARTESIAN_POINT ( 'NONE',  ( -29.13662752439705272, -5.000000000000000000, 7.200000000000000178 ) ) ;
#16584=CARTESIAN_POINT ( 'NONE',  ( -29.48732477999263679, -2.488184282963944671, 0.2032176586593637813 ) ) ;
#16585=ADVANCED_FACE ( 'NONE', ( #17231 ), #6162, .F. ) ;
#16586=EDGE_LOOP ( 'NONE', ( #9558, #17623, #4581, #10801 ) ) ;
#16587=ADVANCED_FACE ( 'NONE', ( #11149 ), #12931, .T. ) ;
#16589=AXIS2_PLACEMENT_3D ( 'NONE', #10112, #8323, #14795 ) ;
#16591=VERTEX_POINT ( 'NONE', #964 ) ;
#16592=CARTESIAN_POINT ( 'NONE',  ( -29.37540678000427619, 6.000000000000000000, 3.799999999999999822 ) ) ;
#16593=CARTESIAN_POINT ( 'NONE',  ( -17.45292532278785913, 50.11873716947361856, 68.00000000000000000 ) ) ;
#16594=CARTESIAN_POINT ( 'NONE',  ( 23.02398829872513986, -2.280095008958279656, 13.43080372783514420 ) ) ;
#16597=DIRECTION ( 'NONE',  ( 0.000000000000000000, 0.000000000000000000, -1.000000000000000000 ) ) ;
#16598=CARTESIAN_POINT ( 'NONE',  ( 9.141460742840918030, 32.93424481021354921, 68.00000000000000000 ) ) ;
#16600=DIRECTION ( 'NONE',  ( 0.000000000000000000, 0.000000000000000000, 1.000000000000000000 ) ) ;
#16602=EDGE_LOOP ( 'NONE', ( #17281, #15989, #7661, #6895 ) ) ;
#16604=VECTOR ( 'NONE', #2641, 1000.000000000000000 ) ;
#16606=DIRECTION ( 'NONE',  ( 0.000000000000000000, 0.000000000000000000, 1.000000000000000000 ) ) ;
#16607=ORIENTED_EDGE ( 'NONE', *, *, #16879, .T. ) ;
#16608=CARTESIAN_POINT ( 'NONE',  ( 23.04273156199908357, 2.261510999192738680, 13.19999999999999929 ) ) ;
#16610=EDGE_LOOP ( 'NONE', ( #19762, #363, #14476, #11720 ) ) ;
#16613=CARTESIAN_POINT ( 'NONE',  ( -14.90262738048940960, 52.32122554936407255, 13.50000000000000000 ) ) ;
#16615=CARTESIAN_POINT ( 'NONE',  ( -29.37540678000427619, -6.000000000000000000, 7.200000000000000178 ) ) ;
#16617=ORIENTED_EDGE ( 'NONE', *, *, #5532, .F. ) ;
#16619=EDGE_CURVE ( 'NONE', #18066, #18442, #16317, .T. ) ;
#16624=DIRECTION ( 'NONE',  ( -1.000000000000000000, 0.000000000000000000, 0.000000000000000000 ) ) ;
#16625=CARTESIAN_POINT ( 'NONE',  ( -23.13120573414546755, -2.711843391866163522, 13.41529098820778110 ) ) ;
#16633=AXIS2_PLACEMENT_3D ( 'NONE', #20134, #3451, #18435 ) ;
#16636=EDGE_CURVE ( 'NONE', #8198, #18, #4176, .T. ) ;
#16637=LINE ( 'NONE', #20440, #10432 ) ;
#16639=EDGE_LOOP ( 'NONE', ( #17717, #10849, #20362, #18752 ) ) ;
#16644=ORIENTED_EDGE ( 'NONE', *, *, #16908, .F. ) ;
#16646=CARTESIAN_POINT ( 'NONE',  ( 29.50000000000003197, -2.473451120191014763, 0.2503162269321387856 ) ) ;
#16648=ORIENTED_EDGE ( 'NONE', *, *, #9569, .F. ) ;
#16649=CIRCLE ( 'NONE', #21302, 0.5000000000000004441 ) ;
#16654=FACE_OUTER_BOUND ( 'NONE', #125, .T. ) ;
#16657=DIRECTION ( 'NONE',  ( 1.000000000000000000, 0.000000000000000000, 0.000000000000000000 ) ) ;
#16658=CARTESIAN_POINT ( 'NONE',  ( 23.26721486835118569, 3.307416615798743909, 13.49999999999999645 ) ) ;
#16662=CARTESIAN_POINT ( 'NONE',  ( -14.66174954725422630, -51.84669727004962425, 13.50000000000000000 ) ) ;
#16663=EDGE_CURVE ( 'NONE', #18637, #5223, #7708, .T. ) ;
#16664=AXIS2_PLACEMENT_3D ( 'NONE', #14809, #6336, #13138 ) ;
#16665=DIRECTION ( 'NONE',  ( -0.000000000000000000, -0.000000000000000000, -1.000000000000000000 ) ) ;
#16666=CIRCLE ( 'NONE', #10255, 1.000000000000000888 ) ;
#16668=ORIENTED_EDGE ( 'NONE', *, *, #20408, .T. ) ;
#16674=ORIENTED_EDGE ( 'NONE', *, *, #16619, .T. ) ;
#16675=TOROIDAL_SURFACE ( 'NONE', #3485, 1.500000000000000000, 0.5000000000000000000 ) ;
#16676=VERTEX_POINT ( 'NONE', #21801 ) ;
#16679=VERTEX_POINT ( 'NONE', #6478 ) ;
#16683=CIRCLE ( 'NONE', #19552, 1.000000000000000888 ) ;
#16684=EDGE_CURVE ( 'NONE', #10017, #21319, #6359, .T. ) ;
#16685=AXIS2_PLACEMENT_3D ( 'NONE', #17219, #13851, #197 ) ;
#16686=AXIS2_PLACEMENT_3D ( 'NONE', #5163, #11964, #4941 ) ;
#16688=LINE ( 'NONE', #6764, #593 ) ;
#16690=DIRECTION ( 'NONE',  ( 0.000000000000000000, 0.000000000000000000, 1.000000000000000000 ) ) ;
#16692=VERTEX_POINT ( 'NONE', #14729 ) ;
#16694=EDGE_CURVE ( 'NONE', #19806, #6030, #6250, .T. ) ;
#16696=CARTESIAN_POINT ( 'NONE',  ( -15.95292532278785913, 50.11873716947361856, 13.87499999999999822 ) ) ;
#16697=CARTESIAN_POINT ( 'NONE',  ( -29.17540678000427690, 6.499884319688664647, 7.500000000000000000 ) ) ;
#16698=DIRECTION ( 'NONE',  ( -0.000000000000000000, 1.000000000000000000, -0.000000000000000000 ) ) ;
#16701=VECTOR ( 'NONE', #18423, 1000.000000000000000 ) ;
#16704=ORIENTED_EDGE ( 'NONE', *, *, #4716, .T. ) ;
#16706=DIRECTION ( 'NONE',  ( 0.000000000000000000, -0.000000000000000000, 1.000000000000000000 ) ) ;
#16707=EDGE_LOOP ( 'NONE', ( #21119, #21692, #7161, #20021 ) ) ;
#16714=CARTESIAN_POINT ( 'NONE',  ( 14.96174975910705918, 51.86873716947361856, 14.00000000000000000 ) ) ;
#16716=DIRECTION ( 'NONE',  ( 0.000000000000000000, 0.000000000000000000, 1.000000000000000000 ) ) ;
#16717=AXIS2_PLACEMENT_3D ( 'NONE', #18762, #8707, #3436 ) ;
#16718=AXIS2_PLACEMENT_3D ( 'NONE', #17108, #12052, #16982 ) ;
#16721=DIRECTION ( 'NONE',  ( 0.000000000000000000, 0.000000000000000000, 1.000000000000000000 ) ) ;
#16722=CYLINDRICAL_SURFACE ( 'NONE', #6426, 2.000000000000000000 ) ;
#16724=EDGE_CURVE ( 'NONE', #1905, #20015, #20332, .T. ) ;
#16725=AXIS2_PLACEMENT_3D ( 'NONE', #17223, #7502, #19025 ) ;
#16728=ORIENTED_EDGE ( 'NONE', *, *, #13726, .T. ) ;
#16731=VECTOR ( 'NONE', #13504, 1000.000000000000000 ) ;
#16733=DIRECTION ( 'NONE',  ( 0.000000000000000000, 0.000000000000000000, -1.000000000000000000 ) ) ;
#16734=DIRECTION ( 'NONE',  ( -1.000000000000000000, -0.000000000000000000, 0.000000000000000000 ) ) ;
#16735=ORIENTED_EDGE ( 'NONE', *, *, #14869, .T. ) ;
#16736=ORIENTED_EDGE ( 'NONE', *, *, #7668, .T. ) ;
#16737=ORIENTED_EDGE ( 'NONE', *, *, #21393, .F. ) ;
#16739=FACE_OUTER_BOUND ( 'NONE', #19126, .T. ) ;
#16740=DIRECTION ( 'NONE',  ( -0.000000000000000000, -0.000000000000000000, -1.000000000000000000 ) ) ;
#16742=ORIENTED_EDGE ( 'NONE', *, *, #5634, .F. ) ;
#16743=ADVANCED_FACE ( 'NONE', ( #1518 ), #6689, .F. ) ;
#16744=CIRCLE ( 'NONE', #12092, 1.000000000000000888 ) ;
#16746=DIRECTION ( 'NONE',  ( 1.000000000000000000, 0.000000000000000000, 0.000000000000000000 ) ) ;
#16750=DIRECTION ( 'NONE',  ( 0.000000000000000000, 0.000000000000000000, -1.000000000000000000 ) ) ;
#16751=DIRECTION ( 'NONE',  ( 1.000000000000000000, -0.000000000000000000, -0.000000000000000000 ) ) ;
#16752=DIRECTION ( 'NONE',  ( -0.000000000000000000, 1.000000000000000000, -0.000000000000000000 ) ) ;
#16753=EDGE_LOOP ( 'NONE', ( #2724, #20934, #16385, #11686 ) ) ;
#16755=ADVANCED_FACE ( 'NONE', ( #5002 ), #16955, .T. ) ;
#16761=ADVANCED_FACE ( 'NONE', ( #10040 ), #15163, .F. ) ;
#16763=VERTEX_POINT ( 'NONE', #16847 ) ;
#16768=ORIENTED_EDGE ( 'NONE', *, *, #9201, .T. ) ;
#16771=ORIENTED_EDGE ( 'NONE', *, *, #165, .T. ) ;
#16772=CARTESIAN_POINT ( 'NONE',  ( -30.37540678000427619, 63.74634676501045050, 3.799999999999999822 ) ) ;
#16777=DIRECTION ( 'NONE',  ( -0.000000000000000000, -0.000000000000000000, -1.000000000000000000 ) ) ;
#16778=CARTESIAN_POINT ( 'NONE',  ( -18.22752199202934520, -50.11873716947361856, 13.79999999999999893 ) ) ;
#16780=CARTESIAN_POINT ( 'NONE',  ( -25.37540678000427263, 68.44634676501046044, 7.200000000000000178 ) ) ;
#16781=FACE_OUTER_BOUND ( 'NONE', #4304, .T. ) ;
#16782=ADVANCED_FACE ( 'NONE', ( #6810 ), #5641, .F. ) ;
#16783=DIRECTION ( 'NONE',  ( 0.000000000000000000, 0.000000000000000000, 1.000000000000000000 ) ) ;
#16784=CARTESIAN_POINT ( 'NONE',  ( -14.98564789012718101, -51.95085597973990588, 13.85527924978055481 ) ) ;
#16786=AXIS2_PLACEMENT_3D ( 'NONE', #6223, #14592, #1059 ) ;
#16787=ORIENTED_EDGE ( 'NONE', *, *, #21778, .T. ) ;
#16788=DIRECTION ( 'NONE',  ( -0.000000000000000000, 0.000000000000000000, 1.000000000000000000 ) ) ;
#16794=ORIENTED_EDGE ( 'NONE', *, *, #9180, .F. ) ;
#16797=EDGE_LOOP ( 'NONE', ( #5513, #21136, #1521, #1080 ) ) ;
#16798=EDGE_CURVE ( 'NONE', #12793, #170, #10142, .T. ) ;
#16799=ORIENTED_EDGE ( 'NONE', *, *, #14245, .T. ) ;
#16801=ORIENTED_EDGE ( 'NONE', *, *, #6432, .F. ) ;
#16806=DIRECTION ( 'NONE',  ( 0.000000000000000000, 1.000000000000000000, 0.000000000000000000 ) ) ;
#16808=DIRECTION ( 'NONE',  ( 0.000000000000000000, 0.000000000000000000, 1.000000000000000000 ) ) ;
#16810=CYLINDRICAL_SURFACE ( 'NONE', #12547, 0.3000000000000016542 ) ;
#16811=DIRECTION ( 'NONE',  ( 0.000000000000000000, 0.000000000000000000, 1.000000000000000000 ) ) ;
#16813=VERTEX_POINT ( 'NONE', #15280 ) ;
#16814=VERTEX_POINT ( 'NONE', #22138 ) ;
#16815=ORIENTED_EDGE ( 'NONE', *, *, #13550, .T. ) ;
#16823=ADVANCED_FACE ( 'NONE', ( #5225 ), #13609, .F. ) ;
#16824=LINE ( 'NONE', #5201, #17387 ) ;
#16826=CYLINDRICAL_SURFACE ( 'NONE', #22061, 0.2500000000000002220 ) ;
#16828=DIRECTION ( 'NONE',  ( 0.000000000000000000, -1.000000000000000000, 0.000000000000000000 ) ) ;
#16830=CARTESIAN_POINT ( 'NONE',  ( 23.32398829872514057, 2.157133568460765538, 13.50000000000000000 ) ) ;
#16831=DIRECTION ( 'NONE',  ( 0.000000000000000000, -1.000000000000000000, 0.000000000000000000 ) ) ;
#16832=VECTOR ( 'NONE', #7025, 1000.000000000000000 ) ;
#16833=DIRECTION ( 'NONE',  ( -0.000000000000000000, 1.000000000000000000, -0.000000000000000000 ) ) ;
#16835=LINE ( 'NONE', #15154, #4379 ) ;
#16838=LINE ( 'NONE', #14750, #10346 ) ;
#16840=CARTESIAN_POINT ( 'NONE',  ( -9.141460742840918030, 33.93424481021354921, 68.00000000000000000 ) ) ;
#16841=CIRCLE ( 'NONE', #14330, 0.2999999999999999334 ) ;
#16842=DIRECTION ( 'NONE',  ( 0.000000000000000000, 0.000000000000000000, 1.000000000000000000 ) ) ;
#16844=ORIENTED_EDGE ( 'NONE', *, *, #18728, .F. ) ;
#16845=VERTEX_POINT ( 'NONE', #8793 ) ;
#16847=CARTESIAN_POINT ( 'NONE',  ( 4.127054932750481520, -33.93424481021354921, 68.50000000000000000 ) ) ;
#16848=AXIS2_PLACEMENT_3D ( 'NONE', #21428, #12889, #19969 ) ;
#16849=DIRECTION ( 'NONE',  ( 0.000000000000000000, -1.000000000000000000, 0.000000000000000000 ) ) ;
#16850=CIRCLE ( 'NONE', #8290, 0.5000000000000004441 ) ;
#16851=( BOUNDED_CURVE ( )  B_SPLINE_CURVE ( 3, ( #9280, #323, #2117, #5603 ),
 .UNSPECIFIED., .F., .T. ) 
 B_SPLINE_CURVE_WITH_KNOTS ( ( 4, 4 ),
 ( 0.000000000000000000, 1.570796326794896558 ),
 .UNSPECIFIED. ) 
 CURVE ( )  GEOMETRIC_REPRESENTATION_ITEM ( )  RATIONAL_B_SPLINE_CURVE ( ( 1.000000000000000000, 0.8047378541243649375, 0.8047378541243649375, 1.000000000000000000 ) ) 
 REPRESENTATION_ITEM ( '' )  );
#16852=ORIENTED_EDGE ( 'NONE', *, *, #18918, .T. ) ;
#16853=ADVANCED_FACE ( 'NONE', ( #15597 ), #16675, .T. ) ;
#16854=VERTEX_POINT ( 'NONE', #276 ) ;
#16855=EDGE_CURVE ( 'NONE', #1525, #14178, #19546, .T. ) ;
#16856=ORIENTED_EDGE ( 'NONE', *, *, #12806, .F. ) ;
#16857=DIRECTION ( 'NONE',  ( -3.052134192567367925E-16, -1.000000000000000000, 0.000000000000000000 ) ) ;
#16858=VERTEX_POINT ( 'NONE', #17393 ) ;
#16859=DIRECTION ( 'NONE',  ( 0.000000000000000000, 1.000000000000000000, 0.000000000000000000 ) ) ;
#16862=FACE_OUTER_BOUND ( 'NONE', #7878, .T. ) ;
#16863=CARTESIAN_POINT ( 'NONE',  ( -29.50000000000002132, -2.473451120191013430, 0.2999999999999947153 ) ) ;
#16865=AXIS2_PLACEMENT_3D ( 'NONE', #21518, #9308, #7740 ) ;
#16866=AXIS2_PLACEMENT_3D ( 'NONE', #2112, #7275, #5599 ) ;
#16868=DIRECTION ( 'NONE',  ( 1.000000000000000000, 0.000000000000000000, 0.000000000000000000 ) ) ;
#16869=ORIENTED_EDGE ( 'NONE', *, *, #6994, .F. ) ;
#16873=VERTEX_POINT ( 'NONE', #9337 ) ;
#16874=DIRECTION ( 'NONE',  ( 1.000000000000000000, -0.000000000000000000, -0.000000000000000000 ) ) ;
#16878=CARTESIAN_POINT ( 'NONE',  ( 25.37540678000427263, -63.74634676501045050, 7.799999999999999822 ) ) ;
#16879=EDGE_CURVE ( 'NONE', #13276, #21191, #16142, .T. ) ;
#16881=EDGE_CURVE ( 'NONE', #1455, #252, #2300, .T. ) ;
#16883=EDGE_CURVE ( 'NONE', #10410, #19345, #15713, .T. ) ;
#16885=EDGE_CURVE ( 'NONE', #1148, #21866, #19392, .T. ) ;
#16886=CARTESIAN_POINT ( 'NONE',  ( -29.17540678000427690, -63.74634676501045050, 7.799999999999999822 ) ) ;
#16888=CARTESIAN_POINT ( 'NONE',  ( -27.37540678000427619, 7.754037881813018962E-15, 42.50000000000000000 ) ) ;
#16891=CARTESIAN_POINT ( 'NONE',  ( -4.127054932750482408, 32.93424481021354921, 68.00000000000000000 ) ) ;
#16896=CARTESIAN_POINT ( 'NONE',  ( -25.37540678000427263, 68.74634676501045760, 7.500000000000000000 ) ) ;
#16897=CARTESIAN_POINT ( 'NONE',  ( -15.07123959906592248, -52.06981400416638905, 13.87294810141926149 ) ) ;
#16901=EDGE_LOOP ( 'NONE', ( #6255, #7015, #19631, #3304 ) ) ;
#16903=DIRECTION ( 'NONE',  ( 0.000000000000000000, 0.000000000000000000, 1.000000000000000000 ) ) ;
#16905=ORIENTED_EDGE ( 'NONE', *, *, #21624, .T. ) ;
#16906=CARTESIAN_POINT ( 'NONE',  ( 0.000000000000000000, -38.74634676501045760, 13.79999999999999893 ) ) ;
#16908=EDGE_CURVE ( 'NONE', #11436, #2833, #14199, .T. ) ;
#16909=EDGE_CURVE ( 'NONE', #2503, #3013, #21366, .T. ) ;
#16910=ORIENTED_EDGE ( 'NONE', *, *, #17052, .F. ) ;
#16912=ORIENTED_EDGE ( 'NONE', *, *, #1930, .F. ) ;
#16913=CARTESIAN_POINT ( 'NONE',  ( -26.37540678000427619, 10.94079601157914539, 13.79999999999999893 ) ) ;
#16914=B_SPLINE_CURVE_WITH_KNOTS ( 'NONE', 3,
 ( #20947, #5519, #17475, #2251, #9083, #21075, #15884, #9192 ),
 .UNSPECIFIED., .F., .F.,
 ( 4, 2, 2, 4 ),
 ( -3.470042892451968281E-06, 0.0002769752510348927397, 0.0004171978979985645165, 0.0005574205449622362391 ),
 .UNSPECIFIED. ) ;
#16915=CARTESIAN_POINT ( 'NONE',  ( 14.96174975910705918, -51.76873716947361004, 13.79999999999999716 ) ) ;
#16916=DIRECTION ( 'NONE',  ( -0.000000000000000000, 1.000000000000000000, 0.000000000000000000 ) ) ;
#16918=DIRECTION ( 'NONE',  ( -0.000000000000000000, -0.000000000000000000, -1.000000000000000000 ) ) ;
#16920=LINE ( 'NONE', #13570, #21868 ) ;
#16921=CARTESIAN_POINT ( 'NONE',  ( 30.07540678000427548, -6.000000000000000000, 7.200000000000000178 ) ) ;
#16922=ADVANCED_FACE ( 'NONE', ( #5784 ), #5678, .T. ) ;
#16923=DIRECTION ( 'NONE',  ( 1.000000000000000000, 0.000000000000000000, 0.000000000000000000 ) ) ;
#16928=ORIENTED_EDGE ( 'NONE', *, *, #2043, .T. ) ;
#16929=B_SPLINE_CURVE_WITH_KNOTS ( 'NONE', 3,
 ( #2146, #19054, #3507, #3954, #10445, #8661, #3722, #15679, #238, #10340, #8874, #12426, #1822, #12204 ),
 .UNSPECIFIED., .F., .F.,
 ( 4, 2, 2, 2, 2, 2, 4 ),
 ( 0.000000000000000000, 0.0006835338044177905739, 0.001025300706626683855, 0.001196184157731130333, 0.001281625883283352705, 0.001324346746059462806, 0.001367067608835572691 ),
 .UNSPECIFIED. ) ;
#16930=CARTESIAN_POINT ( 'NONE',  ( 14.96243083687292952, -51.84435441965536739, 13.82657707279502546 ) ) ;
#16934=CARTESIAN_POINT ( 'NONE',  ( 25.37540678000427263, -63.74634676501045050, 7.200000000000000178 ) ) ;
#16937=CARTESIAN_POINT ( 'NONE',  ( -14.96174975910705207, -51.61873716947361856, 14.00000000000000000 ) ) ;
#16938=ORIENTED_EDGE ( 'NONE', *, *, #2093, .T. ) ;
#16942=CARTESIAN_POINT ( 'NONE',  ( 25.37540678000429040, -36.74634676501047181, 13.79999999999999893 ) ) ;
#16945=CARTESIAN_POINT ( 'NONE',  ( -26.63662752439704917, -3.061616997868386099E-16, 3.500000000000000000 ) ) ;
#16946=EDGE_CURVE ( 'NONE', #19232, #9803, #14258, .T. ) ;
#16947=ORIENTED_EDGE ( 'NONE', *, *, #20385, .T. ) ;
#16949=DIRECTION ( 'NONE',  ( 0.000000000000000000, 0.000000000000000000, -1.000000000000000000 ) ) ;
#16955=PLANE ( 'NONE',  #8836 ) ;
#16957=FACE_OUTER_BOUND ( 'NONE', #12520, .T. ) ;
#16958=ORIENTED_EDGE ( 'NONE', *, *, #328, .T. ) ;
#16962=DIRECTION ( 'NONE',  ( 1.000000000000000000, 0.000000000000000000, 0.000000000000000000 ) ) ;
#16963=ORIENTED_EDGE ( 'NONE', *, *, #18247, .T. ) ;
#16966=EDGE_CURVE ( 'NONE', #1026, #20751, #18485, .T. ) ;
#16967=AXIS2_PLACEMENT_3D ( 'NONE', #18249, #6290, #6743 ) ;
#16970=DIRECTION ( 'NONE',  ( 1.000000000000000000, 0.000000000000000000, 0.000000000000000000 ) ) ;
#16971=VERTEX_POINT ( 'NONE', #3876 ) ;
#16972=CARTESIAN_POINT ( 'NONE',  ( 23.02398829872513630, 2.211005466174524425, 13.25091654438544353 ) ) ;
#16973=DIRECTION ( 'NONE',  ( 1.000000000000000000, 0.000000000000000000, 0.000000000000000000 ) ) ;
#16976=ORIENTED_EDGE ( 'NONE', *, *, #18025, .F. ) ;
#16978=EDGE_CURVE ( 'NONE', #3289, #5001, #2180, .T. ) ;
#16980=ORIENTED_EDGE ( 'NONE', *, *, #16724, .F. ) ;
#16981=DIRECTION ( 'NONE',  ( -0.000000000000000000, -0.000000000000000000, -1.000000000000000000 ) ) ;
#16982=DIRECTION ( 'NONE',  ( -1.000000000000000000, 0.000000000000000000, 0.000000000000000000 ) ) ;
#16986=DIRECTION ( 'NONE',  ( -2.388292521039847891E-16, 0.000000000000000000, -1.000000000000000000 ) ) ;
#16989=EDGE_LOOP ( 'NONE', ( #20536, #14017, #13674, #2637 ) ) ;
#16990=DIRECTION ( 'NONE',  ( -0.000000000000000000, 0.000000000000000000, 1.000000000000000000 ) ) ;
#16992=FACE_OUTER_BOUND ( 'NONE', #15068, .T. ) ;
#16993=DIRECTION ( 'NONE',  ( 1.000000000000000000, 0.000000000000000000, -0.000000000000000000 ) ) ;
#16995=FACE_OUTER_BOUND ( 'NONE', #16514, .T. ) ;
#16996=VECTOR ( 'NONE', #17272, 1000.000000000000000 ) ;
#16998=CARTESIAN_POINT ( 'NONE',  ( 14.96174975910705918, 51.61873716947361856, 14.00000000000000000 ) ) ;
#17000=ADVANCED_FACE ( 'NONE', ( #9785 ), #17782, .T. ) ;
#17001=DIRECTION ( 'NONE',  ( 1.000000000000000000, 0.000000000000000000, 0.000000000000000000 ) ) ;
#17003=CARTESIAN_POINT ( 'NONE',  ( -14.96174975910705207, -51.76873716947361714, 13.50000000000000000 ) ) ;
#17005=DIRECTION ( 'NONE',  ( -1.000000000000000000, 0.000000000000000000, 0.000000000000000000 ) ) ;
#17006=CARTESIAN_POINT ( 'NONE',  ( -30.37540678000427619, -63.74634676501045050, 3.799999999999999822 ) ) ;
#17007=CIRCLE ( 'NONE', #13785, 4.699999999999999289 ) ;
#17014=ORIENTED_EDGE ( 'NONE', *, *, #17867, .T. ) ;
#17016=EDGE_CURVE ( 'NONE', #15626, #15586, #4569, .T. ) ;
#17020=FACE_OUTER_BOUND ( 'NONE', #2345, .T. ) ;
#17021=CARTESIAN_POINT ( 'NONE',  ( -9.141460742840918030, -33.93424481021354921, 68.00000000000000000 ) ) ;
#17023=VECTOR ( 'NONE', #6793, 1000.000000000000000 ) ;
#17026=VECTOR ( 'NONE', #20255, 1000.000000000000000 ) ;
#17028=ADVANCED_FACE ( 'NONE', ( #14586 ), #9684, .T. ) ;
#17030=ADVANCED_FACE ( 'NONE', ( #14915 ), #19746, .F. ) ;
#17036=VERTEX_POINT ( 'NONE', #11117 ) ;
#17037=LINE ( 'NONE', #1588, #76 ) ;
#17038=ORIENTED_EDGE ( 'NONE', *, *, #4424, .T. ) ;
#17039=VERTEX_POINT ( 'NONE', #7998 ) ;
#17041=CARTESIAN_POINT ( 'NONE',  ( 30.07540678000427548, -6.000000000000000000, 7.500000000000000000 ) ) ;
#17044=CIRCLE ( 'NONE', #18842, 0.2999999999999999334 ) ;
#17045=AXIS2_PLACEMENT_3D ( 'NONE', #11527, #1346, #4821 ) ;
#17046=CYLINDRICAL_SURFACE ( 'NONE', #10235, 0.2999999999999999334 ) ;
#17047=EDGE_CURVE ( 'NONE', #11031, #11974, #8156, .T. ) ;
#17048=AXIS2_PLACEMENT_3D ( 'NONE', #14463, #7783, #9564 ) ;
#17049=ORIENTED_EDGE ( 'NONE', *, *, #5541, .F. ) ;
#17050=CARTESIAN_POINT ( 'NONE',  ( -9.641460742840918030, -32.11873716947361856, 109.6002446535588319 ) ) ;
#17051=VECTOR ( 'NONE', #4556, 1000.000000000000000 ) ;
#17052=EDGE_CURVE ( 'NONE', #20269, #14744, #7781, .T. ) ;
#17054=DIRECTION ( 'NONE',  ( 0.000000000000000000, -0.000000000000000000, -1.000000000000000000 ) ) ;
#17055=ORIENTED_EDGE ( 'NONE', *, *, #10824, .T. ) ;
#17057=DIRECTION ( 'NONE',  ( -2.832483164223434527E-16, 1.000000000000000000, 0.000000000000000000 ) ) ;
#17059=DIRECTION ( 'NONE',  ( 0.000000000000000000, 0.000000000000000000, 1.000000000000000000 ) ) ;
#17060=CARTESIAN_POINT ( 'NONE',  ( 28.87540678000427619, 63.74634676501045050, 7.799999999999999822 ) ) ;
#17062=CIRCLE ( 'NONE', #19570, 6.800000000000000711 ) ;
#17063=VECTOR ( 'NONE', #19677, 1000.000000000000000 ) ;
#17066=EDGE_CURVE ( 'NONE', #18311, #13976, #12436, .T. ) ;
#17067=EDGE_LOOP ( 'NONE', ( #15157, #1282, #21907, #7921 ) ) ;
#17069=DIRECTION ( 'NONE',  ( -0.000000000000000000, -1.000000000000000000, -0.000000000000000000 ) ) ;
#17070=AXIS2_PLACEMENT_3D ( 'NONE', #15821, #10808, #12573 ) ;
#17075=ORIENTED_EDGE ( 'NONE', *, *, #13630, .T. ) ;
#17076=DIRECTION ( 'NONE',  ( 1.000000000000000000, 0.000000000000000000, 0.000000000000000000 ) ) ;
#17078=AXIS2_PLACEMENT_3D ( 'NONE', #13322, #16559, #8081 ) ;
#17079=CARTESIAN_POINT ( 'NONE',  ( 8.641460742840918030, -32.93424481021354921, 42.50000000000000000 ) ) ;
#17081=DIRECTION ( 'NONE',  ( 1.000000000000000000, 0.000000000000000000, 0.000000000000000000 ) ) ;
#17082=EDGE_LOOP ( 'NONE', ( #2622, #6097, #5514, #10858 ) ) ;
#17083=AXIS2_PLACEMENT_3D ( 'NONE', #17116, #22051, #21724 ) ;
#17090=ADVANCED_FACE ( 'NONE', ( #18281 ), #21437, .T. ) ;
#17091=LINE ( 'NONE', #5465, #16731 ) ;
#17093=CARTESIAN_POINT ( 'NONE',  ( 9.641460742840918030, -32.61873716947361856, 68.00000000000000000 ) ) ;
#17095=CARTESIAN_POINT ( 'NONE',  ( 29.13662752439705272, 0.000000000000000000, 1.500000000000001332 ) ) ;
#17096=ORIENTED_EDGE ( 'NONE', *, *, #3600, .F. ) ;
#17097=CARTESIAN_POINT ( 'NONE',  ( 23.02398829872514341, 2.245853328535763360, 13.29652846991536563 ) ) ;
#17099=CARTESIAN_POINT ( 'NONE',  ( -18.22752199202934520, -39.04634676501046187, 13.50000000000000000 ) ) ;
#17102=DIRECTION ( 'NONE',  ( -0.000000000000000000, -0.000000000000000000, -1.000000000000000000 ) ) ;
#17105=VECTOR ( 'NONE', #15122, 1000.000000000000000 ) ;
#17106=VERTEX_POINT ( 'NONE', #16583 ) ;
#17108=CARTESIAN_POINT ( 'NONE',  ( -4.127054932750482408, 32.93424481021354921, 7.321391277662001151 ) ) ;
#17110=VECTOR ( 'NONE', #1769, 1000.000000000000000 ) ;
#17114=ORIENTED_EDGE ( 'NONE', *, *, #6252, .T. ) ;
#17115=EDGE_CURVE ( 'NONE', #7135, #8671, #9894, .T. ) ;
#17116=CARTESIAN_POINT ( 'NONE',  ( -3.127054932750481964, -32.93424481021354921, 68.00000000000000000 ) ) ;
#17118=CARTESIAN_POINT ( 'NONE',  ( 25.37540678000429040, -36.74634676501047181, 13.50000000000000000 ) ) ;
#17122=DIRECTION ( 'NONE',  ( 0.000000000000000000, 0.000000000000000000, 1.000000000000000000 ) ) ;
#17127=ORIENTED_EDGE ( 'NONE', *, *, #3559, .T. ) ;
#17129=DIRECTION ( 'NONE',  ( 0.000000000000000000, 0.000000000000000000, -1.000000000000000000 ) ) ;
#17131=ADVANCED_FACE ( 'NONE', ( #11339 ), #22103, .T. ) ;
#17133=ORIENTED_EDGE ( 'NONE', *, *, #8723, .F. ) ;
#17137=EDGE_CURVE ( 'NONE', #16854, #1535, #9923, .T. ) ;
#17138=ORIENTED_EDGE ( 'NONE', *, *, #15428, .F. ) ;
#17139=VERTEX_POINT ( 'NONE', #11995 ) ;
#17142=CARTESIAN_POINT ( 'NONE',  ( -23.32398829872514057, 2.157133568460765538, 13.50000000000000000 ) ) ;
#17144=AXIS2_PLACEMENT_3D ( 'NONE', #20413, #19157, #7202 ) ;
#17151=DIRECTION ( 'NONE',  ( 1.000000000000000000, 0.000000000000000000, 0.000000000000000000 ) ) ;
#17153=ORIENTED_EDGE ( 'NONE', *, *, #4070, .F. ) ;
#17154=DIRECTION ( 'NONE',  ( 0.000000000000000000, 1.000000000000000000, -0.000000000000000000 ) ) ;
#17158=AXIS2_PLACEMENT_3D ( 'NONE', #3189, #3069, #1601 ) ;
#17159=EDGE_CURVE ( 'NONE', #14847, #4254, #18838, .T. ) ;
#17161=EDGE_CURVE ( 'NONE', #15492, #13894, #15033, .T. ) ;
#17166=DIRECTION ( 'NONE',  ( 1.000000000000000000, 0.000000000000000000, 0.000000000000000000 ) ) ;
#17170=DIRECTION ( 'NONE',  ( 0.000000000000000000, -1.000000000000000000, 0.000000000000000000 ) ) ;
#17172=CARTESIAN_POINT ( 'NONE',  ( -9.141460742840918030, -33.43424481021354921, 68.00000000000000000 ) ) ;
#17173=AXIS2_PLACEMENT_3D ( 'NONE', #21284, #12866, #14099 ) ;
#17176=CARTESIAN_POINT ( 'NONE',  ( 9.141460742840918030, -33.43424481021354921, 42.50000000000000000 ) ) ;
#17178=DIRECTION ( 'NONE',  ( 1.000000000000000000, 0.000000000000000000, 0.000000000000000000 ) ) ;
#17180=ORIENTED_EDGE ( 'NONE', *, *, #9536, .T. ) ;
#17190=ORIENTED_EDGE ( 'NONE', *, *, #16619, .F. ) ;
#17192=CIRCLE ( 'NONE', #20067, 1.299999999999999156 ) ;
#17193=DIRECTION ( 'NONE',  ( -1.000000000000000000, 0.000000000000000000, -0.000000000000000000 ) ) ;
#17194=CARTESIAN_POINT ( 'NONE',  ( 4.127054932750481520, 33.43424481021354921, 42.50000000000000000 ) ) ;
#17195=DIRECTION ( 'NONE',  ( -1.000000000000000000, -0.000000000000000000, -0.000000000000000000 ) ) ;
#17197=CYLINDRICAL_SURFACE ( 'NONE', #5595, 5.000000000000004441 ) ;
#17198=DIRECTION ( 'NONE',  ( 0.000000000000000000, 0.000000000000000000, -1.000000000000000000 ) ) ;
#17199=CIRCLE ( 'NONE', #6152, 1.000000000000000888 ) ;
#17204=AXIS2_PLACEMENT_3D ( 'NONE', #5411, #1476, #11765 ) ;
#17206=CIRCLE ( 'NONE', #18990, 5.000000000000004441 ) ;
#17208=VERTEX_POINT ( 'NONE', #139 ) ;
#17210=ADVANCED_FACE ( 'NONE', ( #6559 ), #19946, .T. ) ;
#17211=CYLINDRICAL_SURFACE ( 'NONE', #7444, 1.000000000000000888 ) ;
#17212=VERTEX_POINT ( 'NONE', #17041 ) ;
#17213=ORIENTED_EDGE ( 'NONE', *, *, #17605, .F. ) ;
#17214=VERTEX_POINT ( 'NONE', #12111 ) ;
#17215=AXIS2_PLACEMENT_3D ( 'NONE', #14046, #290, #5466 ) ;
#17216=EDGE_CURVE ( 'NONE', #9183, #6237, #3269, .T. ) ;
#17217=CIRCLE ( 'NONE', #18286, 0.2500000000000002220 ) ;
#17218=ORIENTED_EDGE ( 'NONE', *, *, #21774, .T. ) ;
#17219=CARTESIAN_POINT ( 'NONE',  ( 29.05186365738250842, 0.05288320938007240457, 0.000000000000000000 ) ) ;
#17221=VECTOR ( 'NONE', #18162, 1000.000000000000000 ) ;
#17222=FACE_OUTER_BOUND ( 'NONE', #19632, .T. ) ;
#17223=CARTESIAN_POINT ( 'NONE',  ( -17.45292532278785913, 0.000000000000000000, 68.00000000000000000 ) ) ;
#17224=DIRECTION ( 'NONE',  ( 0.000000000000000000, 1.000000000000000000, -0.000000000000000000 ) ) ;
#17226=CYLINDRICAL_SURFACE ( 'NONE', #17944, 0.5000000000000004441 ) ;
#17228=VECTOR ( 'NONE', #18978, 1000.000000000000000 ) ;
#17231=FACE_OUTER_BOUND ( 'NONE', #2177, .T. ) ;
#17233=LINE ( 'NONE', #14, #186 ) ;
#17234=EDGE_CURVE ( 'NONE', #21381, #8248, #628, .T. ) ;
#17235=ORIENTED_EDGE ( 'NONE', *, *, #12667, .T. ) ;
#17236=ORIENTED_EDGE ( 'NONE', *, *, #2405, .T. ) ;
#17237=CYLINDRICAL_SURFACE ( 'NONE', #8886, 0.5000000000000004441 ) ;
#17241=DIRECTION ( 'NONE',  ( 0.000000000000000000, 1.000000000000000000, -0.000000000000000000 ) ) ;
#17244=DIRECTION ( 'NONE',  ( 0.000000000000000000, 0.000000000000000000, -1.000000000000000000 ) ) ;
#17246=EDGE_CURVE ( 'NONE', #17318, #21351, #3131, .T. ) ;
#17249=CARTESIAN_POINT ( 'NONE',  ( -23.02398829872525710, 2.334689865870841263, 13.36916081092377873 ) ) ;
#17250=CARTESIAN_POINT ( 'NONE',  ( 30.07540678000427548, -63.74634676501045050, 7.200000000000000178 ) ) ;
#17251=CARTESIAN_POINT ( 'NONE',  ( -29.37540678000427619, 5.000000000000000000, 3.799999999999999822 ) ) ;
#17252=CARTESIAN_POINT ( 'NONE',  ( 17.45292532278785913, 38.74634676501045760, 13.79999999999999893 ) ) ;
#17254=EDGE_CURVE ( 'NONE', #2496, #8891, #2035, .T. ) ;
#17256=VERTEX_POINT ( 'NONE', #9089 ) ;
#17258=DIRECTION ( 'NONE',  ( 0.000000000000000000, 1.000000000000000000, -0.000000000000000000 ) ) ;
#17259=LINE ( 'NONE', #20959, #2757 ) ;
#17262=ADVANCED_FACE ( 'NONE', ( #17687 ), #4938, .F. ) ;
#17265=CARTESIAN_POINT ( 'NONE',  ( 31.50000000000002132, -71.70000000000001705, 3.500000000000000000 ) ) ;
#17269=DIRECTION ( 'NONE',  ( 0.000000000000000000, 0.000000000000000000, 1.000000000000000000 ) ) ;
#17270=PLANE ( 'NONE',  #8026 ) ;
#17272=DIRECTION ( 'NONE',  ( 0.000000000000000000, 0.000000000000000000, -1.000000000000000000 ) ) ;
#17273=CARTESIAN_POINT ( 'NONE',  ( 29.37540678000427619, -6.000000000000000000, 7.500000000000000000 ) ) ;
#17274=EDGE_CURVE ( 'NONE', #11635, #19777, #4165, .T. ) ;
#17275=EDGE_CURVE ( 'NONE', #2212, #9069, #15567, .T. ) ;
#17281=ORIENTED_EDGE ( 'NONE', *, *, #19214, .T. ) ;
#17283=ORIENTED_EDGE ( 'NONE', *, *, #21196, .F. ) ;
#17285=DIRECTION ( 'NONE',  ( -3.052134192567367925E-16, -1.000000000000000000, 0.000000000000000000 ) ) ;
#17287=VECTOR ( 'NONE', #15000, 1000.000000000000000 ) ;
#17291=EDGE_CURVE ( 'NONE', #4773, #19066, #14940, .T. ) ;
#17294=LINE ( 'NONE', #11816, #6396 ) ;
#17295=DIRECTION ( 'NONE',  ( 0.000000000000000000, 0.000000000000000000, 1.000000000000000000 ) ) ;
#17296=DIRECTION ( 'NONE',  ( 0.000000000000000000, 0.000000000000000000, 1.000000000000000000 ) ) ;
#17297=ORIENTED_EDGE ( 'NONE', *, *, #8254, .T. ) ;
#17298=DIRECTION ( 'NONE',  ( -1.000000000000000000, 0.000000000000000000, 0.000000000000000000 ) ) ;
#17300=CARTESIAN_POINT ( 'NONE',  ( -17.92752199202934094, -50.11873716947361856, 13.79999999999999893 ) ) ;
#17301=DIRECTION ( 'NONE',  ( 1.000000000000000000, -0.000000000000000000, 0.000000000000000000 ) ) ;
#17302=ORIENTED_EDGE ( 'NONE', *, *, #7882, .T. ) ;
#17304=EDGE_CURVE ( 'NONE', #13966, #16058, #15686, .T. ) ;
#17306=EDGE_CURVE ( 'NONE', #11011, #497, #4587, .T. ) ;
#17308=ORIENTED_EDGE ( 'NONE', *, *, #6241, .F. ) ;
#17309=ORIENTED_EDGE ( 'NONE', *, *, #12884, .T. ) ;
#17313=VERTEX_POINT ( 'NONE', #2368 ) ;
#17315=CIRCLE ( 'NONE', #20911, 0.2999999999999999334 ) ;
#17316=AXIS2_PLACEMENT_3D ( 'NONE', #2360, #9524, #562 ) ;
#17318=VERTEX_POINT ( 'NONE', #17594 ) ;
#17319=DIRECTION ( 'NONE',  ( -3.052134192567367925E-16, 1.000000000000000000, -0.000000000000000000 ) ) ;
#17320=DIRECTION ( 'NONE',  ( 1.000000000000000000, 0.000000000000000000, 0.000000000000000000 ) ) ;
#17322=EDGE_CURVE ( 'NONE', #3983, #21319, #10548, .T. ) ;
#17324=CARTESIAN_POINT ( 'NONE',  ( 29.42075962687198754, 2.605814368445832141, 0.09348339755409348917 ) ) ;
#17326=DIRECTION ( 'NONE',  ( 0.000000000000000000, 0.000000000000000000, 1.000000000000000000 ) ) ;
#17329=EDGE_CURVE ( 'NONE', #9447, #16467, #569, .T. ) ;
#17330=VERTEX_POINT ( 'NONE', #17365 ) ;
#17332=CARTESIAN_POINT ( 'NONE',  ( -14.66174975910705136, 51.76873716947361714, 13.50000000000000000 ) ) ;
#17334=ORIENTED_EDGE ( 'NONE', *, *, #6994, .T. ) ;
#17337=ORIENTED_EDGE ( 'NONE', *, *, #11702, .F. ) ;
#17338=ORIENTED_EDGE ( 'NONE', *, *, #18680, .T. ) ;
#17339=DIRECTION ( 'NONE',  ( 0.000000000000000000, 0.000000000000000000, -1.000000000000000000 ) ) ;
#17340=EDGE_LOOP ( 'NONE', ( #19388, #17535, #1517, #8533 ) ) ;
#17342=AXIS2_PLACEMENT_3D ( 'NONE', #11689, #13483, #11796 ) ;
#17344=ORIENTED_EDGE ( 'NONE', *, *, #126, .F. ) ;
#17345=DIRECTION ( 'NONE',  ( -0.000000000000000000, -1.000000000000000000, -0.000000000000000000 ) ) ;
#17346=ADVANCED_FACE ( 'NONE', ( #14339 ), #359, .T. ) ;
#17347=CARTESIAN_POINT ( 'NONE',  ( -25.37540678000426908, 38.74634676501045760, 13.79999999999999893 ) ) ;
#17348=CARTESIAN_POINT ( 'NONE',  ( 0.000000000000000000, -51.61873716947361856, 14.00000000000000000 ) ) ;
#17351=CARTESIAN_POINT ( 'NONE',  ( 30.67540678000428045, -63.74634676501045050, 3.500000000000000000 ) ) ;
#17355=DIRECTION ( 'NONE',  ( 1.000000000000000000, 0.000000000000000000, 0.000000000000000000 ) ) ;
#17356=AXIS2_PLACEMENT_3D ( 'NONE', #679, #10862, #20620 ) ;
#17358=VECTOR ( 'NONE', #7964, 1000.000000000000000 ) ;
#17359=DIRECTION ( 'NONE',  ( 0.000000000000000000, -0.000000000000000000, -1.000000000000000000 ) ) ;
#17361=AXIS2_PLACEMENT_3D ( 'NONE', #7774, #4300, #17939 ) ;
#17363=VECTOR ( 'NONE', #8234, 1000.000000000000000 ) ;
#17364=VERTEX_POINT ( 'NONE', #2152 ) ;
#17365=CARTESIAN_POINT ( 'NONE',  ( -17.45292532278785913, -34.11873716947361856, 68.50000000000000000 ) ) ;
#17366=CARTESIAN_POINT ( 'NONE',  ( 29.05186365738250842, 0.05288320938007240457, 0.2999999999999947153 ) ) ;
#17367=VERTEX_POINT ( 'NONE', #9200 ) ;
#17369=CIRCLE ( 'NONE', #2731, 0.5000000000000004441 ) ;
#17370=VECTOR ( 'NONE', #10036, 1000.000000000000000 ) ;
#17371=TOROIDAL_SURFACE ( 'NONE', #3462, 3.200000000000003286, 0.2999999999999999889 ) ;
#17373=DIRECTION ( 'NONE',  ( -2.388292521039847891E-16, 0.000000000000000000, -1.000000000000000000 ) ) ;
#17374=FACE_OUTER_BOUND ( 'NONE', #21440, .T. ) ;
#17376=EDGE_LOOP ( 'NONE', ( #19142, #14461, #8240, #5510 ) ) ;
#17377=FACE_OUTER_BOUND ( 'NONE', #15340, .T. ) ;
#17379=CARTESIAN_POINT ( 'NONE',  ( -23.32398829872514057, 5.683640910026983128, 13.50000000000000000 ) ) ;
#17380=CARTESIAN_POINT ( 'NONE',  ( 29.20000000000002061, 2.848961824869257864, 0.000000000000000000 ) ) ;
#17382=DIRECTION ( 'NONE',  ( 0.000000000000000000, 0.000000000000000000, -1.000000000000000000 ) ) ;
#17383=CARTESIAN_POINT ( 'NONE',  ( 15.21174975910707161, -41.81054587065082728, 68.50000000000000000 ) ) ;
#17386=CYLINDRICAL_SURFACE ( 'NONE', #13757, 2.500000000000002220 ) ;
#17387=VECTOR ( 'NONE', #8336, 1000.000000000000000 ) ;
#17390=AXIS2_PLACEMENT_3D ( 'NONE', #15916, #594, #14254 ) ;
#17392=VERTEX_POINT ( 'NONE', #10877 ) ;
#17393=CARTESIAN_POINT ( 'NONE',  ( -17.95292532278785913, -50.11873716947361856, 13.99999999999999822 ) ) ;
#17395=LINE ( 'NONE', #15600, #20376 ) ;
#17398=AXIS2_PLACEMENT_3D ( 'NONE', #1856, #20448, #18531 ) ;
#17404=CIRCLE ( 'NONE', #4187, 2.500000000000002220 ) ;
#17405=EDGE_CURVE ( 'NONE', #21160, #21055, #20062, .T. ) ;
#17411=ORIENTED_EDGE ( 'NONE', *, *, #6612, .T. ) ;
#17412=LINE ( 'NONE', #14049, #5975 ) ;
#17414=DIRECTION ( 'NONE',  ( -0.000000000000000000, -1.000000000000000000, -0.000000000000000000 ) ) ;
#17415=DIRECTION ( 'NONE',  ( 0.000000000000000000, 1.000000000000000000, 0.000000000000000000 ) ) ;
#17417=AXIS2_PLACEMENT_3D ( 'NONE', #4409, #2852, #16246 ) ;
#17418=AXIS2_PLACEMENT_3D ( 'NONE', #1349, #18138, #12976 ) ;
#17420=CARTESIAN_POINT ( 'NONE',  ( 15.21174975910707161, -32.10873716947361345, 68.25000000000000000 ) ) ;
#17421=CYLINDRICAL_SURFACE ( 'NONE', #4502, 0.3000000000000016542 ) ;
#17422=ORIENTED_EDGE ( 'NONE', *, *, #17329, .F. ) ;
#17427=AXIS2_PLACEMENT_3D ( 'NONE', #6731, #9962, #1443 ) ;
#17428=VECTOR ( 'NONE', #14596, 1000.000000000000000 ) ;
#17430=ORIENTED_EDGE ( 'NONE', *, *, #16497, .T. ) ;
#17431=CIRCLE ( 'NONE', #4585, 3.800000000000004707 ) ;
#17433=AXIS2_PLACEMENT_3D ( 'NONE', #4282, #14555, #7753 ) ;
#17434=AXIS2_PLACEMENT_3D ( 'NONE', #1900, #5285, #16903 ) ;
#17435=EDGE_CURVE ( 'NONE', #9735, #15755, #1720, .T. ) ;
#17436=EDGE_CURVE ( 'NONE', #2755, #9735, #10985, .T. ) ;
#17438=FACE_OUTER_BOUND ( 'NONE', #21270, .T. ) ;
#17439=EDGE_CURVE ( 'NONE', #16241, #20933, #17798, .T. ) ;
#17442=DIRECTION ( 'NONE',  ( 1.000000000000000000, -0.000000000000000000, 0.000000000000000000 ) ) ;
#17444=VERTEX_POINT ( 'NONE', #4388 ) ;
#17446=VECTOR ( 'NONE', #20028, 1000.000000000000000 ) ;
#17447=CYLINDRICAL_SURFACE ( 'NONE', #13202, 0.2999999999999999334 ) ;
#17450=AXIS2_PLACEMENT_3D ( 'NONE', #3898, #7253, #7358 ) ;
#17452=VECTOR ( 'NONE', #12844, 1000.000000000000000 ) ;
#17453=AXIS2_PLACEMENT_3D ( 'NONE', #5525, #20847, #7307 ) ;
#17454=VERTEX_POINT ( 'NONE', #9314 ) ;
#17456=CARTESIAN_POINT ( 'NONE',  ( 32.20000000000001705, 71.00000000000001421, 3.500000000000000000 ) ) ;
#17460=ORIENTED_EDGE ( 'NONE', *, *, #18469, .T. ) ;
#17464=DIRECTION ( 'NONE',  ( 1.000000000000000000, -0.000000000000000000, 0.000000000000000000 ) ) ;
#17465=ORIENTED_EDGE ( 'NONE', *, *, #10260, .T. ) ;
#17467=EDGE_CURVE ( 'NONE', #21328, #20804, #2936, .T. ) ;
#17469=VECTOR ( 'NONE', #9471, 1000.000000000000000 ) ;
#17471=CARTESIAN_POINT ( 'NONE',  ( -17.95292532278785913, 38.74634676501045760, 42.50000000000000000 ) ) ;
#17472=CARTESIAN_POINT ( 'NONE',  ( 29.20000000000002061, 0.000000000000000000, 0.2999999999999947153 ) ) ;
#17475=CARTESIAN_POINT ( 'NONE',  ( 28.71290943744531177, 6.649236572130504896, 13.47739020623642325 ) ) ;
#17478=DIRECTION ( 'NONE',  ( 0.000000000000000000, 1.000000000000000000, 0.000000000000000000 ) ) ;
#17481=ORIENTED_EDGE ( 'NONE', *, *, #20069, .F. ) ;
#17485=ADVANCED_FACE ( 'NONE', ( #9534 ), #9941, .T. ) ;
#17486=EDGE_CURVE ( 'NONE', #15569, #15927, #8177, .T. ) ;
#17491=VECTOR ( 'NONE', #9613, 1000.000000000000000 ) ;
#17493=AXIS2_PLACEMENT_3D ( 'NONE', #9767, #1237, #16226 ) ;
#17495=DIRECTION ( 'NONE',  ( -0.000000000000000000, -0.000000000000000000, -1.000000000000000000 ) ) ;
#17496=EDGE_LOOP ( 'NONE', ( #16261, #14797, #10809, #6775, #17411 ) ) ;
#17497=CARTESIAN_POINT ( 'NONE',  ( 9.141460742840918030, 33.93424481021354921, 68.50000000000000000 ) ) ;
#17498=CARTESIAN_POINT ( 'NONE',  ( 15.21174975910705918, 51.86873716947361856, 13.05380965755522737 ) ) ;
#17499=DIRECTION ( 'NONE',  ( 0.000000000000000000, 0.000000000000000000, 1.000000000000000000 ) ) ;
#17504=ORIENTED_EDGE ( 'NONE', *, *, #16178, .T. ) ;
#17505=DIRECTION ( 'NONE',  ( -0.000000000000000000, -0.000000000000000000, -1.000000000000000000 ) ) ;
#17506=CARTESIAN_POINT ( 'NONE',  ( 15.21174975910705918, -52.39333383871510108, 13.79999999999999893 ) ) ;
#17507=CARTESIAN_POINT ( 'NONE',  ( -15.95292532278785913, -52.11873716947361856, 68.50000000000000000 ) ) ;
#17510=ORIENTED_EDGE ( 'NONE', *, *, #7203, .F. ) ;
#17511=CARTESIAN_POINT ( 'NONE',  ( 18.22752199202934520, 50.11873716947361856, 13.79999999999999893 ) ) ;
#17512=AXIS2_PLACEMENT_3D ( 'NONE', #16592, #1263, #18051 ) ;
#17517=CIRCLE ( 'NONE', #9669, 1.500000000000001332 ) ;
#17518=EDGE_CURVE ( 'NONE', #20718, #16569, #8085, .T. ) ;
#17526=DIRECTION ( 'NONE',  ( 0.000000000000000000, 1.000000000000000000, 0.000000000000000000 ) ) ;
#17528=ORIENTED_EDGE ( 'NONE', *, *, #22111, .F. ) ;
#17533=DIRECTION ( 'NONE',  ( 1.000000000000000000, 0.000000000000000000, 0.000000000000000000 ) ) ;
#17534=CARTESIAN_POINT ( 'NONE',  ( -15.95292532278785913, 51.61873716947361856, 14.00000000000000000 ) ) ;
#17535=ORIENTED_EDGE ( 'NONE', *, *, #10874, .F. ) ;
#17536=EDGE_CURVE ( 'NONE', #14127, #2103, #19953, .T. ) ;
#17537=CARTESIAN_POINT ( 'NONE',  ( 29.50000000000002132, -69.00000000000000000, 1.500000000000000000 ) ) ;
#17538=EDGE_LOOP ( 'NONE', ( #4135, #15269, #8407, #16362 ) ) ;
#17539=CYLINDRICAL_SURFACE ( 'NONE', #4817, 0.2500000000000002220 ) ;
#17543=FACE_OUTER_BOUND ( 'NONE', #6215, .T. ) ;
#17545=EDGE_CURVE ( 'NONE', #15319, #19806, #15998, .T. ) ;
#17546=DIRECTION ( 'NONE',  ( 1.000000000000000000, 0.000000000000000000, 0.000000000000000000 ) ) ;
#17547=ORIENTED_EDGE ( 'NONE', *, *, #4594, .T. ) ;
#17550=ORIENTED_EDGE ( 'NONE', *, *, #10627, .T. ) ;
#17551=DIRECTION ( 'NONE',  ( -0.000000000000000000, -0.000000000000000000, -1.000000000000000000 ) ) ;
#17553=CARTESIAN_POINT ( 'NONE',  ( 28.87540678000427619, 6.494748934539263274, 7.799999999999999822 ) ) ;
#17554=DIRECTION ( 'NONE',  ( 0.000000000000000000, -1.000000000000000000, 0.000000000000000000 ) ) ;
#17558=CARTESIAN_POINT ( 'NONE',  ( 15.21174975910707161, -51.61873716947361856, 68.50000000000000000 ) ) ;
#17559=VERTEX_POINT ( 'NONE', #9983 ) ;
#17560=DIRECTION ( 'NONE',  ( 1.000000000000000000, 0.000000000000000000, 0.000000000000000000 ) ) ;
#17563=EDGE_LOOP ( 'NONE', ( #13269, #13143, #17190, #11051 ) ) ;
#17564=EDGE_CURVE ( 'NONE', #5485, #9706, #11533, .T. ) ;
#17566=ORIENTED_EDGE ( 'NONE', *, *, #12072, .F. ) ;
#17570=CARTESIAN_POINT ( 'NONE',  ( 23.02398829872513986, 2.157133568460765538, 13.19999999999999929 ) ) ;
#17572=CIRCLE ( 'NONE', #16848, 6.800000000000000711 ) ;
#17577=VERTEX_POINT ( 'NONE', #4730 ) ;
#17578=DIRECTION ( 'NONE',  ( -0.000000000000000000, -1.000000000000000000, 0.000000000000000000 ) ) ;
#17580=EDGE_CURVE ( 'NONE', #877, #22102, #8520, .T. ) ;
#17586=DIRECTION ( 'NONE',  ( 0.000000000000000000, -1.000000000000000000, 0.000000000000000000 ) ) ;
#17590=ADVANCED_FACE ( 'NONE', ( #13325 ), #22073, .T. ) ;
#17592=ORIENTED_EDGE ( 'NONE', *, *, #3017, .T. ) ;
#17594=CARTESIAN_POINT ( 'NONE',  ( 29.50000000000002132, -2.473451120191013430, 1.500000000000001332 ) ) ;
#17595=EDGE_CURVE ( 'NONE', #18889, #20015, #22107, .T. ) ;
#17596=DIRECTION ( 'NONE',  ( -0.000000000000000000, -0.000000000000000000, -1.000000000000000000 ) ) ;
#17597=ORIENTED_EDGE ( 'NONE', *, *, #17435, .F. ) ;
#17601=CARTESIAN_POINT ( 'NONE',  ( 25.37540678000426908, 36.74634676501047181, 42.50000000000000000 ) ) ;
#17602=ORIENTED_EDGE ( 'NONE', *, *, #2656, .T. ) ;
#17603=DIRECTION ( 'NONE',  ( 0.000000000000000000, 0.000000000000000000, 1.000000000000000000 ) ) ;
#17604=DIRECTION ( 'NONE',  ( 0.000000000000000000, 0.000000000000000000, -1.000000000000000000 ) ) ;
#17605=EDGE_CURVE ( 'NONE', #8891, #22102, #20161, .T. ) ;
#17606=CARTESIAN_POINT ( 'NONE',  ( 15.21174975910705918, 52.11873716947361856, 14.00000000000000000 ) ) ;
#17607=DIRECTION ( 'NONE',  ( -0.000000000000000000, 1.000000000000000000, 0.000000000000000000 ) ) ;
#17608=CARTESIAN_POINT ( 'NONE',  ( -14.66895125224955621, 51.92349729544097414, 13.49999999999999822 ) ) ;
#17611=LINE ( 'NONE', #2280, #1253 ) ;
#17612=CARTESIAN_POINT ( 'NONE',  ( 29.50000000000002132, -69.00000000000000000, 0.2999999999999947153 ) ) ;
#17613=ORIENTED_EDGE ( 'NONE', *, *, #17921, .T. ) ;
#17615=ORIENTED_EDGE ( 'NONE', *, *, #19340, .F. ) ;
#17616=CARTESIAN_POINT ( 'NONE',  ( 27.77120804565220169, -2.094189496455408861, 0.2999999999999947153 ) ) ;
#17623=ORIENTED_EDGE ( 'NONE', *, *, #11585, .F. ) ;
#17624=CYLINDRICAL_SURFACE ( 'NONE', #9576, 0.5000000000000004441 ) ;
#17625=DIRECTION ( 'NONE',  ( 0.000000000000000000, 0.000000000000000000, 1.000000000000000000 ) ) ;
#17627=CARTESIAN_POINT ( 'NONE',  ( -9.141460742840918030, 33.43424481021354921, 42.50000000000000000 ) ) ;
#17629=CARTESIAN_POINT ( 'NONE',  ( -17.95292532278785913, 0.000000000000000000, 109.6002446535588319 ) ) ;
#17631=ADVANCED_FACE ( 'NONE', ( #8643 ), #10201, .F. ) ;
#17632=DIRECTION ( 'NONE',  ( 0.000000000000000000, 0.000000000000000000, 1.000000000000000000 ) ) ;
#17633=ORIENTED_EDGE ( 'NONE', *, *, #16295, .F. ) ;
#17634=ADVANCED_FACE ( 'NONE', ( #3487 ), #5694, .T. ) ;
#17637=CYLINDRICAL_SURFACE ( 'NONE', #10535, 0.5000000000000004441 ) ;
#17638=LINE ( 'NONE', #7364, #565 ) ;
#17640=ORIENTED_EDGE ( 'NONE', *, *, #15099, .T. ) ;
#17642=CYLINDRICAL_SURFACE ( 'NONE', #9608, 0.2999999999999999334 ) ;
#17647=EDGE_LOOP ( 'NONE', ( #10292, #4770, #5419, #8495 ) ) ;
#17648=CARTESIAN_POINT ( 'NONE',  ( -30.67540678000428045, 0.000000000000000000, 3.799999999999999822 ) ) ;
#17650=CARTESIAN_POINT ( 'NONE',  ( -15.95292532278785913, 51.61873716947361856, 68.00000000000000000 ) ) ;
#17655=CARTESIAN_POINT ( 'NONE',  ( 0.000000000000000000, 52.11873716947361856, 109.6002446535588319 ) ) ;
#17657=DIRECTION ( 'NONE',  ( 0.000000000000000000, 0.000000000000000000, 1.000000000000000000 ) ) ;
#17658=CARTESIAN_POINT ( 'NONE',  ( 15.95292532278785913, 50.11873716947361856, 68.00000000000000000 ) ) ;
#17663=VERTEX_POINT ( 'NONE', #17570 ) ;
#17665=CARTESIAN_POINT ( 'NONE',  ( -25.37540678000427263, 63.74634676501045050, 13.19999999999999929 ) ) ;
#17666=EDGE_CURVE ( 'NONE', #7269, #21686, #20931, .T. ) ;
#17669=CARTESIAN_POINT ( 'NONE',  ( 15.95292532278785913, 52.09333383871509682, 13.79999999999999893 ) ) ;
#17670=EDGE_LOOP ( 'NONE', ( #17920, #2488, #8679, #11097 ) ) ;
#17672=ORIENTED_EDGE ( 'NONE', *, *, #21139, .F. ) ;
#17673=ADVANCED_FACE ( 'NONE', ( #5289 ), #17237, .T. ) ;
#17676=DIRECTION ( 'NONE',  ( 0.000000000000000000, 0.000000000000000000, 1.000000000000000000 ) ) ;
#17677=EDGE_CURVE ( 'NONE', #7044, #20727, #2010, .T. ) ;
#17680=CARTESIAN_POINT ( 'NONE',  ( -23.02398829872513986, 2.192121262983578234, 13.33089993820317964 ) ) ;
#17684=ORIENTED_EDGE ( 'NONE', *, *, #2808, .F. ) ;
#17686=ORIENTED_EDGE ( 'NONE', *, *, #14919, .T. ) ;
#17687=FACE_OUTER_BOUND ( 'NONE', #22076, .T. ) ;
#17690=VERTEX_POINT ( 'NONE', #10850 ) ;
#17691=CIRCLE ( 'NONE', #15189, 5.000000000000000888 ) ;
#17693=VERTEX_POINT ( 'NONE', #8965 ) ;
#17695=FACE_OUTER_BOUND ( 'NONE', #18084, .T. ) ;
#17696=ADVANCED_FACE ( 'NONE', ( #4040 ), #3165, .T. ) ;
#17697=VECTOR ( 'NONE', #3780, 1000.000000000000000 ) ;
#17699=AXIS2_PLACEMENT_3D ( 'NONE', #7248, #16390, #5178 ) ;
#17701=CARTESIAN_POINT ( 'NONE',  ( 31.50000000000002132, -71.70000000000001705, 1.800000000000000044 ) ) ;
#17702=EDGE_CURVE ( 'NONE', #11864, #18602, #10329, .T. ) ;
#17703=CYLINDRICAL_SURFACE ( 'NONE', #5369, 0.5000000000000004441 ) ;
#17705=CARTESIAN_POINT ( 'NONE',  ( 15.21174975910705918, 52.10286008774955491, 13.87500000000000000 ) ) ;
#17706=CARTESIAN_POINT ( 'NONE',  ( -15.95292532278785913, -32.11873716947361856, 68.00000000000000000 ) ) ;
#17707=CARTESIAN_POINT ( 'NONE',  ( -23.02398829872515051, 3.003070052962827141, 13.75712488064577599 ) ) ;
#17708=AXIS2_PLACEMENT_3D ( 'NONE', #2613, #12998, #19509 ) ;
#17709=VECTOR ( 'NONE', #1146, 1000.000000000000000 ) ;
#17713=DIRECTION ( 'NONE',  ( 1.000000000000000000, -0.000000000000000000, -0.000000000000000000 ) ) ;
#17714=FACE_OUTER_BOUND ( 'NONE', #12514, .T. ) ;
#17715=VERTEX_POINT ( 'NONE', #2343 ) ;
#17716=ORIENTED_EDGE ( 'NONE', *, *, #18639, .T. ) ;
#17717=ORIENTED_EDGE ( 'NONE', *, *, #8207, .T. ) ;
#17718=CARTESIAN_POINT ( 'NONE',  ( -28.90801073195815718, -6.496214187273303686, 7.643093741255248652 ) ) ;
#17719=CARTESIAN_POINT ( 'NONE',  ( -15.95292532278785913, -32.11873716947361856, 68.00000000000000000 ) ) ;
#17722=AXIS2_PLACEMENT_3D ( 'NONE', #1767, #13938, #20567 ) ;
#17727=ORIENTED_EDGE ( 'NONE', *, *, #14189, .T. ) ;
#17728=DIRECTION ( 'NONE',  ( -1.000000000000000000, 0.000000000000000000, 0.000000000000000000 ) ) ;
#17729=VECTOR ( 'NONE', #21742, 1000.000000000000000 ) ;
#17730=CARTESIAN_POINT ( 'NONE',  ( 18.22752199202934520, -50.11873716947361856, 13.50000000000000000 ) ) ;
#17731=CARTESIAN_POINT ( 'NONE',  ( 30.67540678000428045, 6.000000000000000000, 3.500000000000000000 ) ) ;
#17733=CARTESIAN_POINT ( 'NONE',  ( 9.141460742840918030, 33.43424481021354921, 42.50000000000000000 ) ) ;
#17735=ORIENTED_EDGE ( 'NONE', *, *, #3341, .F. ) ;
#17736=DIRECTION ( 'NONE',  ( 0.000000000000000000, 0.000000000000000000, -1.000000000000000000 ) ) ;
#17737=EDGE_CURVE ( 'NONE', #19665, #5001, #20324, .T. ) ;
#17738=CARTESIAN_POINT ( 'NONE',  ( -14.96174975910704852, 41.81054587065082728, 13.62426406871192697 ) ) ;
#17740=CARTESIAN_POINT ( 'NONE',  ( 24.13662752439704917, 0.000000000000000000, 7.200000000000000178 ) ) ;
#17741=ORIENTED_EDGE ( 'NONE', *, *, #4758, .T. ) ;
#17743=AXIS2_PLACEMENT_3D ( 'NONE', #20430, #18854, #7115 ) ;
#17744=AXIS2_PLACEMENT_3D ( 'NONE', #4436, #11247, #18071 ) ;
#17745=CARTESIAN_POINT ( 'NONE',  ( -29.20000000000002061, 0.000000000000000000, 0.2999999999999947153 ) ) ;
#17747=ORIENTED_EDGE ( 'NONE', *, *, #18806, .F. ) ;
#17749=CARTESIAN_POINT ( 'NONE',  ( -31.50000000000002132, -71.00000000000001421, 3.500000000000000000 ) ) ;
#17750=ORIENTED_EDGE ( 'NONE', *, *, #401, .F. ) ;
#17752=VERTEX_POINT ( 'NONE', #12405 ) ;
#17753=DIRECTION ( 'NONE',  ( 1.000000000000000000, -1.334402673828314029E-15, 0.000000000000000000 ) ) ;
#17756=EDGE_CURVE ( 'NONE', #21336, #11610, #9607, .T. ) ;
#17758=EDGE_CURVE ( 'NONE', #8119, #5089, #12084, .T. ) ;
#17759=VERTEX_POINT ( 'NONE', #3603 ) ;
#17760=VECTOR ( 'NONE', #6724, 1000.000000000000000 ) ;
#17761=AXIS2_PLACEMENT_3D ( 'NONE', #2393, #12561, #19630 ) ;
#17762=ORIENTED_EDGE ( 'NONE', *, *, #17137, .F. ) ;
#17764=VECTOR ( 'NONE', #8670, 1000.000000000000000 ) ;
#17768=CARTESIAN_POINT ( 'NONE',  ( 0.000000000000000000, 4.700000000000000178, 3.500000000000000000 ) ) ;
#17771=CARTESIAN_POINT ( 'NONE',  ( 9.141460742840918030, -32.61873716947361856, 42.50000000000000000 ) ) ;
#17774=AXIS2_PLACEMENT_3D ( 'NONE', #20143, #14987, #4924 ) ;
#17776=CARTESIAN_POINT ( 'NONE',  ( 31.50000000000002132, 71.00000000000001421, 3.500000000000000000 ) ) ;
#17777=ORIENTED_EDGE ( 'NONE', *, *, #2656, .F. ) ;
#17779=VERTEX_POINT ( 'NONE', #19139 ) ;
#17781=ORIENTED_EDGE ( 'NONE', *, *, #3251, .T. ) ;
#17782=TOROIDAL_SURFACE ( 'NONE', #17417, 0.7000000000000000666, 0.2999999999999999889 ) ;
#17783=AXIS2_PLACEMENT_3D ( 'NONE', #7018, #1951, #15397 ) ;
#17786=ORIENTED_EDGE ( 'NONE', *, *, #5557, .F. ) ;
#17787=ORIENTED_EDGE ( 'NONE', *, *, #1416, .F. ) ;
#17789=DIRECTION ( 'NONE',  ( 0.000000000000000000, 1.000000000000000000, 0.000000000000000000 ) ) ;
#17791=CARTESIAN_POINT ( 'NONE',  ( -17.95292532278785913, 38.74634676501045760, 109.6002446535588319 ) ) ;
#17797=CIRCLE ( 'NONE', #2061, 0.2999999999999999334 ) ;
#17798=CIRCLE ( 'NONE', #17433, 0.2500000000000002220 ) ;
#17799=CARTESIAN_POINT ( 'NONE',  ( -15.95292532278785913, 32.11873716947361856, 68.00000000000000000 ) ) ;
#17800=CIRCLE ( 'NONE', #11716, 0.2999999999999999334 ) ;
#17805=CARTESIAN_POINT ( 'NONE',  ( 17.95292532278785913, -38.74634676501046471, 42.50000000000000711 ) ) ;
#17807=ORIENTED_EDGE ( 'NONE', *, *, #19626, .F. ) ;
#17808=VERTEX_POINT ( 'NONE', #19580 ) ;
#17813=CIRCLE ( 'NONE', #17453, 4.999999999999997335 ) ;
#17814=CARTESIAN_POINT ( 'NONE',  ( 14.66918479711007706, -51.92478806352735887, 13.50000000000000000 ) ) ;
#17815=CARTESIAN_POINT ( 'NONE',  ( 25.37540678000427263, 63.74634676501045050, 13.19999999999999929 ) ) ;
#17820=CARTESIAN_POINT ( 'NONE',  ( -28.64417692495746692, 6.713479613976641502, 13.50000000000000000 ) ) ;
#17822=DIRECTION ( 'NONE',  ( 2.832483164223434527E-16, -1.000000000000000000, 0.000000000000000000 ) ) ;
#17823=CIRCLE ( 'NONE', #8915, 0.2999999999999999334 ) ;
#17826=CARTESIAN_POINT ( 'NONE',  ( -29.20000000000002061, -68.70000000000001705, 0.000000000000000000 ) ) ;
#17827=CARTESIAN_POINT ( 'NONE',  ( 25.37540678000427263, 69.04634676501045476, 3.500000000000000000 ) ) ;
#17828=ORIENTED_EDGE ( 'NONE', *, *, #14427, .F. ) ;
#17829=ORIENTED_EDGE ( 'NONE', *, *, #12390, .T. ) ;
#17831=DIRECTION ( 'NONE',  ( 1.000000000000000000, 0.000000000000000000, 0.000000000000000000 ) ) ;
#17832=EDGE_CURVE ( 'NONE', #9069, #13657, #4256, .T. ) ;
#17833=DIRECTION ( 'NONE',  ( 1.000000000000000000, 0.000000000000000000, 0.000000000000000000 ) ) ;
#17834=ADVANCED_FACE ( 'NONE', ( #16540 ), #2673, .T. ) ;
#17835=ORIENTED_EDGE ( 'NONE', *, *, #14689, .F. ) ;
#17836=ADVANCED_FACE ( 'NONE', ( #14413 ), #14315, .T. ) ;
#17838=ADVANCED_FACE ( 'NONE', ( #16313 ), #11407, .T. ) ;
#17839=AXIS2_PLACEMENT_3D ( 'NONE', #5079, #239, #20629 ) ;
#17840=AXIS2_PLACEMENT_3D ( 'NONE', #528, #10742, #17560 ) ;
#17841=VERTEX_POINT ( 'NONE', #18234 ) ;
#17842=DIRECTION ( 'NONE',  ( -1.000000000000000000, 0.000000000000000000, 0.000000000000000000 ) ) ;
#17843=LINE ( 'NONE', #11127, #18823 ) ;
#17844=DIRECTION ( 'NONE',  ( -0.000000000000000000, 1.000000000000000000, -0.000000000000000000 ) ) ;
#17845=DIRECTION ( 'NONE',  ( 1.000000000000000000, 0.000000000000000000, 0.000000000000000000 ) ) ;
#17849=DIRECTION ( 'NONE',  ( 0.000000000000000000, 0.000000000000000000, 1.000000000000000000 ) ) ;
#17850=DIRECTION ( 'NONE',  ( 1.000000000000000000, 0.000000000000000000, 0.000000000000000000 ) ) ;
#17851=EDGE_CURVE ( 'NONE', #16066, #15986, #2798, .T. ) ;
#17852=DIRECTION ( 'NONE',  ( 0.000000000000000000, 1.000000000000000000, 0.000000000000000000 ) ) ;
#17853=CARTESIAN_POINT ( 'NONE',  ( 0.000000000000000000, 68.44634676501046044, 7.500000000000000000 ) ) ;
#17854=ORIENTED_EDGE ( 'NONE', *, *, #4636, .T. ) ;
#17856=CARTESIAN_POINT ( 'NONE',  ( 29.37540678000427619, -4.700000000000000178, 3.799999999999999822 ) ) ;
#17857=VECTOR ( 'NONE', #10266, 1000.000000000000000 ) ;
#17858=ORIENTED_EDGE ( 'NONE', *, *, #21040, .F. ) ;
#17860=CARTESIAN_POINT ( 'NONE',  ( 15.95292532278785913, 50.11873716947361856, 68.00000000000000000 ) ) ;
#17861=LINE ( 'NONE', #6246, #9880 ) ;
#17863=ORIENTED_EDGE ( 'NONE', *, *, #19155, .F. ) ;
#17867=EDGE_CURVE ( 'NONE', #8633, #7269, #7474, .T. ) ;
#17871=CIRCLE ( 'NONE', #17158, 0.2999999999999999334 ) ;
#17872=ORIENTED_EDGE ( 'NONE', *, *, #8146, .F. ) ;
#17873=DIRECTION ( 'NONE',  ( 0.000000000000000000, -0.000000000000000000, -1.000000000000000000 ) ) ;
#17876=FACE_OUTER_BOUND ( 'NONE', #7388, .T. ) ;
#17877=DIRECTION ( 'NONE',  ( 1.000000000000000000, 0.000000000000000000, 0.000000000000000000 ) ) ;
#17884=CARTESIAN_POINT ( 'NONE',  ( 25.37540678000427263, 68.74634676501045760, 7.500000000000000000 ) ) ;
#17885=AXIS2_PLACEMENT_3D ( 'NONE', #7862, #21515, #1119 ) ;
#17886=ORIENTED_EDGE ( 'NONE', *, *, #19403, .T. ) ;
#17887=ORIENTED_EDGE ( 'NONE', *, *, #15105, .T. ) ;
#17888=ORIENTED_EDGE ( 'NONE', *, *, #4099, .T. ) ;
#17889=CARTESIAN_POINT ( 'NONE',  ( 29.50000000000002132, 69.00000000000000000, -150.0833101980363722 ) ) ;
#17890=EDGE_CURVE ( 'NONE', #19133, #18309, #7622, .T. ) ;
#17891=ORIENTED_EDGE ( 'NONE', *, *, #9474, .F. ) ;
#17895=ORIENTED_EDGE ( 'NONE', *, *, #2157, .T. ) ;
#17896=CARTESIAN_POINT ( 'NONE',  ( 25.37540678000427263, 68.44634676501046044, 7.200000000000000178 ) ) ;
#17897=VECTOR ( 'NONE', #8691, 1000.000000000000000 ) ;
#17898=ORIENTED_EDGE ( 'NONE', *, *, #22110, .T. ) ;
#17899=CARTESIAN_POINT ( 'NONE',  ( 25.37540678000427263, -63.74634676501045050, 7.500000000000000000 ) ) ;
#17900=CARTESIAN_POINT ( 'NONE',  ( -29.50000000000002132, 69.00000000000000000, 0.2999999999999947153 ) ) ;
#17901=DIRECTION ( 'NONE',  ( 1.000000000000000000, 0.000000000000000000, 0.000000000000000000 ) ) ;
#17904=EDGE_CURVE ( 'NONE', #3783, #9842, #1110, .T. ) ;
#17907=DIRECTION ( 'NONE',  ( -0.000000000000000000, -0.000000000000000000, 1.000000000000000000 ) ) ;
#17908=EDGE_CURVE ( 'NONE', #20038, #21627, #10961, .T. ) ;
#17909=CARTESIAN_POINT ( 'NONE',  ( -4.127054932750482408, -33.43424481021354921, 68.50000000000000000 ) ) ;
#17910=CARTESIAN_POINT ( 'NONE',  ( -8.641460742840918030, 33.43424481021354921, 13.50000000000000000 ) ) ;
#17911=DIRECTION ( 'NONE',  ( 1.000000000000000000, 0.000000000000000000, 0.000000000000000000 ) ) ;
#17912=VECTOR ( 'NONE', #16698, 1000.000000000000000 ) ;
#17913=DIRECTION ( 'NONE',  ( 0.000000000000000000, 0.000000000000000000, 1.000000000000000000 ) ) ;
#17916=DIRECTION ( 'NONE',  ( 0.000000000000000000, 0.000000000000000000, 1.000000000000000000 ) ) ;
#17918=CARTESIAN_POINT ( 'NONE',  ( 0.000000000000000000, -52.11873716947361856, 109.6002446535588319 ) ) ;
#17919=EDGE_LOOP ( 'NONE', ( #8829, #8210, #12848, #14172 ) ) ;
#17920=ORIENTED_EDGE ( 'NONE', *, *, #19688, .F. ) ;
#17921=EDGE_CURVE ( 'NONE', #421, #21336, #12743, .T. ) ;
#17924=CYLINDRICAL_SURFACE ( 'NONE', #8531, 0.2999999999999999334 ) ;
#17926=CIRCLE ( 'NONE', #1498, 0.5000000000000000000 ) ;
#17929=ORIENTED_EDGE ( 'NONE', *, *, #17291, .F. ) ;
#17931=ADVANCED_FACE ( 'NONE', ( #21610 ), #21360, .T. ) ;
#17932=EDGE_CURVE ( 'NONE', #9735, #16845, #16095, .T. ) ;
#17933=CARTESIAN_POINT ( 'NONE',  ( -29.13662752439705272, 0.000000000000000000, 3.500000000000000000 ) ) ;
#17937=VERTEX_POINT ( 'NONE', #18563 ) ;
#17939=DIRECTION ( 'NONE',  ( 1.000000000000000000, 0.000000000000000000, 0.000000000000000000 ) ) ;
#17942=VERTEX_POINT ( 'NONE', #8178 ) ;
#17943=CARTESIAN_POINT ( 'NONE',  ( 15.05356361075494576, 52.05881965543597545, 13.87239990309209503 ) ) ;
#17944=AXIS2_PLACEMENT_3D ( 'NONE', #326, #5730, #1896 ) ;
#17945=CARTESIAN_POINT ( 'NONE',  ( 15.21174975910705918, 52.39333383871510108, 13.79999999999999893 ) ) ;
#17949=EDGE_CURVE ( 'NONE', #9183, #7977, #13636, .T. ) ;
#17951=PLANE ( 'NONE',  #2548 ) ;
#17952=PLANE ( 'NONE',  #2785 ) ;
#17954=CARTESIAN_POINT ( 'NONE',  ( 23.02398829872513630, -2.624937972534827413, 13.63083126556636593 ) ) ;
#17956=CARTESIAN_POINT ( 'NONE',  ( 9.641460742840918030, 32.61873716947361856, 68.50000000000000000 ) ) ;
#17957=FACE_OUTER_BOUND ( 'NONE', #15093, .T. ) ;
#17959=DIRECTION ( 'NONE',  ( 1.000000000000000000, 0.000000000000000000, 0.000000000000000000 ) ) ;
#17960=DIRECTION ( 'NONE',  ( -2.388292521039847891E-16, -0.000000000000000000, -1.000000000000000000 ) ) ;
#17961=ADVANCED_FACE ( 'NONE', ( #20244 ), #10173, .T. ) ;
#17962=EDGE_CURVE ( 'NONE', #21143, #20337, #8502, .T. ) ;
#17964=DIRECTION ( 'NONE',  ( 1.000000000000000000, 0.000000000000000000, 0.000000000000000000 ) ) ;
#17966=VERTEX_POINT ( 'NONE', #4701 ) ;
#17968=ORIENTED_EDGE ( 'NONE', *, *, #5382, .T. ) ;
#17969=LINE ( 'NONE', #1077, #16604 ) ;
#17971=ORIENTED_EDGE ( 'NONE', *, *, #21612, .T. ) ;
#17973=CARTESIAN_POINT ( 'NONE',  ( -31.50000000000002132, -71.70000000000001705, 3.200000000000000178 ) ) ;
#17974=CARTESIAN_POINT ( 'NONE',  ( -31.50000000000002132, 71.00000000000001421, 1.800000000000000044 ) ) ;
#17976=ORIENTED_EDGE ( 'NONE', *, *, #17832, .F. ) ;
#17977=EDGE_CURVE ( 'NONE', #5468, #21585, #14418, .T. ) ;
#17978=EDGE_LOOP ( 'NONE', ( #3676, #12952, #21827, #6086, #16170, #2202 ) ) ;
#17981=DIRECTION ( 'NONE',  ( 3.052134192567367925E-16, 1.000000000000000000, -0.000000000000000000 ) ) ;
#17982=DIRECTION ( 'NONE',  ( -0.000000000000000000, 1.000000000000000000, 0.000000000000000000 ) ) ;
#17983=CARTESIAN_POINT ( 'NONE',  ( 9.141460742840918030, -33.43424481021354921, 68.00000000000000000 ) ) ;
#17985=ADVANCED_FACE ( 'NONE', ( #11512 ), #10974, .F. ) ;
#17986=EDGE_CURVE ( 'NONE', #16569, #9928, #8702, .T. ) ;
#17992=DIRECTION ( 'NONE',  ( -0.000000000000000000, 0.000000000000000000, 1.000000000000000000 ) ) ;
#17993=LINE ( 'NONE', #1199, #8899 ) ;
#17994=DIRECTION ( 'NONE',  ( -0.000000000000000000, -1.000000000000000000, 0.000000000000000000 ) ) ;
#17995=CIRCLE ( 'NONE', #12631, 0.5000000000000004441 ) ;
#17997=ORIENTED_EDGE ( 'NONE', *, *, #19738, .F. ) ;
#17998=DIRECTION ( 'NONE',  ( 0.000000000000000000, 0.000000000000000000, 1.000000000000000000 ) ) ;
#17999=ADVANCED_FACE ( 'NONE', ( #15090 ), #7412, .F. ) ;
#18001=ORIENTED_EDGE ( 'NONE', *, *, #21477, .F. ) ;
#18004=ADVANCED_FACE ( 'NONE', ( #5037 ), #4805, .T. ) ;
#18007=DIRECTION ( 'NONE',  ( -0.000000000000000000, 1.000000000000000000, -0.000000000000000000 ) ) ;
#18009=CARTESIAN_POINT ( 'NONE',  ( 29.13662752439705272, -5.299999999999999822, 7.500000000000000000 ) ) ;
#18013=ADVANCED_FACE ( 'NONE', ( #3128 ), #6703, .T. ) ;
#18015=CARTESIAN_POINT ( 'NONE',  ( 27.67540678000427690, 10.94079601157914539, 13.50000000000000000 ) ) ;
#18016=DIRECTION ( 'NONE',  ( 1.000000000000000000, 0.000000000000000000, 0.000000000000000000 ) ) ;
#18018=CARTESIAN_POINT ( 'NONE',  ( 29.37540678000427619, 5.000000000000000000, 7.500000000000000000 ) ) ;
#18019=CARTESIAN_POINT ( 'NONE',  ( 27.37540678000427619, 5.683640910026986681, 42.50000000000000000 ) ) ;
#18025=EDGE_CURVE ( 'NONE', #21063, #15844, #7758, .T. ) ;
#18028=CIRCLE ( 'NONE', #9841, 5.300000000000006040 ) ;
#18032=VERTEX_POINT ( 'NONE', #1781 ) ;
#18033=CARTESIAN_POINT ( 'NONE',  ( 18.05178606074127501, -38.87061083372239523, 13.49999999999999822 ) ) ;
#18034=DIRECTION ( 'NONE',  ( -0.000000000000000000, -0.000000000000000000, -1.000000000000000000 ) ) ;
#18035=CARTESIAN_POINT ( 'NONE',  ( 15.06741964789885024, 51.94542257242142824, 13.49999999999999645 ) ) ;
#18036=DIRECTION ( 'NONE',  ( 1.000000000000000000, 0.000000000000000000, 0.000000000000000000 ) ) ;
#18037=CARTESIAN_POINT ( 'NONE',  ( 27.37540678000427619, 7.754037881813018962E-15, 42.50000000000000000 ) ) ;
#18038=ORIENTED_EDGE ( 'NONE', *, *, #14394, .T. ) ;
#18039=DIRECTION ( 'NONE',  ( 0.000000000000000000, 1.000000000000000000, 0.000000000000000000 ) ) ;
#18040=CARTESIAN_POINT ( 'NONE',  ( -29.13662752439705272, 0.000000000000000000, 13.19999999999999929 ) ) ;
#18041=ORIENTED_EDGE ( 'NONE', *, *, #446, .F. ) ;
#18050=ORIENTED_EDGE ( 'NONE', *, *, #19215, .F. ) ;
#18051=DIRECTION ( 'NONE',  ( 1.000000000000000000, 0.000000000000000000, 0.000000000000000000 ) ) ;
#18053=DIRECTION ( 'NONE',  ( 1.000000000000000000, -0.000000000000000000, 0.000000000000000000 ) ) ;
#18054=CARTESIAN_POINT ( 'NONE',  ( 9.141460742840918030, -32.11873716947361856, 68.00000000000000000 ) ) ;
#18055=DIRECTION ( 'NONE',  ( 1.000000000000000000, 0.000000000000000000, 0.000000000000000000 ) ) ;
#18058=VECTOR ( 'NONE', #7227, 1000.000000000000000 ) ;
#18063=CARTESIAN_POINT ( 'NONE',  ( -23.02398829872514341, -5.683640910026986681, 42.50000000000000000 ) ) ;
#18065=DIRECTION ( 'NONE',  ( 1.000000000000000000, 0.000000000000000000, -0.000000000000000000 ) ) ;
#18066=VERTEX_POINT ( 'NONE', #8620 ) ;
#18069=ORIENTED_EDGE ( 'NONE', *, *, #18957, .T. ) ;
#18070=DIRECTION ( 'NONE',  ( 0.000000000000000000, -0.000000000000000000, -1.000000000000000000 ) ) ;
#18071=DIRECTION ( 'NONE',  ( 0.000000000000000000, 0.000000000000000000, 1.000000000000000000 ) ) ;
#18075=AXIS2_PLACEMENT_3D ( 'NONE', #5748, #3946, #12417 ) ;
#18077=DIRECTION ( 'NONE',  ( 0.1868663427273192512, -0.9823853469773029534, 0.000000000000000000 ) ) ;
#18079=CARTESIAN_POINT ( 'NONE',  ( -23.32398829872514057, 2.157133568460765538, 7.500000000000000000 ) ) ;
#18081=AXIS2_PLACEMENT_3D ( 'NONE', #18511, #11677, #11898 ) ;
#18083=ADVANCED_FACE ( 'NONE', ( #16654 ), #20263, .T. ) ;
#18084=EDGE_LOOP ( 'NONE', ( #13154, #957, #13986, #2517 ) ) ;
#18086=DIRECTION ( 'NONE',  ( -0.000000000000000000, -0.000000000000000000, -1.000000000000000000 ) ) ;
#18087=LINE ( 'NONE', #6593, #265 ) ;
#18090=VECTOR ( 'NONE', #9697, 1000.000000000000000 ) ;
#18092=DIRECTION ( 'NONE',  ( 0.000000000000000000, -0.000000000000000000, 1.000000000000000000 ) ) ;
#18094=DIRECTION ( 'NONE',  ( 0.000000000000000000, 0.000000000000000000, 1.000000000000000000 ) ) ;
#18095=FACE_OUTER_BOUND ( 'NONE', #17340, .T. ) ;
#18096=CARTESIAN_POINT ( 'NONE',  ( 9.641460742840918030, 32.61873716947361856, 42.50000000000000711 ) ) ;
#18097=DIRECTION ( 'NONE',  ( -0.000000000000000000, -0.000000000000000000, -1.000000000000000000 ) ) ;
#18098=VERTEX_POINT ( 'NONE', #2916 ) ;
#18099=LINE ( 'NONE', #16533, #13037 ) ;
#18100=CIRCLE ( 'NONE', #7045, 1.299999999999999156 ) ;
#18102=CARTESIAN_POINT ( 'NONE',  ( -30.67540678000428045, 63.74634676501045050, 3.500000000000000000 ) ) ;
#18105=LINE ( 'NONE', #9736, #2087 ) ;
#18108=TOROIDAL_SURFACE ( 'NONE', #14174, 4.051418481279137396, 0.2999999999999999889 ) ;
#18110=AXIS2_PLACEMENT_3D ( 'NONE', #1851, #18867, #13920 ) ;
#18114=EDGE_CURVE ( 'NONE', #8248, #1905, #21725, .T. ) ;
#18116=ORIENTED_EDGE ( 'NONE', *, *, #2252, .T. ) ;
#18117=CARTESIAN_POINT ( 'NONE',  ( -9.141460742840918030, 32.61873716947361856, 42.50000000000000000 ) ) ;
#18118=ADVANCED_FACE ( 'NONE', ( #6513 ), #13105, .T. ) ;
#18119=ORIENTED_EDGE ( 'NONE', *, *, #2764, .F. ) ;
#18120=DIRECTION ( 'NONE',  ( 1.000000000000000000, 0.000000000000000000, 0.000000000000000000 ) ) ;
#18121=ORIENTED_EDGE ( 'NONE', *, *, #20709, .F. ) ;
#18123=LINE ( 'NONE', #9640, #21327 ) ;
#18125=AXIS2_PLACEMENT_3D ( 'NONE', #21694, #20123, #18319 ) ;
#18127=DIRECTION ( 'NONE',  ( -0.000000000000000000, -0.000000000000000000, -1.000000000000000000 ) ) ;
#18130=CARTESIAN_POINT ( 'NONE',  ( 8.641460742840918030, 33.93424481021354921, 68.00000000000000000 ) ) ;
#18132=DIRECTION ( 'NONE',  ( 1.000000000000000000, 0.000000000000000000, 0.000000000000000000 ) ) ;
#18133=FACE_OUTER_BOUND ( 'NONE', #10239, .T. ) ;
#18134=VECTOR ( 'NONE', #4974, 1000.000000000000000 ) ;
#18135=VECTOR ( 'NONE', #14552, 1000.000000000000000 ) ;
#18136=ORIENTED_EDGE ( 'NONE', *, *, #7247, .T. ) ;
#18137=DIRECTION ( 'NONE',  ( -0.000000000000000000, -0.000000000000000000, -1.000000000000000000 ) ) ;
#18138=DIRECTION ( 'NONE',  ( -0.000000000000000000, 0.000000000000000000, 1.000000000000000000 ) ) ;
#18140=ORIENTED_EDGE ( 'NONE', *, *, #21177, .F. ) ;
#18143=EDGE_CURVE ( 'NONE', #18524, #17779, #11518, .T. ) ;
#18144=VECTOR ( 'NONE', #20890, 1000.000000000000000 ) ;
#18147=AXIS2_PLACEMENT_3D ( 'NONE', #11954, #8389, #13738 ) ;
#18148=VECTOR ( 'NONE', #1132, 1000.000000000000000 ) ;
#18149=ORIENTED_EDGE ( 'NONE', *, *, #16694, .F. ) ;
#18150=VECTOR ( 'NONE', #8708, 1000.000000000000000 ) ;
#18151=CARTESIAN_POINT ( 'NONE',  ( 15.21174975910706095, -52.00603550409435627, 13.50000000000000000 ) ) ;
#18152=DIRECTION ( 'NONE',  ( -0.000000000000000000, 1.000000000000000000, 0.000000000000000000 ) ) ;
#18155=DIRECTION ( 'NONE',  ( -0.000000000000000000, -0.000000000000000000, -1.000000000000000000 ) ) ;
#18158=VECTOR ( 'NONE', #745, 1000.000000000000000 ) ;
#18160=EDGE_CURVE ( 'NONE', #15453, #13909, #20641, .T. ) ;
#18162=DIRECTION ( 'NONE',  ( -0.000000000000000000, 1.000000000000000000, -0.000000000000000000 ) ) ;
#18164=ADVANCED_FACE ( 'NONE', ( #16320 ), #4473, .T. ) ;
#18165=AXIS2_PLACEMENT_3D ( 'NONE', #12585, #16052, #7582 ) ;
#18168=VERTEX_POINT ( 'NONE', #9847 ) ;
#18169=VECTOR ( 'NONE', #20831, 1000.000000000000000 ) ;
#18171=DIRECTION ( 'NONE',  ( -0.000000000000000000, 0.000000000000000000, 1.000000000000000000 ) ) ;
#18173=DIRECTION ( 'NONE',  ( 2.388292521039847891E-16, 0.000000000000000000, 1.000000000000000000 ) ) ;
#18174=VERTEX_POINT ( 'NONE', #9964 ) ;
#18178=CARTESIAN_POINT ( 'NONE',  ( 4.127054932750481520, -33.43424481021354921, 42.50000000000000000 ) ) ;
#18179=AXIS2_PLACEMENT_3D ( 'NONE', #19004, #7149, #20471 ) ;
#18180=DIRECTION ( 'NONE',  ( 0.000000000000000000, 1.000000000000000000, 0.000000000000000000 ) ) ;
#18182=DIRECTION ( 'NONE',  ( 0.000000000000000000, 0.000000000000000000, -1.000000000000000000 ) ) ;
#18183=AXIS2_PLACEMENT_3D ( 'NONE', #6794, #18297, #4658 ) ;
#18184=DIRECTION ( 'NONE',  ( 1.000000000000000000, 0.000000000000000000, -0.000000000000000000 ) ) ;
#18185=CARTESIAN_POINT ( 'NONE',  ( 0.000000000000000000, 4.700000000000000178, 3.799999999999999822 ) ) ;
#18186=ORIENTED_EDGE ( 'NONE', *, *, #16359, .F. ) ;
#18188=CARTESIAN_POINT ( 'NONE',  ( 29.37540678000427619, 6.000000000000000000, 7.500000000000000000 ) ) ;
#18189=VECTOR ( 'NONE', #5929, 1000.000000000000000 ) ;
#18193=ORIENTED_EDGE ( 'NONE', *, *, #3389, .F. ) ;
#18199=LINE ( 'NONE', #9258, #7039 ) ;
#18203=VERTEX_POINT ( 'NONE', #6614 ) ;
#18204=CARTESIAN_POINT ( 'NONE',  ( -15.04741597961255728, 51.92573430214628871, 13.50000000000006750 ) ) ;
#18205=DIRECTION ( 'NONE',  ( 1.000000000000000000, 0.000000000000000000, 0.000000000000000000 ) ) ;
#18207=AXIS2_PLACEMENT_3D ( 'NONE', #21943, #6620, #6738 ) ;
#18208=ORIENTED_EDGE ( 'NONE', *, *, #17291, .T. ) ;
#18211=CARTESIAN_POINT ( 'NONE',  ( -14.96174975910705207, -41.81054587065082728, 13.79999999999999893 ) ) ;
#18212=CARTESIAN_POINT ( 'NONE',  ( -23.10708008847558403, -2.595912616485783975, 13.38952209624200762 ) ) ;
#18213=DIRECTION ( 'NONE',  ( 0.000000000000000000, -1.000000000000000000, 0.000000000000000000 ) ) ;
#18214=EDGE_CURVE ( 'NONE', #13600, #20804, #3477, .T. ) ;
#18215=CYLINDRICAL_SURFACE ( 'NONE', #13904, 3.500000000000003109 ) ;
#18216=LINE ( 'NONE', #19789, #19731 ) ;
#18222=LINE ( 'NONE', #15081, #17446 ) ;
#18224=CARTESIAN_POINT ( 'NONE',  ( 15.95292532278785913, 52.39333383871510108, 13.79999999999999716 ) ) ;
#18226=ADVANCED_FACE ( 'NONE', ( #12168 ), #10301, .T. ) ;
#18229=ORIENTED_EDGE ( 'NONE', *, *, #6505, .F. ) ;
#18230=FACE_OUTER_BOUND ( 'NONE', #13003, .T. ) ;
#18232=ORIENTED_EDGE ( 'NONE', *, *, #18554, .T. ) ;
#18234=CARTESIAN_POINT ( 'NONE',  ( 27.67540678000427690, -10.94079601157914716, 13.50000000000000000 ) ) ;
#18235=CIRCLE ( 'NONE', #21109, 0.5000000000000000000 ) ;
#18237=EDGE_CURVE ( 'NONE', #2211, #252, #2395, .T. ) ;
#18238=DIRECTION ( 'NONE',  ( 0.000000000000000000, 0.000000000000000000, 1.000000000000000000 ) ) ;
#18239=DIRECTION ( 'NONE',  ( 0.000000000000000000, 0.000000000000000000, -1.000000000000000000 ) ) ;
#18245=EDGE_CURVE ( 'NONE', #3327, #17367, #19554, .T. ) ;
#18247=EDGE_CURVE ( 'NONE', #13733, #2108, #4926, .T. ) ;
#18249=CARTESIAN_POINT ( 'NONE',  ( 25.37540678000427263, -67.54634676501045476, 7.799999999999999822 ) ) ;
#18251=CARTESIAN_POINT ( 'NONE',  ( -27.37540678000427619, 5.683640910026986681, 13.79999999999999893 ) ) ;
#18255=ORIENTED_EDGE ( 'NONE', *, *, #21702, .T. ) ;
#18260=ORIENTED_EDGE ( 'NONE', *, *, #2961, .F. ) ;
#18264=ORIENTED_EDGE ( 'NONE', *, *, #9356, .T. ) ;
#18265=CARTESIAN_POINT ( 'NONE',  ( 15.12813070831323969, -51.99253567353609640, 13.49999999999999822 ) ) ;
#18267=ORIENTED_EDGE ( 'NONE', *, *, #5227, .T. ) ;
#18268=DIRECTION ( 'NONE',  ( -0.000000000000000000, -0.000000000000000000, -1.000000000000000000 ) ) ;
#18273=EDGE_CURVE ( 'NONE', #19672, #2805, #13481, .T. ) ;
#18275=CARTESIAN_POINT ( 'NONE',  ( -23.04709339880125185, 2.285361808764050817, 13.25160309052396279 ) ) ;
#18277=CARTESIAN_POINT ( 'NONE',  ( -23.04273156199908357, 2.261510999192738680, 13.19999999999999929 ) ) ;
#18279=EDGE_LOOP ( 'NONE', ( #10225, #7212 ) ) ;
#18280=EDGE_LOOP ( 'NONE', ( #8559, #9120, #901, #15872 ) ) ;
#18281=FACE_OUTER_BOUND ( 'NONE', #1232, .T. ) ;
#18282=LINE ( 'NONE', #13459, #9606 ) ;
#18286=AXIS2_PLACEMENT_3D ( 'NONE', #7200, #682, #9085 ) ;
#18287=VECTOR ( 'NONE', #5845, 1000.000000000000000 ) ;
#18288=TOROIDAL_SURFACE ( 'NONE', #8659, 0.2500000000000000000, 0.2500000000000000000 ) ;
#18293=CARTESIAN_POINT ( 'NONE',  ( -15.95292532278785913, -50.11873716947361856, 68.50000000000000000 ) ) ;
#18294=CARTESIAN_POINT ( 'NONE',  ( 17.45292532278785913, -34.11873716947361856, 68.50000000000000000 ) ) ;
#18295=ORIENTED_EDGE ( 'NONE', *, *, #1494, .T. ) ;
#18297=DIRECTION ( 'NONE',  ( 1.000000000000000000, 0.000000000000000000, 0.000000000000000000 ) ) ;
#18298=CARTESIAN_POINT ( 'NONE',  ( 25.37540678000427263, 68.74634676501045760, 3.799999999999999822 ) ) ;
#18300=ORIENTED_EDGE ( 'NONE', *, *, #2347, .T. ) ;
#18301=DIRECTION ( 'NONE',  ( 0.000000000000000000, 0.000000000000000000, -1.000000000000000000 ) ) ;
#18302=DIRECTION ( 'NONE',  ( -0.000000000000000000, -1.000000000000000000, -0.000000000000000000 ) ) ;
#18307=VECTOR ( 'NONE', #13825, 1000.000000000000000 ) ;
#18308=DIRECTION ( 'NONE',  ( 0.000000000000000000, -1.000000000000000000, 0.000000000000000000 ) ) ;
#18309=VERTEX_POINT ( 'NONE', #20813 ) ;
#18311=VERTEX_POINT ( 'NONE', #5379 ) ;
#18312=CARTESIAN_POINT ( 'NONE',  ( -29.37573593128808369, 68.87573593128806237, -5.214931150217776400E-15 ) ) ;
#18314=DIRECTION ( 'NONE',  ( -1.000000000000000000, -0.000000000000000000, 0.000000000000000000 ) ) ;
#18316=AXIS2_PLACEMENT_3D ( 'NONE', #5308, #15356, #20409 ) ;
#18318=EDGE_CURVE ( 'NONE', #2078, #21878, #22080, .T. ) ;
#18319=DIRECTION ( 'NONE',  ( 0.000000000000000000, 0.000000000000000000, 1.000000000000000000 ) ) ;
#18321=ADVANCED_FACE ( 'NONE', ( #4796 ), #10630, .T. ) ;
#18324=ORIENTED_EDGE ( 'NONE', *, *, #6936, .T. ) ;
#18325=CARTESIAN_POINT ( 'NONE',  ( -28.57540678000427548, 6.494748934539263274, 13.50000000000000000 ) ) ;
#18326=DIRECTION ( 'NONE',  ( 0.000000000000000000, 1.000000000000000000, 0.000000000000000000 ) ) ;
#18331=CARTESIAN_POINT ( 'NONE',  ( -15.95292532278785913, -51.61873716947361856, 68.50000000000000000 ) ) ;
#18333=FACE_OUTER_BOUND ( 'NONE', #4703, .T. ) ;
#18335=ORIENTED_EDGE ( 'NONE', *, *, #7176, .T. ) ;
#18336=EDGE_CURVE ( 'NONE', #17454, #1239, #18790, .T. ) ;
#18337=ORIENTED_EDGE ( 'NONE', *, *, #16448, .T. ) ;
#18338=CARTESIAN_POINT ( 'NONE',  ( 29.48732456384755807, -2.488184534793062674, 0.2032168635956394243 ) ) ;
#18339=ORIENTED_EDGE ( 'NONE', *, *, #17159, .T. ) ;
#18340=EDGE_CURVE ( 'NONE', #21627, #14858, #11335, .T. ) ;
#18342=DIRECTION ( 'NONE',  ( -0.000000000000000000, -0.000000000000000000, -1.000000000000000000 ) ) ;
#18346=CARTESIAN_POINT ( 'NONE',  ( 23.05999184077136377, 2.354728237135330637, 13.30000967910994092 ) ) ;
#18349=CARTESIAN_POINT ( 'NONE',  ( -14.96174975910705207, -51.83071861726173779, 13.82019355104894309 ) ) ;
#18350=DIRECTION ( 'NONE',  ( 0.000000000000000000, 0.000000000000000000, -1.000000000000000000 ) ) ;
#18360=ORIENTED_EDGE ( 'NONE', *, *, #18558, .T. ) ;
#18364=ORIENTED_EDGE ( 'NONE', *, *, #8479, .T. ) ;
#18366=ORIENTED_EDGE ( 'NONE', *, *, #8597, .T. ) ;
#18367=ADVANCED_FACE ( 'NONE', ( #5043 ), #19939, .T. ) ;
#18370=DIRECTION ( 'NONE',  ( 1.000000000000000000, 0.000000000000000000, 0.000000000000000000 ) ) ;
#18371=ORIENTED_EDGE ( 'NONE', *, *, #6402, .F. ) ;
#18372=LINE ( 'NONE', #9884, #11076 ) ;
#18375=DIRECTION ( 'NONE',  ( -0.000000000000000000, -0.000000000000000000, -1.000000000000000000 ) ) ;
#18376=EDGE_CURVE ( 'NONE', #21328, #18168, #15270, .T. ) ;
#18377=DIRECTION ( 'NONE',  ( 0.000000000000000000, 0.000000000000000000, 1.000000000000000000 ) ) ;
#18378=EDGE_LOOP ( 'NONE', ( #18954, #4140, #639, #19045 ) ) ;
#18379=EDGE_LOOP ( 'NONE', ( #5813, #301, #6696, #14412 ) ) ;
#18385=ADVANCED_FACE ( 'NONE', ( #14501 ), #5594, .F. ) ;
#18389=CARTESIAN_POINT ( 'NONE',  ( 25.37540678000427263, -66.94634676501046044, 13.50000000000000000 ) ) ;
#18390=DIRECTION ( 'NONE',  ( 0.000000000000000000, 0.000000000000000000, 1.000000000000000000 ) ) ;
#18391=ADVANCED_FACE ( 'NONE', ( #16077 ), #4024, .T. ) ;
#18392=CARTESIAN_POINT ( 'NONE',  ( 23.02398829872515051, -3.003070052962832026, 13.75712488064577599 ) ) ;
#18393=CARTESIAN_POINT ( 'NONE',  ( 30.07540678000427548, 0.000000000000000000, 7.200000000000000178 ) ) ;
#18395=CARTESIAN_POINT ( 'NONE',  ( -27.37540678000427619, 5.683640910026986681, 42.50000000000000000 ) ) ;
#18399=ORIENTED_EDGE ( 'NONE', *, *, #16909, .T. ) ;
#18400=CIRCLE ( 'NONE', #21638, 3.800000000000004707 ) ;
#18403=ORIENTED_EDGE ( 'NONE', *, *, #9201, .F. ) ;
#18406=VERTEX_POINT ( 'NONE', #5720 ) ;
#18414=ORIENTED_EDGE ( 'NONE', *, *, #13185, .T. ) ;
#18415=EDGE_CURVE ( 'NONE', #2490, #8846, #16181, .T. ) ;
#18422=LINE ( 'NONE', #4565, #12395 ) ;
#18423=DIRECTION ( 'NONE',  ( -0.000000000000000000, -1.000000000000000000, 0.000000000000000000 ) ) ;
#18424=CARTESIAN_POINT ( 'NONE',  ( -15.95292532278785913, 32.61873716947361856, 68.00000000000000000 ) ) ;
#18426=CARTESIAN_POINT ( 'NONE',  ( -4.127054932750482408, -32.93424481021354921, 68.00000000000000000 ) ) ;
#18427=ORIENTED_EDGE ( 'NONE', *, *, #12875, .T. ) ;
#18431=EDGE_LOOP ( 'NONE', ( #6230, #3880, #1347, #5761 ) ) ;
#18432=VECTOR ( 'NONE', #14377, 1000.000000000000000 ) ;
#18433=DIRECTION ( 'NONE',  ( -0.000000000000000000, 1.000000000000000000, -0.000000000000000000 ) ) ;
#18434=TOROIDAL_SURFACE ( 'NONE', #7729, 1.300000000000000044, 0.2999999999999999889 ) ;
#18435=DIRECTION ( 'NONE',  ( 0.000000000000000000, 0.000000000000000000, -1.000000000000000000 ) ) ;
#18436=EDGE_LOOP ( 'NONE', ( #17422, #610, #4848, #21660 ) ) ;
#18437=CIRCLE ( 'NONE', #551, 6.500000000000002665 ) ;
#18441=CARTESIAN_POINT ( 'NONE',  ( 15.21174975910707161, 51.61873716947361856, 68.50000000000000000 ) ) ;
#18442=VERTEX_POINT ( 'NONE', #5917 ) ;
#18447=VERTEX_POINT ( 'NONE', #19444 ) ;
#18449=CIRCLE ( 'NONE', #17744, 0.3000000000000003775 ) ;
#18451=CARTESIAN_POINT ( 'NONE',  ( -1.836970198721029934E-16, -72.00000000000001421, 1.800000000000000044 ) ) ;
#18453=VECTOR ( 'NONE', #18583, 1000.000000000000000 ) ;
#18454=CARTESIAN_POINT ( 'NONE',  ( 28.87540678000427619, -6.494748934539263274, 13.50000000000000000 ) ) ;
#18456=LINE ( 'NONE', #13417, #10000 ) ;
#18458=CARTESIAN_POINT ( 'NONE',  ( -23.32398829872514057, -5.683640910026986681, 13.79999999999999893 ) ) ;
#18459=DIRECTION ( 'NONE',  ( 1.000000000000000000, 0.000000000000000000, 0.000000000000000000 ) ) ;
#18461=DIRECTION ( 'NONE',  ( -0.000000000000000000, -0.000000000000000000, -1.000000000000000000 ) ) ;
#18463=AXIS2_PLACEMENT_3D ( 'NONE', #380, #5549, #20770 ) ;
#18464=ORIENTED_EDGE ( 'NONE', *, *, #19201, .T. ) ;
#18466=DIRECTION ( 'NONE',  ( 0.000000000000000000, -1.000000000000000000, 0.000000000000000000 ) ) ;
#18467=VERTEX_POINT ( 'NONE', #15962 ) ;
#18468=CARTESIAN_POINT ( 'NONE',  ( 29.20000000000002061, 68.70000000000001705, 0.000000000000000000 ) ) ;
#18469=EDGE_CURVE ( 'NONE', #1150, #21455, #10290, .T. ) ;
#18471=VECTOR ( 'NONE', #6920, 1000.000000000000000 ) ;
#18472=ORIENTED_EDGE ( 'NONE', *, *, #20217, .F. ) ;
#18474=ORIENTED_EDGE ( 'NONE', *, *, #149, .F. ) ;
#18475=LINE ( 'NONE', #14672, #12483 ) ;
#18481=CARTESIAN_POINT ( 'NONE',  ( 14.96174975910705740, -51.76873716947361004, 13.50000000000000000 ) ) ;
#18484=CARTESIAN_POINT ( 'NONE',  ( 30.07540678000427548, -63.74634676501045050, 7.500000000000000000 ) ) ;
#18485=CIRCLE ( 'NONE', #22088, 0.2999999999999999334 ) ;
#18486=ORIENTED_EDGE ( 'NONE', *, *, #13912, .T. ) ;
#18488=CYLINDRICAL_SURFACE ( 'NONE', #18316, 0.3000000000000016542 ) ;
#18490=FACE_OUTER_BOUND ( 'NONE', #16169, .T. ) ;
#18491=ADVANCED_FACE ( 'NONE', ( #17438 ), #4240, .T. ) ;
#18493=LINE ( 'NONE', #8762, #2558 ) ;
#18500=ORIENTED_EDGE ( 'NONE', *, *, #8101, .T. ) ;
#18501=AXIS2_PLACEMENT_3D ( 'NONE', #1992, #10412, #4028 ) ;
#18502=DIRECTION ( 'NONE',  ( 0.000000000000000000, 0.000000000000000000, 1.000000000000000000 ) ) ;
#18503=AXIS2_PLACEMENT_3D ( 'NONE', #2260, #12308, #19165 ) ;
#18505=ORIENTED_EDGE ( 'NONE', *, *, #20023, .T. ) ;
#18506=CARTESIAN_POINT ( 'NONE',  ( -3.127054932750481964, 32.61873716947361856, 42.50000000000000711 ) ) ;
#18507=EDGE_CURVE ( 'NONE', #8501, #15453, #14840, .T. ) ;
#18508=CARTESIAN_POINT ( 'NONE',  ( -26.56227312273159313, 9.958410664601840878, 13.79999999999999893 ) ) ;
#18509=AXIS2_PLACEMENT_3D ( 'NONE', #19526, #5794, #10813 ) ;
#18511=CARTESIAN_POINT ( 'NONE',  ( -17.45292532278785913, -50.11873716947361856, 14.00000000000000000 ) ) ;
#18513=CYLINDRICAL_SURFACE ( 'NONE', #17743, 0.5000000000000004441 ) ;
#18515=CARTESIAN_POINT ( 'NONE',  ( 9.141460742840918030, 32.61873716947361856, 68.00000000000000000 ) ) ;
#18518=EDGE_LOOP ( 'NONE', ( #9711, #19726, #17344, #18863 ) ) ;
#18521=AXIS2_PLACEMENT_3D ( 'NONE', #10287, #13519, #13297 ) ;
#18523=EDGE_CURVE ( 'NONE', #2320, #8961, #21695, .T. ) ;
#18524=VERTEX_POINT ( 'NONE', #1418 ) ;
#18526=ADVANCED_FACE ( 'NONE', ( #2773 ), #11589, .T. ) ;
#18528=EDGE_LOOP ( 'NONE', ( #16401, #16928, #4177, #8744 ) ) ;
#18529=ORIENTED_EDGE ( 'NONE', *, *, #7259, .T. ) ;
#18531=DIRECTION ( 'NONE',  ( 0.000000000000000000, 0.000000000000000000, 1.000000000000000000 ) ) ;
#18532=ADVANCED_FACE ( 'NONE', ( #1090 ), #8260, .T. ) ;
#18533=CARTESIAN_POINT ( 'NONE',  ( -9.641460742840918030, -32.61873716947361856, 68.00000000000000000 ) ) ;
#18534=VECTOR ( 'NONE', #10716, 1000.000000000000000 ) ;
#18539=ORIENTED_EDGE ( 'NONE', *, *, #3389, .T. ) ;
#18541=TOROIDAL_SURFACE ( 'NONE', #7122, 4.700000000000000178, 0.2999999999999999889 ) ;
#18543=DIRECTION ( 'NONE',  ( 1.000000000000000000, 0.000000000000000000, 0.000000000000000000 ) ) ;
#18545=DIRECTION ( 'NONE',  ( 1.000000000000000000, 0.000000000000000000, -0.000000000000000000 ) ) ;
#18546=DIRECTION ( 'NONE',  ( 1.000000000000000000, 0.000000000000000000, 0.000000000000000000 ) ) ;
#18547=CARTESIAN_POINT ( 'NONE',  ( -23.02398829872513986, 7.027230193580998154E-15, 7.500000000000000000 ) ) ;
#18549=CYLINDRICAL_SURFACE ( 'NONE', #3479, 1.000000000000000888 ) ;
#18550=SPHERICAL_SURFACE ( 'NONE', #13876, 0.5000000000000000000 ) ;
#18553=AXIS2_PLACEMENT_3D ( 'NONE', #16615, #3093, #13273 ) ;
#18554=EDGE_CURVE ( 'NONE', #16569, #17318, #18087, .T. ) ;
#18555=DIRECTION ( 'NONE',  ( -0.000000000000000000, -0.000000000000000000, -1.000000000000000000 ) ) ;
#18556=( BOUNDED_CURVE ( )  B_SPLINE_CURVE ( 3, ( #17612, #20874, #15392, #6916 ),
 .UNSPECIFIED., .F., .T. ) 
 B_SPLINE_CURVE_WITH_KNOTS ( ( 4, 4 ),
 ( 3.141592653589793116, 4.712388980384689674 ),
 .UNSPECIFIED. ) 
 CURVE ( )  GEOMETRIC_REPRESENTATION_ITEM ( )  RATIONAL_B_SPLINE_CURVE ( ( 1.000000000000000000, 0.8047378541243649375, 0.8047378541243649375, 1.000000000000000000 ) ) 
 REPRESENTATION_ITEM ( '' )  );
#18557=ORIENTED_EDGE ( 'NONE', *, *, #20528, .T. ) ;
#18558=EDGE_CURVE ( 'NONE', #4102, #13748, #8150, .T. ) ;
#18559=AXIS2_PLACEMENT_3D ( 'NONE', #14188, #20599, #14079 ) ;
#18561=ORIENTED_EDGE ( 'NONE', *, *, #11172, .T. ) ;
#18563=CARTESIAN_POINT ( 'NONE',  ( 15.21174975910705918, -52.10286008774954780, 13.87500000000000000 ) ) ;
#18566=CARTESIAN_POINT ( 'NONE',  ( -3.627054932750481964, 32.11873716947361856, 68.00000000000000000 ) ) ;
#18571=CARTESIAN_POINT ( 'NONE',  ( -8.641460742840918030, -33.43424481021354921, 42.50000000000000000 ) ) ;
#18572=EDGE_CURVE ( 'NONE', #104, #11610, #6372, .T. ) ;
#18574=DIRECTION ( 'NONE',  ( 0.000000000000000000, -1.000000000000000000, 0.000000000000000000 ) ) ;
#18575=DIRECTION ( 'NONE',  ( 1.000000000000000000, 0.000000000000000000, 0.000000000000000000 ) ) ;
#18576=DIRECTION ( 'NONE',  ( -0.000000000000000000, -0.000000000000000000, -1.000000000000000000 ) ) ;
#18578=DIRECTION ( 'NONE',  ( 0.000000000000000000, 0.000000000000000000, 1.000000000000000000 ) ) ;
#18579=ADVANCED_FACE ( 'NONE', ( #16288 ), #14687, .F. ) ;
#18580=VECTOR ( 'NONE', #11460, 1000.000000000000000 ) ;
#18583=DIRECTION ( 'NONE',  ( -1.000000000000000000, 0.000000000000000000, 0.000000000000000000 ) ) ;
#18584=AXIS2_PLACEMENT_3D ( 'NONE', #17093, #16751, #2997 ) ;
#18588=DIRECTION ( 'NONE',  ( 0.000000000000000000, -0.000000000000000000, -1.000000000000000000 ) ) ;
#18592=EDGE_LOOP ( 'NONE', ( #10064, #5942, #18816, #19690 ) ) ;
#18595=CIRCLE ( 'NONE', #2158, 0.2999999999999999334 ) ;
#18598=DIRECTION ( 'NONE',  ( -0.000000000000000000, 1.000000000000000000, -0.000000000000000000 ) ) ;
#18601=DIRECTION ( 'NONE',  ( -1.000000000000000000, -0.000000000000000000, -0.000000000000000000 ) ) ;
#18602=VERTEX_POINT ( 'NONE', #287 ) ;
#18606=FACE_OUTER_BOUND ( 'NONE', #6816, .T. ) ;
#18607=DIRECTION ( 'NONE',  ( 0.000000000000000000, 0.000000000000000000, 1.000000000000000000 ) ) ;
#18608=EDGE_LOOP ( 'NONE', ( #10115, #20066, #11660, #322, #7657, #18339, #1810, #13774, #20904, #14792, #5073, #21141, #17430, #16704, #7789, #9756, #19011, #21713, #11784, #11077, #5925, #18255, #15336, #15950, #5710, #9500, #16799, #16136, #1358, #8936 ) ) ;
#18609=ORIENTED_EDGE ( 'NONE', *, *, #12416, .T. ) ;
#18610=ORIENTED_EDGE ( 'NONE', *, *, #15150, .T. ) ;
#18611=CARTESIAN_POINT ( 'NONE',  ( 14.83748569039513576, 41.93480993936275070, 13.50000000000000000 ) ) ;
#18613=ORIENTED_EDGE ( 'NONE', *, *, #9449, .T. ) ;
#18614=CIRCLE ( 'NONE', #8976, 1.000000000000000888 ) ;
#18622=CIRCLE ( 'NONE', #12940, 1.299999999999999156 ) ;
#18627=CIRCLE ( 'NONE', #7211, 0.2999999999999999334 ) ;
#18629=ORIENTED_EDGE ( 'NONE', *, *, #1223, .T. ) ;
#18630=CARTESIAN_POINT ( 'NONE',  ( 9.141460742840918030, -33.93424481021354921, 68.00000000000000000 ) ) ;
#18632=DIRECTION ( 'NONE',  ( 0.000000000000000000, -1.000000000000000000, 0.000000000000000000 ) ) ;
#18633=CIRCLE ( 'NONE', #16110, 0.2999999999999999334 ) ;
#18634=DIRECTION ( 'NONE',  ( 0.000000000000000000, 0.000000000000000000, 1.000000000000000000 ) ) ;
#18636=ORIENTED_EDGE ( 'NONE', *, *, #7608, .T. ) ;
#18637=VERTEX_POINT ( 'NONE', #3222 ) ;
#18639=EDGE_CURVE ( 'NONE', #19749, #17444, #4930, .T. ) ;
#18640=AXIS2_PLACEMENT_3D ( 'NONE', #21647, #6100, #18036 ) ;
#18641=LINE ( 'NONE', #13376, #10724 ) ;
#18642=TOROIDAL_SURFACE ( 'NONE', #1482, 1.500000000000000000, 0.5000000000000000000 ) ;
#18643=ORIENTED_EDGE ( 'NONE', *, *, #6976, .T. ) ;
#18645=ORIENTED_EDGE ( 'NONE', *, *, #805, .F. ) ;
#18648=CARTESIAN_POINT ( 'NONE',  ( -29.37540678000427619, -5.000000000000000000, 3.799999999999999822 ) ) ;
#18650=EDGE_CURVE ( 'NONE', #1513, #16076, #13384, .T. ) ;
#18651=ORIENTED_EDGE ( 'NONE', *, *, #21671, .F. ) ;
#18652=DIRECTION ( 'NONE',  ( -1.000000000000000000, 0.000000000000000000, 0.000000000000000000 ) ) ;
#18653=ADVANCED_FACE ( 'NONE', ( #1528 ), #5126, .T. ) ;
#18656=CARTESIAN_POINT ( 'NONE',  ( -15.95292532278785913, 52.11873716947361856, 14.00000000000000000 ) ) ;
#18658=CARTESIAN_POINT ( 'NONE',  ( 23.02398829872513986, 2.502127083158334653, 13.57904421648001225 ) ) ;
#18663=DIRECTION ( 'NONE',  ( -0.000000000000000000, -0.000000000000000000, -1.000000000000000000 ) ) ;
#18667=CYLINDRICAL_SURFACE ( 'NONE', #18521, 0.2999999999999999334 ) ;
#18670=ORIENTED_EDGE ( 'NONE', *, *, #6744, .F. ) ;
#18672=CARTESIAN_POINT ( 'NONE',  ( -8.641460742840918030, 33.93424481021354921, 68.00000000000000000 ) ) ;
#18675=ORIENTED_EDGE ( 'NONE', *, *, #19001, .T. ) ;
#18676=EDGE_CURVE ( 'NONE', #20280, #8695, #14210, .T. ) ;
#18677=LINE ( 'NONE', #5041, #4929 ) ;
#18679=DIRECTION ( 'NONE',  ( -0.000000000000000000, -0.000000000000000000, -1.000000000000000000 ) ) ;
#18680=EDGE_CURVE ( 'NONE', #12963, #1148, #2076, .T. ) ;
#18684=FACE_OUTER_BOUND ( 'NONE', #5147, .T. ) ;
#18685=LINE ( 'NONE', #6281, #19172 ) ;
#18687=CARTESIAN_POINT ( 'NONE',  ( -31.50000000000002132, -72.00000000000001421, 3.500000000000000000 ) ) ;
#18688=DIRECTION ( 'NONE',  ( -0.1868663427273192512, 0.9823853469773029534, 0.000000000000000000 ) ) ;
#18689=CARTESIAN_POINT ( 'NONE',  ( -14.98285978764165449, -51.83353206222920306, 13.49999999999971756 ) ) ;
#18690=DIRECTION ( 'NONE',  ( -1.000000000000000000, -0.000000000000000000, -0.000000000000000000 ) ) ;
#18691=VERTEX_POINT ( 'NONE', #6928 ) ;
#18694=EDGE_LOOP ( 'NONE', ( #20483, #14137, #14650, #7538 ) ) ;
#18696=ORIENTED_EDGE ( 'NONE', *, *, #3064, .F. ) ;
#18698=DIRECTION ( 'NONE',  ( 0.000000000000000000, 0.000000000000000000, -1.000000000000000000 ) ) ;
#18700=EDGE_CURVE ( 'NONE', #6512, #14892, #4230, .T. ) ;
#18701=ORIENTED_EDGE ( 'NONE', *, *, #360, .T. ) ;
#18703=ORIENTED_EDGE ( 'NONE', *, *, #8624, .T. ) ;
#18705=VERTEX_POINT ( 'NONE', #3998 ) ;
#18706=ADVANCED_FACE ( 'NONE', ( #15724 ), #17624, .T. ) ;
#18709=CARTESIAN_POINT ( 'NONE',  ( 15.21174975910705918, -51.61873716947361856, 14.00000000000000000 ) ) ;
#18710=ORIENTED_EDGE ( 'NONE', *, *, #19863, .F. ) ;
#18714=CARTESIAN_POINT ( 'NONE',  ( 25.37540678000427263, 63.74634676501045050, 13.50000000000000000 ) ) ;
#18715=CARTESIAN_POINT ( 'NONE',  ( -29.50000000000002132, -69.00000000000000000, 0.2999999999999947153 ) ) ;
#18717=DIRECTION ( 'NONE',  ( 0.000000000000000000, 0.000000000000000000, 1.000000000000000000 ) ) ;
#18719=ORIENTED_EDGE ( 'NONE', *, *, #17234, .T. ) ;
#18720=ORIENTED_EDGE ( 'NONE', *, *, #3989, .T. ) ;
#18721=CARTESIAN_POINT ( 'NONE',  ( -15.95292532278785913, 50.11873716947361856, 13.99999999999999822 ) ) ;
#18724=EDGE_CURVE ( 'NONE', #14227, #17330, #7100, .T. ) ;
#18726=EDGE_LOOP ( 'NONE', ( #11101, #20297, #4949, #8056, #20369, #12283, #4328, #18300, #1687, #16566, #4777, #20209, #8255, #16238, #7765, #11368, #17886, #15745, #383, #16947, #13344 ) ) ;
#18727=ADVANCED_FACE ( 'NONE', ( #7576 ), #19590, .T. ) ;
#18728=EDGE_CURVE ( 'NONE', #13909, #5745, #539, .T. ) ;
#18729=CARTESIAN_POINT ( 'NONE',  ( 14.98852729675274986, -51.95836184682382708, 13.85634242029625973 ) ) ;
#18732=PRODUCT_DEFINITION_FORMATION_WITH_SPECIFIED_SOURCE ( 'ANY', '', #11428, .NOT_KNOWN. ) ;
#18733=DIRECTION ( 'NONE',  ( 1.000000000000000000, 0.000000000000000000, 0.000000000000000000 ) ) ;
#18734=LINE ( 'NONE', #5327, #987 ) ;
#18738=DIRECTION ( 'NONE',  ( 0.000000000000000000, -0.000000000000000000, -1.000000000000000000 ) ) ;
#18739=FACE_OUTER_BOUND ( 'NONE', #21165, .T. ) ;
#18743=DIRECTION ( 'NONE',  ( -0.000000000000000000, -0.000000000000000000, -1.000000000000000000 ) ) ;
#18745=ORIENTED_EDGE ( 'NONE', *, *, #5875, .F. ) ;
#18750=ORIENTED_EDGE ( 'NONE', *, *, #15483, .F. ) ;
#18752=ORIENTED_EDGE ( 'NONE', *, *, #8552, .F. ) ;
#18754=EDGE_CURVE ( 'NONE', #2833, #9554, #498, .T. ) ;
#18755=CARTESIAN_POINT ( 'NONE',  ( -4.127054932750482408, 32.93424481021354921, 68.00000000000000000 ) ) ;
#18759=ORIENTED_EDGE ( 'NONE', *, *, #8000, .T. ) ;
#18760=LINE ( 'NONE', #3220, #15049 ) ;
#18761=EDGE_LOOP ( 'NONE', ( #10694, #5232, #408 ) ) ;
#18762=CARTESIAN_POINT ( 'NONE',  ( -29.13662752439705272, 0.000000000000000000, 7.500000000000000000 ) ) ;
#18764=VECTOR ( 'NONE', #16061, 1000.000000000000000 ) ;
#18766=AXIS2_PLACEMENT_3D ( 'NONE', #5705, #508, #19221 ) ;
#18767=DIRECTION ( 'NONE',  ( -0.000000000000000000, 0.000000000000000000, 1.000000000000000000 ) ) ;
#18768=ORIENTED_EDGE ( 'NONE', *, *, #6257, .F. ) ;
#18769=CARTESIAN_POINT ( 'NONE',  ( 23.04884263981453785, 2.295195349811796071, 13.26498523032724819 ) ) ;
#18772=PRODUCT_DEFINITION_SHAPE ( 'NONE', 'NONE',  #2891 ) ;
#18775=DIRECTION ( 'NONE',  ( 0.000000000000000000, 0.000000000000000000, 1.000000000000000000 ) ) ;
#18778=CIRCLE ( 'NONE', #9122, 0.5000000000000000000 ) ;
#18779=CARTESIAN_POINT ( 'NONE',  ( 31.50000000000002132, -71.70000000000001705, 3.500000000000000000 ) ) ;
#18780=ADVANCED_FACE ( 'NONE', ( #21224 ), #22099, .T. ) ;
#18781=DIRECTION ( 'NONE',  ( -1.000000000000000000, -0.000000000000000000, 0.000000000000000000 ) ) ;
#18782=CIRCLE ( 'NONE', #10551, 0.5000000000000004441 ) ;
#18784=AXIS2_PLACEMENT_3D ( 'NONE', #20438, #18743, #13260 ) ;
#18785=CIRCLE ( 'NONE', #8070, 2.000000000000000000 ) ;
#18786=DIRECTION ( 'NONE',  ( 0.000000000000000000, 0.000000000000000000, 1.000000000000000000 ) ) ;
#18788=LINE ( 'NONE', #18451, #13842 ) ;
#18789=VERTEX_POINT ( 'NONE', #12351 ) ;
#18790=LINE ( 'NONE', #3466, #970 ) ;
#18791=CARTESIAN_POINT ( 'NONE',  ( 28.87540678000427619, 6.494748934539263274, 13.50000000000000000 ) ) ;
#18800=DIRECTION ( 'NONE',  ( 0.000000000000000000, 0.000000000000000000, -1.000000000000000000 ) ) ;
#18801=CARTESIAN_POINT ( 'NONE',  ( 25.37540678000427263, 63.74634676501045050, 3.799999999999999822 ) ) ;
#18803=EDGE_CURVE ( 'NONE', #5223, #9561, #614, .T. ) ;
#18804=FACE_OUTER_BOUND ( 'NONE', #11116, .T. ) ;
#18805=CARTESIAN_POINT ( 'NONE',  ( 9.141460742840918030, -32.61873716947361856, 68.00000000000000000 ) ) ;
#18806=EDGE_CURVE ( 'NONE', #8904, #19806, #13500, .T. ) ;
#18811=AXIS2_PLACEMENT_3D ( 'NONE', #6594, #18213, #16750 ) ;
#18812=VERTEX_POINT ( 'NONE', #3763 ) ;
#18816=ORIENTED_EDGE ( 'NONE', *, *, #20709, .T. ) ;
#18817=CIRCLE ( 'NONE', #14497, 0.6999999999999992895 ) ;
#18819=EDGE_LOOP ( 'NONE', ( #15037, #2631, #3441, #9664 ) ) ;
#18823=VECTOR ( 'NONE', #20588, 1000.000000000000000 ) ;
#18826=LINE ( 'NONE', #10335, #285 ) ;
#18827=VECTOR ( 'NONE', #8687, 1000.000000000000000 ) ;
#18829=CARTESIAN_POINT ( 'NONE',  ( -23.02398829872514341, 3.052854503364687666, 13.54964687161600700 ) ) ;
#18830=FACE_OUTER_BOUND ( 'NONE', #14009, .T. ) ;
#18832=CARTESIAN_POINT ( 'NONE',  ( 15.21174975910705918, -52.39333383871510108, 13.50000000000000000 ) ) ;
#18833=AXIS2_PLACEMENT_3D ( 'NONE', #11304, #4161, #19718 ) ;
#18834=DIRECTION ( 'NONE',  ( 0.000000000000000000, 1.000000000000000000, 0.000000000000000000 ) ) ;
#18836=EDGE_LOOP ( 'NONE', ( #5912, #12487, #12269, #17096 ) ) ;
#18838=LINE ( 'NONE', #1593, #5305 ) ;
#18840=LINE ( 'NONE', #7314, #21719 ) ;
#18841=ORIENTED_EDGE ( 'NONE', *, *, #6240, .T. ) ;
#18842=AXIS2_PLACEMENT_3D ( 'NONE', #10459, #21200, #8773 ) ;
#18843=CLOSED_SHELL ( 'NONE', ( #3888, #20055, #19103, #9375, #9976, #9503, #18118, #12638, #10772, #6641, #16267, #7450, #10732, #20432, #129, #9238, #17210, #5436, #13737, #7369, #10965, #8927, #3802, #19823, #719, #15736, #14626, #14262, #7483, #9510, #11556, #21244, #2435, #4393, #7433, #8013, #17673, #18004, #10011, #21553, #20858, #12496, #11453, #11609, #12442, #21860, #11972, #3094, #20034, #19506, #12597, #3142, #13385, #9633, #21520, #7224, #6634, #17838, #19180, #14037, #2544, #18321, #3522, #1365, #22024, #20335, #10306, #21118, #6008, #10227, #5490, #9050, #15020, #15113, #19064, #7979, #19248, #12182, #10357, #8312, #13467, #6573, #9119, #2477, #19892, #3358, #95, #11535, #10193, #15104, #4377, #7566, #7098, #8189, #16444, #14721, #19482, #17028, #1280, #19017, #5779, #667, #1539, #6836, #1819, #9596, #13572, #15136, #20743, #5127, #17631, #16761, #3283, #1387, #15785, #12792, #8883, #2818, #22095, #14143, #15980, #6191, #13196, #18706, #20162, #9268, #10642, #1313, #7411, #19985, #1250, #15036, #1157, #17834, #16853, #2176, #5398, #4714, #18164, #1919, #18727, #9840, #17485, #7142, #18391, #300, #6709, #11288, #5094, #7549, #21421, #19341, #14810, #16743, #12494, #8580, #6857, #20333, #3417, #5853, #11391, #14301, #10520, #335, #12742, #18491, #16755, #14850, #12035, #19478, #15772, #790, #13207, #9067, #16229, #13484, #18653, #19983, #1873, #4427, #8989, #7486, #14156, #18226, #3475, #4179, #4913, #1716, #17961, #1608, #16565, #11666, #13884, #4803, #12101, #15321, #20616, #17131, #19774, #12329, #7079, #2821, #5535, #12569, #6648, #9355, #20835, #15064, #13735, #15997, #21261, #9081, #1187, #15634, #12304, #4469, #1667, #3761, #7575, #5196, #13627, #9693, #19770, #890, #14237, #5046, #2105, #16587, #16922, #5071, #18780, #8059, #6170, #10079, #17590, #188, #2938, #16085, #7802, #16823, #2228, #13833, #2482, #13471, #22109, #11052, #7392, #15497, #16585, #20102, #19500, #11226, #19771, #11421, #15531, #3987, #11142, #5983, #13314, #21830, #1088, #15039, #17634, #4859, #18526, #8700, #13989, #2903, #3015, #12490, #9705, #10676, #11595, #10955, #13962, #17262, #3854, #3886, #19343, #14796, #8885, #7503, #19354, #80, #6115, #13562, #18579, #16782, #18367, #7890, #8376, #19436, #7932, #1893, #9116, #10864, #5193, #17985, #15807, #19263, #17931, #2827, #2265, #17030, #22114, #8284, #9092, #17999, #14995, #16027, #15353, #5054, #4234, #5229, #21161, #8806, #10743, #9492, #21531, #17346, #18532, #18013, #1966, #4029, #6291, #6725, #17696, #17090, #3450, #18875, #14777, #2790, #15650, #2073, #15676, #6171, #13281, #12524, #12366, #7076, #10380, #3735, #6640, #6616, #12141, #21457, #8074, #18385, #15666, #9621, #14562, #19752, #11681, #5248, #11261, #5149, #16520, #5087, #18083, #13049, #9403, #4037, #17000, #17836, #11497, #5333, #2226, #19371, #8272, #7510 ) ) ;
#18846=CARTESIAN_POINT ( 'NONE',  ( 17.95292532278785913, 38.74634676501045760, 42.50000000000000000 ) ) ;
#18847=AXIS2_PLACEMENT_3D ( 'NONE', #19515, #7999, #14803 ) ;
#18849=AXIS2_PLACEMENT_3D ( 'NONE', #3653, #8588, #18872 ) ;
#18851=FACE_OUTER_BOUND ( 'NONE', #4792, .T. ) ;
#18854=DIRECTION ( 'NONE',  ( -1.000000000000000000, 0.000000000000000000, 0.000000000000000000 ) ) ;
#18855=FACE_OUTER_BOUND ( 'NONE', #19827, .T. ) ;
#18863=ORIENTED_EDGE ( 'NONE', *, *, #3505, .F. ) ;
#18865=CYLINDRICAL_SURFACE ( 'NONE', #2335, 0.2999999999999999334 ) ;
#18867=DIRECTION ( 'NONE',  ( 0.000000000000000000, 0.000000000000000000, 1.000000000000000000 ) ) ;
#18870=VECTOR ( 'NONE', #21108, 1000.000000000000000 ) ;
#18872=DIRECTION ( 'NONE',  ( 1.000000000000000000, 0.000000000000000000, 0.000000000000000000 ) ) ;
#18875=ADVANCED_FACE ( 'NONE', ( #9573 ), #10307, .T. ) ;
#18876=DIRECTION ( 'NONE',  ( 1.000000000000000000, 0.000000000000000000, 0.000000000000000000 ) ) ;
#18878=EDGE_LOOP ( 'NONE', ( #14437, #4467, #10526, #11978 ) ) ;
#18880=VECTOR ( 'NONE', #2739, 1000.000000000000000 ) ;
#18883=CARTESIAN_POINT ( 'NONE',  ( -23.26572410265623958, -3.298136152264965038, 13.49420500573782888 ) ) ;
#18884=CARTESIAN_POINT ( 'NONE',  ( -15.21174975910705207, -52.39333383871510108, 13.79999999999999893 ) ) ;
#18885=TOROIDAL_SURFACE ( 'NONE', #19960, 4.700000000000000178, 0.2999999999999999889 ) ;
#18886=LINE ( 'NONE', #3562, #20810 ) ;
#18887=VECTOR ( 'NONE', #18698, 1000.000000000000000 ) ;
#18889=VERTEX_POINT ( 'NONE', #11351 ) ;
#18890=CARTESIAN_POINT ( 'NONE',  ( 23.07496371939382129, 2.433385307706760869, 13.33569868627438382 ) ) ;
#18893=EDGE_CURVE ( 'NONE', #20293, #9425, #19955, .T. ) ;
#18895=CARTESIAN_POINT ( 'NONE',  ( -4.127054932750482408, -33.93424481021354921, 68.50000000000000000 ) ) ;
#18899=FACE_OUTER_BOUND ( 'NONE', #1583, .T. ) ;
#18903=CARTESIAN_POINT ( 'NONE',  ( 17.45292532278785913, -50.11873716947361856, 68.50000000000000000 ) ) ;
#18909=ORIENTED_EDGE ( 'NONE', *, *, #5162, .T. ) ;
#18910=EDGE_CURVE ( 'NONE', #17808, #10531, #6009, .T. ) ;
#18913=DIRECTION ( 'NONE',  ( 1.000000000000000000, 0.000000000000000000, 0.000000000000000000 ) ) ;
#18914=AXIS2_PLACEMENT_3D ( 'NONE', #15151, #13593, #3198 ) ;
#18915=CIRCLE ( 'NONE', #18179, 1.299999999999999156 ) ;
#18916=CARTESIAN_POINT ( 'NONE',  ( 27.67540678000426269, 36.74634676501047181, 13.50000000000000000 ) ) ;
#18918=EDGE_CURVE ( 'NONE', #4113, #6512, #7792, .T. ) ;
#18919=CARTESIAN_POINT ( 'NONE',  ( 15.95292532278785913, 52.11873716947361856, 109.6002446535588319 ) ) ;
#18920=EDGE_CURVE ( 'NONE', #1239, #8409, #5653, .T. ) ;
#18923=CIRCLE ( 'NONE', #15331, 1.984122918275927239 ) ;
#18925=DIRECTION ( 'NONE',  ( 0.000000000000000000, 0.000000000000000000, -1.000000000000000000 ) ) ;
#18926=VERTEX_POINT ( 'NONE', #14811 ) ;
#18929=ORIENTED_EDGE ( 'NONE', *, *, #10693, .T. ) ;
#18932=EDGE_CURVE ( 'NONE', #12734, #3260, #8008, .T. ) ;
#18933=ORIENTED_EDGE ( 'NONE', *, *, #7308, .F. ) ;
#18934=AXIS2_PLACEMENT_3D ( 'NONE', #6469, #4221, #19657 ) ;
#18935=TOROIDAL_SURFACE ( 'NONE', #17840, 2.274596669241483848, 0.2999999999999999889 ) ;
#18939=EDGE_CURVE ( 'NONE', #497, #15133, #11232, .T. ) ;
#18941=LINE ( 'NONE', #3714, #7379 ) ;
#18942=EDGE_CURVE ( 'NONE', #4947, #14127, #11462, .T. ) ;
#18943=CARTESIAN_POINT ( 'NONE',  ( 23.02398829872514341, 2.623740515231442583, 13.63037280509750993 ) ) ;
#18947=CIRCLE ( 'NONE', #1076, 1.984122918275925462 ) ;
#18949=CARTESIAN_POINT ( 'NONE',  ( -9.141460742840918030, -33.43424481021354921, 7.321391277662001151 ) ) ;
#18951=CARTESIAN_POINT ( 'NONE',  ( 26.37540678000427619, -10.94079601157914716, 42.50000000000000000 ) ) ;
#18954=ORIENTED_EDGE ( 'NONE', *, *, #5862, .F. ) ;
#18955=CARTESIAN_POINT ( 'NONE',  ( 14.96174975910706628, 41.81054587065081307, 13.62426406871193230 ) ) ;
#18957=EDGE_CURVE ( 'NONE', #17693, #13182, #16389, .T. ) ;
#18959=DIRECTION ( 'NONE',  ( -0.000000000000000000, 1.000000000000000000, -0.000000000000000000 ) ) ;
#18960=AXIS2_PLACEMENT_3D ( 'NONE', #16934, #11673, #13683 ) ;
#18965=EDGE_CURVE ( 'NONE', #10812, #483, #9219, .T. ) ;
#18966=CARTESIAN_POINT ( 'NONE',  ( 17.95292532278785913, -38.74634676501045760, 109.6002446535588319 ) ) ;
#18972=DIRECTION ( 'NONE',  ( 0.000000000000000000, 1.000000000000000000, 0.000000000000000000 ) ) ;
#18973=DIRECTION ( 'NONE',  ( -1.000000000000000000, 0.000000000000000000, 0.000000000000000000 ) ) ;
#18974=DIRECTION ( 'NONE',  ( 1.000000000000000000, 0.000000000000000000, 0.000000000000000000 ) ) ;
#18975=DIRECTION ( 'NONE',  ( 1.000000000000000000, 0.000000000000000000, 0.000000000000000000 ) ) ;
#18978=DIRECTION ( 'NONE',  ( -1.000000000000000000, -0.000000000000000000, -0.000000000000000000 ) ) ;
#18979=VECTOR ( 'NONE', #21808, 1000.000000000000000 ) ;
#18981=DIRECTION ( 'NONE',  ( 0.000000000000000000, 1.000000000000000000, 0.000000000000000000 ) ) ;
#18984=ORIENTED_EDGE ( 'NONE', *, *, #1967, .F. ) ;
#18990=AXIS2_PLACEMENT_3D ( 'NONE', #707, #17505, #7556 ) ;
#18992=CARTESIAN_POINT ( 'NONE',  ( 31.63662752439705272, 0.000000000000000000, 1.500000000000001332 ) ) ;
#18999=EDGE_LOOP ( 'NONE', ( #22047, #15831, #14774, #7555 ) ) ;
#19000=FACE_OUTER_BOUND ( 'NONE', #8358, .T. ) ;
#19001=EDGE_CURVE ( 'NONE', #2851, #21143, #18734, .T. ) ;
#19002=CIRCLE ( 'NONE', #402, 1.000000000000000888 ) ;
#19003=DIRECTION ( 'NONE',  ( 0.000000000000000000, 0.000000000000000000, -1.000000000000000000 ) ) ;
#19004=CARTESIAN_POINT ( 'NONE',  ( 26.37540678000427619, -10.94079601157914716, 13.50000000000000000 ) ) ;
#19005=VERTEX_POINT ( 'NONE', #51 ) ;
#19006=DIRECTION ( 'NONE',  ( -0.000000000000000000, 1.000000000000000000, 0.000000000000000000 ) ) ;
#19008=VECTOR ( 'NONE', #15126, 1000.000000000000000 ) ;
#19009=TOROIDAL_SURFACE ( 'NONE', #2208, 1.300000000000000044, 0.2999999999999999889 ) ;
#19011=ORIENTED_EDGE ( 'NONE', *, *, #17545, .T. ) ;
#19014=EDGE_LOOP ( 'NONE', ( #18229, #19952, #13497, #21862 ) ) ;
#19017=ADVANCED_FACE ( 'NONE', ( #20647 ), #6567, .T. ) ;
#19019=AXIS2_PLACEMENT_3D ( 'NONE', #10869, #1917, #20740 ) ;
#19021=VECTOR ( 'NONE', #15667, 1000.000000000000000 ) ;
#19022=AXIS2_PLACEMENT_3D ( 'NONE', #647, #16080, #860 ) ;
#19024=CARTESIAN_POINT ( 'NONE',  ( 27.37540678000427619, 5.683640910026986681, 42.50000000000000000 ) ) ;
#19025=DIRECTION ( 'NONE',  ( 0.000000000000000000, 0.000000000000000000, 1.000000000000000000 ) ) ;
#19032=ORIENTED_EDGE ( 'NONE', *, *, #7981, .T. ) ;
#19034=DIRECTION ( 'NONE',  ( 0.000000000000000000, 0.000000000000000000, 1.000000000000000000 ) ) ;
#19035=DIRECTION ( 'NONE',  ( 0.000000000000000000, 0.000000000000000000, 1.000000000000000000 ) ) ;
#19039=DIRECTION ( 'NONE',  ( 0.000000000000000000, 0.000000000000000000, -1.000000000000000000 ) ) ;
#19042=ORIENTED_EDGE ( 'NONE', *, *, #17246, .F. ) ;
#19044=CARTESIAN_POINT ( 'NONE',  ( 23.02398829872513986, -3.264233419183535378, 13.78834712654929717 ) ) ;
#19045=ORIENTED_EDGE ( 'NONE', *, *, #15259, .F. ) ;
#19046=ORIENTED_EDGE ( 'NONE', *, *, #9789, .F. ) ;
#19048=DIRECTION ( 'NONE',  ( 0.000000000000000000, 0.000000000000000000, 1.000000000000000000 ) ) ;
#19049=CYLINDRICAL_SURFACE ( 'NONE', #7775, 1.000000000000000888 ) ;
#19053=CARTESIAN_POINT ( 'NONE',  ( 29.50000000000002132, 69.00000000000000000, 1.500000000000000000 ) ) ;
#19054=CARTESIAN_POINT ( 'NONE',  ( 23.26716210542296182, -3.307210766252309142, 13.49999999999999822 ) ) ;
#19057=ORIENTED_EDGE ( 'NONE', *, *, #20087, .T. ) ;
#19059=DIRECTION ( 'NONE',  ( 1.000000000000000000, 0.000000000000000000, 0.000000000000000000 ) ) ;
#19064=ADVANCED_FACE ( 'NONE', ( #22115 ), #16826, .T. ) ;
#19065=DIRECTION ( 'NONE',  ( 0.000000000000000000, 0.000000000000000000, 1.000000000000000000 ) ) ;
#19066=VERTEX_POINT ( 'NONE', #18508 ) ;
#19070=EDGE_LOOP ( 'NONE', ( #4542, #20042, #10400, #2058 ) ) ;
#19071=DIRECTION ( 'NONE',  ( -0.000000000000000000, -0.000000000000000000, -1.000000000000000000 ) ) ;
#19072=DIRECTION ( 'NONE',  ( -0.000000000000000000, -1.000000000000000000, -0.000000000000000000 ) ) ;
#19073=EDGE_CURVE ( 'NONE', #9562, #16208, #4983, .T. ) ;
#19075=DIRECTION ( 'NONE',  ( 0.000000000000000000, 0.000000000000000000, 1.000000000000000000 ) ) ;
#19076=DIRECTION ( 'NONE',  ( 0.000000000000000000, -1.000000000000000000, -0.000000000000000000 ) ) ;
#19077=CARTESIAN_POINT ( 'NONE',  ( -30.37540678000427619, -6.000000000000000000, 7.500000000000000000 ) ) ;
#19078=CYLINDRICAL_SURFACE ( 'NONE', #14881, 1.000000000000000888 ) ;
#19079=AXIS2_PLACEMENT_3D ( 'NONE', #16264, #9700, #11035 ) ;
#19081=DIRECTION ( 'NONE',  ( 1.000000000000000000, 0.000000000000000000, 0.000000000000000000 ) ) ;
#19082=CARTESIAN_POINT ( 'NONE',  ( -9.641460742840918030, 32.11873716947361856, 68.00000000000000000 ) ) ;
#19085=DIRECTION ( 'NONE',  ( 1.000000000000000000, 0.000000000000000000, 0.000000000000000000 ) ) ;
#19087=DIRECTION ( 'NONE',  ( 0.000000000000000000, 0.000000000000000000, 1.000000000000000000 ) ) ;
#19089=AXIS2_PLACEMENT_3D ( 'NONE', #7739, #21281, #21622 ) ;
#19090=EDGE_CURVE ( 'NONE', #4254, #18926, #20311, .T. ) ;
#19093=ORIENTED_EDGE ( 'NONE', *, *, #9399, .F. ) ;
#19095=ORIENTED_EDGE ( 'NONE', *, *, #11543, .T. ) ;
#19097=DIRECTION ( 'NONE',  ( -1.000000000000000000, 0.000000000000000000, -0.000000000000000000 ) ) ;
#19098=CARTESIAN_POINT ( 'NONE',  ( -15.95292532278785913, -32.61873716947361856, 68.50000000000000000 ) ) ;
#19099=LINE ( 'NONE', #17627, #12328 ) ;
#19100=ORIENTED_EDGE ( 'NONE', *, *, #15529, .F. ) ;
#19101=CARTESIAN_POINT ( 'NONE',  ( 23.04273166366736447, 2.261511273149737100, 13.23427437508501647 ) ) ;
#19102=CARTESIAN_POINT ( 'NONE',  ( -14.66174975910705136, 0.000000000000000000, 13.50000000000000000 ) ) ;
#19103=ADVANCED_FACE ( 'NONE', ( #18851 ), #12378, .F. ) ;
#19107=CYLINDRICAL_SURFACE ( 'NONE', #176, 0.5000000000000004441 ) ;
#19110=CARTESIAN_POINT ( 'NONE',  ( -23.02398829872513986, -2.157133568460768647, 7.500000000000000000 ) ) ;
#19111=ORIENTED_EDGE ( 'NONE', *, *, #4671, .T. ) ;
#19114=EDGE_CURVE ( 'NONE', #17690, #4912, #10126, .T. ) ;
#19118=CIRCLE ( 'NONE', #20562, 2.000000000000001776 ) ;
#19123=CARTESIAN_POINT ( 'NONE',  ( -27.67540678000428045, 7.839012376739720627E-15, 13.79999999999999893 ) ) ;
#19124=DIRECTION ( 'NONE',  ( 0.000000000000000000, 0.000000000000000000, -1.000000000000000000 ) ) ;
#19125=CARTESIAN_POINT ( 'NONE',  ( -29.13662752439705272, 4.700000000000000178, 3.500000000000000000 ) ) ;
#19126=EDGE_LOOP ( 'NONE', ( #16456, #2759, #14970, #17138, #16050, #2883, #15449, #6927, #7286, #10733 ) ) ;
#19127=CARTESIAN_POINT ( 'NONE',  ( 29.26786194551793230, 2.777377181973344822, -5.247369108240390601E-15 ) ) ;
#19133=VERTEX_POINT ( 'NONE', #7111 ) ;
#19136=ORIENTED_EDGE ( 'NONE', *, *, #14451, .T. ) ;
#19137=EDGE_LOOP ( 'NONE', ( #19684, #20771, #20399, #4442 ) ) ;
#19138=ORIENTED_EDGE ( 'NONE', *, *, #20907, .T. ) ;
#19139=CARTESIAN_POINT ( 'NONE',  ( 29.13662752439705272, 5.000000000000000000, 3.799999999999999822 ) ) ;
#19142=ORIENTED_EDGE ( 'NONE', *, *, #19394, .F. ) ;
#19144=CARTESIAN_POINT ( 'NONE',  ( 23.02398829872513986, -3.004888651530553290, 13.74579066068641708 ) ) ;
#19147=CIRCLE ( 'NONE', #2702, 0.2999999999999999334 ) ;
#19152=DIRECTION ( 'NONE',  ( 0.000000000000000000, 1.000000000000000000, -0.000000000000000000 ) ) ;
#19154=DIRECTION ( 'NONE',  ( 0.000000000000000000, 0.000000000000000000, -1.000000000000000000 ) ) ;
#19155=EDGE_CURVE ( 'NONE', #1327, #6378, #13516, .T. ) ;
#19157=DIRECTION ( 'NONE',  ( 0.000000000000000000, 0.000000000000000000, 1.000000000000000000 ) ) ;
#19158=AXIS2_PLACEMENT_3D ( 'NONE', #21396, #5953, #4375 ) ;
#19161=CARTESIAN_POINT ( 'NONE',  ( -14.97529860451076722, -51.91950568661984278, 13.84831215707030516 ) ) ;
#19162=TOROIDAL_SURFACE ( 'NONE', #16282, 1.000000000000000000, 0.5000000000000000000 ) ;
#19165=DIRECTION ( 'NONE',  ( 0.000000000000000000, 0.000000000000000000, 1.000000000000000000 ) ) ;
#19167=ORIENTED_EDGE ( 'NONE', *, *, #5117, .F. ) ;
#19168=EDGE_LOOP ( 'NONE', ( #1543, #11761, #18609, #19579, #3573, #3188, #20508, #3693, #10056, #17127 ) ) ;
#19172=VECTOR ( 'NONE', #11742, 1000.000000000000000 ) ;
#19174=DIRECTION ( 'NONE',  ( 0.000000000000000000, -0.000000000000000000, -1.000000000000000000 ) ) ;
#19175=AXIS2_PLACEMENT_3D ( 'NONE', #22069, #4724, #3035 ) ;
#19176=ORIENTED_EDGE ( 'NONE', *, *, #16528, .F. ) ;
#19177=DIRECTION ( 'NONE',  ( -0.000000000000000000, -1.000000000000000000, 0.000000000000000000 ) ) ;
#19178=DIRECTION ( 'NONE',  ( 0.000000000000000000, 0.000000000000000000, -1.000000000000000000 ) ) ;
#19180=ADVANCED_FACE ( 'NONE', ( #8888 ), #21090, .F. ) ;
#19182=CARTESIAN_POINT ( 'NONE',  ( -29.37540678000427619, -6.000000000000000000, 7.500000000000000000 ) ) ;
#19183=CARTESIAN_POINT ( 'NONE',  ( 0.000000000000000000, -69.04634676501045476, 3.799999999999999822 ) ) ;
#19185=VERTEX_POINT ( 'NONE', #10677 ) ;
#19186=CARTESIAN_POINT ( 'NONE',  ( 28.71290943744531177, -6.649236572130504896, 13.47739020623642325 ) ) ;
#19187=DIRECTION ( 'NONE',  ( 0.000000000000000000, 0.000000000000000000, 1.000000000000000000 ) ) ;
#19189=ORIENTED_EDGE ( 'NONE', *, *, #9234, .F. ) ;
#19190=AXIS2_PLACEMENT_3D ( 'NONE', #16878, #20140, #6611 ) ;
#19193=ORIENTED_EDGE ( 'NONE', *, *, #21974, .F. ) ;
#19194=DIRECTION ( 'NONE',  ( 0.000000000000000000, 0.000000000000000000, 1.000000000000000000 ) ) ;
#19197=CIRCLE ( 'NONE', #20991, 0.2999999999999999334 ) ;
#19201=EDGE_CURVE ( 'NONE', #11697, #620, #17044, .T. ) ;
#19204=ORIENTED_EDGE ( 'NONE', *, *, #21113, .T. ) ;
#19207=AXIS2_PLACEMENT_3D ( 'NONE', #8834, #16990, #10510 ) ;
#19208=VECTOR ( 'NONE', #12179, 1000.000000000000000 ) ;
#19211=EDGE_LOOP ( 'NONE', ( #17114, #6562, #16582, #19887 ) ) ;
#19212=LINE ( 'NONE', #12584, #18432 ) ;
#19214=EDGE_CURVE ( 'NONE', #2467, #18467, #12428, .T. ) ;
#19215=EDGE_CURVE ( 'NONE', #2805, #15492, #10269, .T. ) ;
#19218=CARTESIAN_POINT ( 'NONE',  ( 27.37540678000428684, -36.74634676501047181, 13.79999999999999893 ) ) ;
#19219=CARTESIAN_POINT ( 'NONE',  ( -23.04273156199908357, -2.261510999192740901, 13.19999999999999929 ) ) ;
#19221=DIRECTION ( 'NONE',  ( 0.000000000000000000, 0.000000000000000000, 1.000000000000000000 ) ) ;
#19222=EDGE_CURVE ( 'NONE', #6732, #21679, #13102, .T. ) ;
#19223=VECTOR ( 'NONE', #965, 1000.000000000000000 ) ;
#19225=CARTESIAN_POINT ( 'NONE',  ( 23.04273156199908357, -2.261510999192740901, 7.500000000000000000 ) ) ;
#19228=ORIENTED_EDGE ( 'NONE', *, *, #13382, .T. ) ;
#19229=CARTESIAN_POINT ( 'NONE',  ( -17.95292532278785913, 50.11873716947361856, 68.00000000000000000 ) ) ;
#19231=AXIS2_PLACEMENT_3D ( 'NONE', #13521, #20364, #17546 ) ;
#19232=VERTEX_POINT ( 'NONE', #13905 ) ;
#19235=ORIENTED_EDGE ( 'NONE', *, *, #16908, .T. ) ;
#19237=AXIS2_PLACEMENT_3D ( 'NONE', #15503, #13820, #4093 ) ;
#19244=ORIENTED_EDGE ( 'NONE', *, *, #20408, .F. ) ;
#19245=AXIS2_PLACEMENT_3D ( 'NONE', #9210, #694, #7985 ) ;
#19247=DIRECTION ( 'NONE',  ( 0.000000000000000000, 1.000000000000000000, 0.000000000000000000 ) ) ;
#19248=ADVANCED_FACE ( 'NONE', ( #17695 ), #2378, .T. ) ;
#19249=CARTESIAN_POINT ( 'NONE',  ( -25.37540678000427263, 63.74634676501045050, 3.799999999999999822 ) ) ;
#19250=VECTOR ( 'NONE', #14966, 1000.000000000000000 ) ;
#19251=CARTESIAN_POINT ( 'NONE',  ( -29.13662752439705272, 0.000000000000000000, 13.19999999999999929 ) ) ;
#19253=AXIS2_PLACEMENT_3D ( 'NONE', #5508, #666, #219 ) ;
#19254=CIRCLE ( 'NONE', #12805, 0.2500000000000002220 ) ;
#19255=ORIENTED_EDGE ( 'NONE', *, *, #16359, .T. ) ;
#19256=DIRECTION ( 'NONE',  ( 0.000000000000000000, 0.000000000000000000, 1.000000000000000000 ) ) ;
#19259=DIRECTION ( 'NONE',  ( -0.000000000000000000, 1.000000000000000000, 0.000000000000000000 ) ) ;
#19260=ORIENTED_EDGE ( 'NONE', *, *, #165, .F. ) ;
#19263=ADVANCED_FACE ( 'NONE', ( #806 ), #18108, .F. ) ;
#19264=CARTESIAN_POINT ( 'NONE',  ( 23.02398829872513986, -3.395586890286260484, 13.79999998301280328 ) ) ;
#19265=ORIENTED_EDGE ( 'NONE', *, *, #126, .T. ) ;
#19266=AXIS2_PLACEMENT_3D ( 'NONE', #4069, #9852, #19296 ) ;
#19269=LINE ( 'NONE', #3945, #13060 ) ;
#19271=DIRECTION ( 'NONE',  ( -0.000000000000000000, -0.000000000000000000, -1.000000000000000000 ) ) ;
#19273=EDGE_CURVE ( 'NONE', #21435, #17559, #9668, .T. ) ;
#19274=CARTESIAN_POINT ( 'NONE',  ( -23.06501889853218401, 2.381465418138768886, 13.31529126727256873 ) ) ;
#19275=DIRECTION ( 'NONE',  ( -1.000000000000000000, 0.000000000000000000, 0.000000000000000000 ) ) ;
#19277=DIRECTION ( 'NONE',  ( 1.000000000000000000, 0.000000000000000000, 0.000000000000000000 ) ) ;
#19280=( BOUNDED_SURFACE ( )  B_SPLINE_SURFACE ( 3, 2, ( 
 ( #9544, #18151, #16360 ),
 ( #7884, #14679, #21535 ),
 ( #4500, #18265, #11321 ),
 ( #9320, #2838, #1241 ),
 ( #8095, #6433, #13229 ),
 ( #17814, #10212, #10333 ),
 ( #1581, #8211, #15022 ),
 ( #11764, #18481, #16915 ) ),
 .UNSPECIFIED., .F., .F., .T. ) 
 B_SPLINE_SURFACE_WITH_KNOTS ( ( 4, 2, 2, 4 ),
 ( 3, 3 ),
 ( -1.707618421664669484E-18, 0.0004639257417130348096, 0.0006958886125695531088, 0.0009278514834260713539 ),
 ( 0.000000000000000000, 1.000000000000000000 ),
 .UNSPECIFIED. ) 
 GEOMETRIC_REPRESENTATION_ITEM ( )  RATIONAL_B_SPLINE_SURFACE ( (
 ( 1.000000000000000000, 0.6123724356957929160, 1.000000000000000000),
 ( 1.000000000000000000, 0.6127303078017206639, 1.000000000000000000),
 ( 1.000000000000000000, 0.6153173443167760936, 1.000000000000000000),
 ( 1.000000000000000000, 0.6312737947278392880, 1.000000000000000000),
 ( 1.000000000000000000, 0.6386439821288609764, 1.000000000000000000),
 ( 1.000000000000000000, 0.6635434878155272997, 1.000000000000000000),
 ( 1.000000000000000000, 0.6820474757551056033, 1.000000000000000000),
 ( 1.000000000000000000, 0.7071067811865495711, 1.000000000000000000) ) ) 
 REPRESENTATION_ITEM ( '' )  SURFACE ( )  );
#19281=ORIENTED_EDGE ( 'NONE', *, *, #15498, .F. ) ;
#19282=DIRECTION ( 'NONE',  ( 0.000000000000000000, 0.000000000000000000, 1.000000000000000000 ) ) ;
#19285=ORIENTED_EDGE ( 'NONE', *, *, #9538, .T. ) ;
#19289=AXIS2_PLACEMENT_3D ( 'NONE', #7328, #14121, #2166 ) ;
#19294=VERTEX_POINT ( 'NONE', #14567 ) ;
#19295=CARTESIAN_POINT ( 'NONE',  ( 25.37540678000426908, 36.74634676501047181, 13.50000000000000000 ) ) ;
#19296=DIRECTION ( 'NONE',  ( -1.000000000000000000, -2.312964634635729960E-14, 0.000000000000000000 ) ) ;
#19297=DIRECTION ( 'NONE',  ( -0.000000000000000000, -0.000000000000000000, -1.000000000000000000 ) ) ;
#19299=CYLINDRICAL_SURFACE ( 'NONE', #21153, 0.3000000000000003775 ) ;
#19301=DIRECTION ( 'NONE',  ( -1.000000000000000000, 0.000000000000000000, -0.000000000000000000 ) ) ;
#19305=ORIENTED_EDGE ( 'NONE', *, *, #2365, .F. ) ;
#19306=ORIENTED_EDGE ( 'NONE', *, *, #17234, .F. ) ;
#19308=AXIS2_PLACEMENT_3D ( 'NONE', #14808, #16386, #21329 ) ;
#19309=DIRECTION ( 'NONE',  ( 1.000000000000000000, 0.000000000000000000, 0.000000000000000000 ) ) ;
#19313=EDGE_CURVE ( 'NONE', #14178, #4942, #15491, .T. ) ;
#19316=DIRECTION ( 'NONE',  ( 0.000000000000000000, 0.000000000000000000, 1.000000000000000000 ) ) ;
#19318=DIRECTION ( 'NONE',  ( 0.000000000000000000, -1.000000000000000000, 0.000000000000000000 ) ) ;
#19319=CARTESIAN_POINT ( 'NONE',  ( 15.95292532278785913, -34.11873716947361856, 68.00000000000000000 ) ) ;
#19323=CARTESIAN_POINT ( 'NONE',  ( -31.50000000000002132, 72.00000000000001421, 3.500000000000000000 ) ) ;
#19327=CARTESIAN_POINT ( 'NONE',  ( 31.50000000000002132, -71.00000000000001421, 3.500000000000000000 ) ) ;
#19330=DIRECTION ( 'NONE',  ( 0.000000000000000000, 0.000000000000000000, 1.000000000000000000 ) ) ;
#19331=EDGE_CURVE ( 'NONE', #20195, #20211, #7410, .T. ) ;
#19333=DIRECTION ( 'NONE',  ( 0.000000000000000000, 0.000000000000000000, 1.000000000000000000 ) ) ;
#19334=CARTESIAN_POINT ( 'NONE',  ( -4.127054932750482408, -32.93424481021354921, 42.50000000000000000 ) ) ;
#19338=CARTESIAN_POINT ( 'NONE',  ( -15.21174975910705207, 51.61873716947361856, 14.00000000000000000 ) ) ;
#19339=ORIENTED_EDGE ( 'NONE', *, *, #21239, .F. ) ;
#19340=EDGE_CURVE ( 'NONE', #19185, #15364, #9431, .T. ) ;
#19341=ADVANCED_FACE ( 'NONE', ( #10997, #6094 ), #11099, .T. ) ;
#19342=AXIS2_PLACEMENT_3D ( 'NONE', #5157, #22059, #6739 ) ;
#19343=ADVANCED_FACE ( 'NONE', ( #19838 ), #17924, .F. ) ;
#19344=ORIENTED_EDGE ( 'NONE', *, *, #7467, .F. ) ;
#19345=VERTEX_POINT ( 'NONE', #13109 ) ;
#19346=DIRECTION ( 'NONE',  ( 0.000000000000000000, -1.000000000000000000, 0.000000000000000000 ) ) ;
#19349=VECTOR ( 'NONE', #11904, 1000.000000000000000 ) ;
#19350=VECTOR ( 'NONE', #4185, 1000.000000000000000 ) ;
#19352=ORIENTED_EDGE ( 'NONE', *, *, #8129, .F. ) ;
#19354=ADVANCED_FACE ( 'NONE', ( #11205 ), #19280, .F. ) ;
#19355=CARTESIAN_POINT ( 'NONE',  ( 28.57540678000427548, 63.74634676501045050, 13.19999999999999929 ) ) ;
#19357=ORIENTED_EDGE ( 'NONE', *, *, #307, .T. ) ;
#19359=VERTEX_POINT ( 'NONE', #6643 ) ;
#19360=CIRCLE ( 'NONE', #17204, 0.5000000000000004441 ) ;
#19361=VERTEX_POINT ( 'NONE', #15228 ) ;
#19365=EDGE_CURVE ( 'NONE', #2085, #8381, #16688, .T. ) ;
#19370=VERTEX_POINT ( 'NONE', #8415 ) ;
#19371=ADVANCED_FACE ( 'NONE', ( #17020 ), #22084, .T. ) ;
#19372=CARTESIAN_POINT ( 'NONE',  ( 23.06501889853218401, -2.381465418138775103, 13.31529126727256873 ) ) ;
#19377=FACE_OUTER_BOUND ( 'NONE', #1262, .T. ) ;
#19379=AXIS2_PLACEMENT_3D ( 'NONE', #9522, #4380, #9753 ) ;
#19381=CARTESIAN_POINT ( 'NONE',  ( -3.127054932750481964, 32.61873716947361856, 68.00000000000000000 ) ) ;
#19382=AXIS2_PLACEMENT_3D ( 'NONE', #10621, #8948, #14399 ) ;
#19383=FACE_OUTER_BOUND ( 'NONE', #4193, .T. ) ;
#19387=ORIENTED_EDGE ( 'NONE', *, *, #22021, .F. ) ;
#19388=ORIENTED_EDGE ( 'NONE', *, *, #18728, .T. ) ;
#19392=B_SPLINE_CURVE_WITH_KNOTS ( 'NONE', 3,
 ( #2399, #12338, #10697, #17718, #3985, #13923 ),
 .UNSPECIFIED., .F., .F.,
 ( 4, 2, 4 ),
 ( 0.000000000000000000, 0.0002343434414548649890, 0.0004686868829097299780 ),
 .UNSPECIFIED. ) ;
#19394=EDGE_CURVE ( 'NONE', #16467, #8942, #3829, .T. ) ;
#19395=FACE_OUTER_BOUND ( 'NONE', #2401, .T. ) ;
#19397=CARTESIAN_POINT ( 'NONE',  ( -15.21174975910705207, 52.11873716947361856, 14.00000000000000000 ) ) ;
#19398=CARTESIAN_POINT ( 'NONE',  ( 23.04273156199909778, 2.261510999192739124, 13.22936009151389669 ) ) ;
#19400=CARTESIAN_POINT ( 'NONE',  ( 15.14085429618050682, 52.10286008412593617, 13.87499998596578976 ) ) ;
#19401=CARTESIAN_POINT ( 'NONE',  ( -14.90262739788948920, 52.32122552996406739, 13.50000000000000000 ) ) ;
#19403=EDGE_CURVE ( 'NONE', #12457, #17212, #128, .T. ) ;
#19408=DIRECTION ( 'NONE',  ( 1.000000000000000000, 0.000000000000000000, 0.000000000000000000 ) ) ;
#19410=ORIENTED_EDGE ( 'NONE', *, *, #5844, .F. ) ;
#19411=CARTESIAN_POINT ( 'NONE',  ( -4.127054932750482408, 33.43424481021354921, 68.50000000000000000 ) ) ;
#19412=DIRECTION ( 'NONE',  ( -1.000000000000000000, -0.000000000000000000, -0.000000000000000000 ) ) ;
#19417=FACE_OUTER_BOUND ( 'NONE', #18528, .T. ) ;
#19419=CARTESIAN_POINT ( 'NONE',  ( -28.57540678000427548, -6.776800961815481195, 13.50000000000000000 ) ) ;
#19422=DIRECTION ( 'NONE',  ( -1.000000000000000000, 0.000000000000000000, 0.000000000000000000 ) ) ;
#19423=DIRECTION ( 'NONE',  ( 0.000000000000000000, 0.000000000000000000, 1.000000000000000000 ) ) ;
#19424=ORIENTED_EDGE ( 'NONE', *, *, #17518, .F. ) ;
#19426=DIRECTION ( 'NONE',  ( 0.1868663427273192512, 0.9823853469773029534, 0.000000000000000000 ) ) ;
#19428=DIRECTION ( 'NONE',  ( 0.000000000000000000, 0.000000000000000000, -1.000000000000000000 ) ) ;
#19429=VERTEX_POINT ( 'NONE', #10105 ) ;
#19432=VERTEX_POINT ( 'NONE', #20070 ) ;
#19433=LINE ( 'NONE', #10188, #521 ) ;
#19434=CARTESIAN_POINT ( 'NONE',  ( 26.37540678000427619, 10.94079601157914539, 13.79999999999999893 ) ) ;
#19436=ADVANCED_FACE ( 'NONE', ( #11542 ), #3047, .F. ) ;
#19437=ORIENTED_EDGE ( 'NONE', *, *, #18114, .F. ) ;
#19442=ORIENTED_EDGE ( 'NONE', *, *, #21439, .T. ) ;
#19444=CARTESIAN_POINT ( 'NONE',  ( -27.37540678000428684, -36.74634676501047181, 42.50000000000000000 ) ) ;
#19447=CIRCLE ( 'NONE', #16573, 1.000000000000000000 ) ;
#19448=CARTESIAN_POINT ( 'NONE',  ( 15.21174975910707161, 32.10873716947361345, 68.25000000000000000 ) ) ;
#19449=LINE ( 'NONE', #19909, #8175 ) ;
#19450=DIRECTION ( 'NONE',  ( 0.000000000000000000, -0.000000000000000000, 1.000000000000000000 ) ) ;
#19451=ORIENTED_EDGE ( 'NONE', *, *, #16182, .F. ) ;
#19456=EDGE_LOOP ( 'NONE', ( #20414, #1403, #7651, #2956 ) ) ;
#19459=ORIENTED_EDGE ( 'NONE', *, *, #371, .F. ) ;
#19461=VERTEX_POINT ( 'NONE', #2139 ) ;
#19462=CARTESIAN_POINT ( 'NONE',  ( 27.37540678000427619, 10.94079601157914539, 42.50000000000000000 ) ) ;
#19466=CARTESIAN_POINT ( 'NONE',  ( 3.627054932750481964, 32.11873716947361856, 68.00000000000000000 ) ) ;
#19467=VERTEX_POINT ( 'NONE', #14215 ) ;
#19469=DIRECTION ( 'NONE',  ( -1.000000000000000000, 0.000000000000000000, 0.000000000000000000 ) ) ;
#19470=LINE ( 'NONE', #7632, #11649 ) ;
#19472=AXIS2_PLACEMENT_3D ( 'NONE', #16455, #18578, #2817 ) ;
#19474=LINE ( 'NONE', #17351, #5393 ) ;
#19475=EDGE_CURVE ( 'NONE', #20345, #19696, #17404, .T. ) ;
#19478=ADVANCED_FACE ( 'NONE', ( #13885 ), #19049, .T. ) ;
#19480=DIRECTION ( 'NONE',  ( -0.000000000000000000, 0.000000000000000000, -1.000000000000000000 ) ) ;
#19482=ADVANCED_FACE ( 'NONE', ( #8753 ), #12096, .T. ) ;
#19484=ORIENTED_EDGE ( 'NONE', *, *, #2794, .F. ) ;
#19487=DIRECTION ( 'NONE',  ( 0.000000000000000000, 1.000000000000000000, 0.000000000000000000 ) ) ;
#19489=AXIS2_PLACEMENT_3D ( 'NONE', #20976, #7007, #7330 ) ;
#19491=ORIENTED_EDGE ( 'NONE', *, *, #16489, .T. ) ;
#19492=EDGE_CURVE ( 'NONE', #15133, #6809, #16683, .T. ) ;
#19493=DIRECTION ( 'NONE',  ( -0.000000000000000000, -1.000000000000000000, -0.000000000000000000 ) ) ;
#19496=AXIS2_PLACEMENT_3D ( 'NONE', #1815, #7408, #17244 ) ;
#19497=ORIENTED_EDGE ( 'NONE', *, *, #14677, .T. ) ;
#19499=DIRECTION ( 'NONE',  ( -0.000000000000000000, -0.000000000000000000, -1.000000000000000000 ) ) ;
#19500=ADVANCED_FACE ( 'NONE', ( #229 ), #15880, .F. ) ;
#19502=DIRECTION ( 'NONE',  ( -0.000000000000000000, 0.000000000000000000, -1.000000000000000000 ) ) ;
#19503=CARTESIAN_POINT ( 'NONE',  ( -23.14079623692856913, 2.756488901337824426, 13.42422799743261308 ) ) ;
#19505=AXIS2_PLACEMENT_3D ( 'NONE', #5329, #5203, #21993 ) ;
#19506=ADVANCED_FACE ( 'NONE', ( #19377 ), #10651, .F. ) ;
#19508=CARTESIAN_POINT ( 'NONE',  ( 29.13662752439705272, -5.000000000000000000, 3.799999999999999822 ) ) ;
#19509=DIRECTION ( 'NONE',  ( 0.000000000000000000, 0.000000000000000000, -1.000000000000000000 ) ) ;
#19511=EDGE_LOOP ( 'NONE', ( #14589, #16499, #7245, #5994 ) ) ;
#19513=VERTEX_POINT ( 'NONE', #5408 ) ;
#19515=CARTESIAN_POINT ( 'NONE',  ( 25.37540678000427263, -63.74634676501045050, 3.799999999999999822 ) ) ;
#19516=ORIENTED_EDGE ( 'NONE', *, *, #17564, .F. ) ;
#19521=ORIENTED_EDGE ( 'NONE', *, *, #14958, .T. ) ;
#19522=FACE_OUTER_BOUND ( 'NONE', #6031, .T. ) ;
#19523=AXIS2_PLACEMENT_3D ( 'NONE', #12881, #9545, #4395 ) ;
#19524=DIRECTION ( 'NONE',  ( 1.000000000000000000, 0.000000000000000000, 0.000000000000000000 ) ) ;
#19526=CARTESIAN_POINT ( 'NONE',  ( 15.21174975910705918, -51.61873716947361856, 14.00000000000000000 ) ) ;
#19527=DIRECTION ( 'NONE',  ( -1.000000000000000000, 0.000000000000000000, 0.000000000000000000 ) ) ;
#19530=ORIENTED_EDGE ( 'NONE', *, *, #11469, .T. ) ;
#19533=PLANE ( 'NONE',  #4075 ) ;
#19534=CARTESIAN_POINT ( 'NONE',  ( -23.32398829872514057, -3.528912754968629439, 13.50000000000000000 ) ) ;
#19535=ORIENTED_EDGE ( 'NONE', *, *, #2240, .T. ) ;
#19538=CIRCLE ( 'NONE', #13823, 0.2999999999999999334 ) ;
#19539=CARTESIAN_POINT ( 'NONE',  ( -15.95292532278785913, -52.10286008774954780, 13.87500000000000000 ) ) ;
#19542=ORIENTED_EDGE ( 'NONE', *, *, #12099, .F. ) ;
#19543=CARTESIAN_POINT ( 'NONE',  ( 18.22752199202934520, 50.11873716947361856, 13.79999999999999893 ) ) ;
#19545=ORIENTED_EDGE ( 'NONE', *, *, #17580, .T. ) ;
#19546=CIRCLE ( 'NONE', #9902, 0.2999999999999999334 ) ;
#19547=VERTEX_POINT ( 'NONE', #10436 ) ;
#19548=CARTESIAN_POINT ( 'NONE',  ( -14.96502315657345328, 51.87273146205216534, 13.83570993898299406 ) ) ;
#19552=AXIS2_PLACEMENT_3D ( 'NONE', #5518, #347, #5749 ) ;
#19554=CIRCLE ( 'NONE', #9912, 0.2999999999999999334 ) ;
#19556=EDGE_CURVE ( 'NONE', #21336, #21055, #18941, .T. ) ;
#19557=ORIENTED_EDGE ( 'NONE', *, *, #17137, .T. ) ;
#19559=CIRCLE ( 'NONE', #6001, 0.2500000000000002220 ) ;
#19560=EDGE_CURVE ( 'NONE', #20727, #19811, #12706, .T. ) ;
#19562=DIRECTION ( 'NONE',  ( -1.000000000000000000, 0.000000000000000000, 0.000000000000000000 ) ) ;
#19563=CARTESIAN_POINT ( 'NONE',  ( -28.57540678000427548, 0.000000000000000000, 13.19999999999999929 ) ) ;
#19564=DIRECTION ( 'NONE',  ( 0.000000000000000000, -0.000000000000000000, -1.000000000000000000 ) ) ;
#19565=FACE_OUTER_BOUND ( 'NONE', #9031, .T. ) ;
#19566=ORIENTED_EDGE ( 'NONE', *, *, #6884, .T. ) ;
#19569=DIRECTION ( 'NONE',  ( -1.000000000000000000, 0.000000000000000000, -0.000000000000000000 ) ) ;
#19570=AXIS2_PLACEMENT_3D ( 'NONE', #21481, #18086, #1417 ) ;
#19572=CIRCLE ( 'NONE', #22100, 3.500000000000003109 ) ;
#19574=ORIENTED_EDGE ( 'NONE', *, *, #4968, .T. ) ;
#19575=CIRCLE ( 'NONE', #8868, 0.5000000000000004441 ) ;
#19576=EDGE_CURVE ( 'NONE', #14923, #22131, #5249, .T. ) ;
#19579=ORIENTED_EDGE ( 'NONE', *, *, #16305, .T. ) ;
#19580=CARTESIAN_POINT ( 'NONE',  ( -17.95292532278785913, 50.11873716947361856, 68.00000000000000000 ) ) ;
#19587=CARTESIAN_POINT ( 'NONE',  ( 3.127054932750481964, 33.43424481021354921, 68.00000000000000000 ) ) ;
#19588=VERTEX_POINT ( 'NONE', #20944 ) ;
#19590=TOROIDAL_SURFACE ( 'NONE', #18509, 0.2500000000000000000, 0.2500000000000000000 ) ;
#19592=ORIENTED_EDGE ( 'NONE', *, *, #12686, .T. ) ;
#19594=CARTESIAN_POINT ( 'NONE',  ( 32.20000000000001705, 72.00000000000001421, 1.800000000000000044 ) ) ;
#19597=CARTESIAN_POINT ( 'NONE',  ( -9.141460742840918030, -33.43424481021354921, 7.321391277662001151 ) ) ;
#19600=CARTESIAN_POINT ( 'NONE',  ( 25.37540678000426908, 36.74634676501047181, 13.79999999999999893 ) ) ;
#19602=LINE ( 'NONE', #6078, #5404 ) ;
#19603=EDGE_CURVE ( 'NONE', #21679, #12877, #5629, .T. ) ;
#19605=AXIS2_PLACEMENT_3D ( 'NONE', #980, #12098, #5304 ) ;
#19607=ORIENTED_EDGE ( 'NONE', *, *, #8396, .F. ) ;
#19609=DIRECTION ( 'NONE',  ( -0.000000000000000000, -1.000000000000000000, -0.000000000000000000 ) ) ;
#19610=ORIENTED_EDGE ( 'NONE', *, *, #1967, .T. ) ;
#19611=AXIS2_PLACEMENT_3D ( 'NONE', #9384, #21252, #17877 ) ;
#19616=DIRECTION ( 'NONE',  ( -0.000000000000000000, -0.000000000000000000, -1.000000000000000000 ) ) ;
#19618=ORIENTED_EDGE ( 'NONE', *, *, #8634, .F. ) ;
#19620=CARTESIAN_POINT ( 'NONE',  ( -23.83662752439705201, 0.000000000000000000, 7.500000000000000000 ) ) ;
#19624=LINE ( 'NONE', #12557, #3416 ) ;
#19626=EDGE_CURVE ( 'NONE', #12853, #13036, #2684, .T. ) ;
#19628=CARTESIAN_POINT ( 'NONE',  ( 17.95292532278785913, 38.74634676501045760, 109.6002446535588319 ) ) ;
#19630=DIRECTION ( 'NONE',  ( -1.000000000000000000, 0.000000000000000000, 0.000000000000000000 ) ) ;
#19631=ORIENTED_EDGE ( 'NONE', *, *, #11637, .F. ) ;
#19632=EDGE_LOOP ( 'NONE', ( #21741, #2989, #11372, #14207 ) ) ;
#19635=CARTESIAN_POINT ( 'NONE',  ( 29.37540678000427619, -4.700000000000000178, 3.500000000000000000 ) ) ;
#19636=ORIENTED_EDGE ( 'NONE', *, *, #18469, .F. ) ;
#19638=EDGE_CURVE ( 'NONE', #16219, #9468, #10234, .T. ) ;
#19639=CIRCLE ( 'NONE', #9652, 0.2999999999999999334 ) ;
#19641=AXIS2_PLACEMENT_3D ( 'NONE', #16780, #3140, #15202 ) ;
#19643=ORIENTED_EDGE ( 'NONE', *, *, #2298, .F. ) ;
#19645=LINE ( 'NONE', #12465, #15943 ) ;
#19646=EDGE_CURVE ( 'NONE', #20083, #14314, #17007, .T. ) ;
#19647=DIRECTION ( 'NONE',  ( 0.000000000000000000, 0.000000000000000000, -1.000000000000000000 ) ) ;
#19651=ORIENTED_EDGE ( 'NONE', *, *, #17737, .T. ) ;
#19652=CARTESIAN_POINT ( 'NONE',  ( -14.96174975910705207, 41.81054587065082728, 13.75000000000000000 ) ) ;
#19654=CARTESIAN_POINT ( 'NONE',  ( -15.95292532278785913, -50.11873716947361856, 13.99999999999999822 ) ) ;
#19657=DIRECTION ( 'NONE',  ( 0.000000000000000000, 0.000000000000000000, 1.000000000000000000 ) ) ;
#19664=LINE ( 'NONE', #21470, #8115 ) ;
#19665=VERTEX_POINT ( 'NONE', #4151 ) ;
#19668=DIRECTION ( 'NONE',  ( 0.000000000000000000, 0.000000000000000000, -1.000000000000000000 ) ) ;
#19671=EDGE_LOOP ( 'NONE', ( #7103, #11181, #9279, #12020, #4908, #3544 ) ) ;
#19672=VERTEX_POINT ( 'NONE', #6073 ) ;
#19676=CARTESIAN_POINT ( 'NONE',  ( 17.95292532278785913, 50.11873716947361856, 14.00000000000000000 ) ) ;
#19677=DIRECTION ( 'NONE',  ( 0.000000000000000000, 1.000000000000000000, 0.000000000000000000 ) ) ;
#19680=LINE ( 'NONE', #4351, #16126 ) ;
#19684=ORIENTED_EDGE ( 'NONE', *, *, #11172, .F. ) ;
#19688=EDGE_CURVE ( 'NONE', #8431, #9468, #14535, .T. ) ;
#19689=CARTESIAN_POINT ( 'NONE',  ( -28.87540678000427619, 63.74634676501045050, 13.19999999999999929 ) ) ;
#19690=ORIENTED_EDGE ( 'NONE', *, *, #21321, .T. ) ;
#19691=EDGE_CURVE ( 'NONE', #20699, #12236, #16649, .T. ) ;
#19693=ORIENTED_EDGE ( 'NONE', *, *, #7319, .F. ) ;
#19694=DIRECTION ( 'NONE',  ( 1.000000000000000000, 0.000000000000000000, 0.000000000000000000 ) ) ;
#19696=VERTEX_POINT ( 'NONE', #11083 ) ;
#19697=DIRECTION ( 'NONE',  ( 0.000000000000000000, -1.000000000000000000, 0.000000000000000000 ) ) ;
#19698=CARTESIAN_POINT ( 'NONE',  ( -15.95292532278785913, -52.39333383871510108, 13.50000000000000000 ) ) ;
#19699=ORIENTED_EDGE ( 'NONE', *, *, #16966, .T. ) ;
#19700=DIRECTION ( 'NONE',  ( 0.000000000000000000, 0.000000000000000000, -1.000000000000000000 ) ) ;
#19705=DIRECTION ( 'NONE',  ( 0.000000000000000000, -0.000000000000000000, -1.000000000000000000 ) ) ;
#19706=CIRCLE ( 'NONE', #2193, 6.499999999999999112 ) ;
#19707=EDGE_CURVE ( 'NONE', #8649, #6333, #3796, .T. ) ;
#19708=PLANE ( 'NONE',  #16452 ) ;
#19710=VECTOR ( 'NONE', #21204, 1000.000000000000000 ) ;
#19713=CARTESIAN_POINT ( 'NONE',  ( -28.87540678000427619, -6.494748934539263274, 7.799999999999999822 ) ) ;
#19716=CIRCLE ( 'NONE', #6879, 1.000000000000000888 ) ;
#19717=ORIENTED_EDGE ( 'NONE', *, *, #7199, .F. ) ;
#19718=DIRECTION ( 'NONE',  ( 1.000000000000000000, 0.000000000000000000, 0.000000000000000000 ) ) ;
#19720=CARTESIAN_POINT ( 'NONE',  ( 27.37540678000427974, -10.94079601157914716, 42.50000000000000000 ) ) ;
#19721=ORIENTED_EDGE ( 'NONE', *, *, #20411, .F. ) ;
#19722=ORIENTED_EDGE ( 'NONE', *, *, #7782, .F. ) ;
#19726=ORIENTED_EDGE ( 'NONE', *, *, #12644, .T. ) ;
#19727=AXIS2_PLACEMENT_3D ( 'NONE', #725, #7578, #14710 ) ;
#19728=ORIENTED_EDGE ( 'NONE', *, *, #7666, .T. ) ;
#19729=VECTOR ( 'NONE', #4272, 1000.000000000000000 ) ;
#19730=DIRECTION ( 'NONE',  ( 1.000000000000000000, 0.000000000000000000, -0.000000000000000000 ) ) ;
#19731=VECTOR ( 'NONE', #2777, 1000.000000000000000 ) ;
#19732=CARTESIAN_POINT ( 'NONE',  ( -26.37540678000427619, -10.94079601157914716, 42.50000000000000000 ) ) ;
#19734=DIRECTION ( 'NONE',  ( -0.000000000000000000, -0.000000000000000000, 1.000000000000000000 ) ) ;
#19735=CARTESIAN_POINT ( 'NONE',  ( 14.66174954729678248, 51.84624528035402591, 13.50000000000000000 ) ) ;
#19737=CARTESIAN_POINT ( 'NONE',  ( -23.02398829872514341, 2.280095008958276104, 13.43080372783514598 ) ) ;
#19738=EDGE_CURVE ( 'NONE', #9842, #8846, #21618, .T. ) ;
#19744=ORIENTED_EDGE ( 'NONE', *, *, #15483, .T. ) ;
#19745=ORIENTED_EDGE ( 'NONE', *, *, #17254, .T. ) ;
#19746=CYLINDRICAL_SURFACE ( 'NONE', #3500, 0.3000000000000016542 ) ;
#19747=AXIS2_PLACEMENT_3D ( 'NONE', #9734, #19569, #9283 ) ;
#19749=VERTEX_POINT ( 'NONE', #6933 ) ;
#19752=ADVANCED_FACE ( 'NONE', ( #7146 ), #13622, .F. ) ;
#19753=VERTEX_POINT ( 'NONE', #3335 ) ;
#19756=TOROIDAL_SURFACE ( 'NONE', #10463, 2.274596669241483848, 0.2999999999999999889 ) ;
#19757=EDGE_CURVE ( 'NONE', #16569, #1455, #10938, .T. ) ;
#19758=DIRECTION ( 'NONE',  ( 0.000000000000000000, 0.000000000000000000, -1.000000000000000000 ) ) ;
#19760=CARTESIAN_POINT ( 'NONE',  ( 15.21174975910705918, 51.61873716947361856, 14.00000000000000000 ) ) ;
#19761=FACE_OUTER_BOUND ( 'NONE', #13189, .T. ) ;
#19762=ORIENTED_EDGE ( 'NONE', *, *, #1768, .T. ) ;
#19765=FACE_OUTER_BOUND ( 'NONE', #10833, .T. ) ;
#19766=DIRECTION ( 'NONE',  ( 0.000000000000000000, 0.000000000000000000, 1.000000000000000000 ) ) ;
#19768=DIRECTION ( 'NONE',  ( 0.000000000000000000, 0.000000000000000000, 1.000000000000000000 ) ) ;
#19770=ADVANCED_FACE ( 'NONE', ( #5020 ), #1640, .F. ) ;
#19771=ADVANCED_FACE ( 'NONE', ( #11931 ), #12259, .F. ) ;
#19774=ADVANCED_FACE ( 'NONE', ( #19000 ), #17197, .T. ) ;
#19775=LINE ( 'NONE', #2882, #3087 ) ;
#19776=ORIENTED_EDGE ( 'NONE', *, *, #6612, .F. ) ;
#19777=VERTEX_POINT ( 'NONE', #15938 ) ;
#19779=LINE ( 'NONE', #1082, #17469 ) ;
#19781=DIRECTION ( 'NONE',  ( 0.000000000000000000, 0.000000000000000000, 1.000000000000000000 ) ) ;
#19782=ORIENTED_EDGE ( 'NONE', *, *, #16879, .F. ) ;
#19784=CARTESIAN_POINT ( 'NONE',  ( -15.21174975910705207, -51.86873716947361856, 68.00000000000000000 ) ) ;
#19786=PLANE ( 'NONE',  #3494 ) ;
#19787=CARTESIAN_POINT ( 'NONE',  ( -23.06502549581203354, -2.381505846144857941, 13.31536975879940954 ) ) ;
#19789=CARTESIAN_POINT ( 'NONE',  ( 28.87540678000427619, 0.000000000000000000, 7.799999999999999822 ) ) ;
#19795=ORIENTED_EDGE ( 'NONE', *, *, #20857, .T. ) ;
#19798=EDGE_CURVE ( 'NONE', #8047, #1047, #19212, .T. ) ;
#19800=VERTEX_POINT ( 'NONE', #621 ) ;
#19804=ORIENTED_EDGE ( 'NONE', *, *, #21671, .T. ) ;
#19805=VERTEX_POINT ( 'NONE', #12474 ) ;
#19806=VERTEX_POINT ( 'NONE', #399 ) ;
#19809=AXIS2_PLACEMENT_3D ( 'NONE', #16942, #16600, #1611 ) ;
#19811=VERTEX_POINT ( 'NONE', #7476 ) ;
#19813=EDGE_CURVE ( 'NONE', #4141, #8047, #8796, .T. ) ;
#19814=DIRECTION ( 'NONE',  ( 0.000000000000000000, 1.000000000000000000, -0.000000000000000000 ) ) ;
#19816=EDGE_CURVE ( 'NONE', #19232, #2467, #15832, .T. ) ;
#19823=ADVANCED_FACE ( 'NONE', ( #14273 ), #10818, .F. ) ;
#19826=B_SPLINE_CURVE_WITH_KNOTS ( 'NONE', 3,
 ( #19534, #14480, #5703, #12477, #4217, #9359, #12809, #11036, #9137, #10821, #16162, #19219 ),
 .UNSPECIFIED., .F., .F.,
 ( 4, 2, 2, 2, 2, 4 ),
 ( 0.000000000000000000, 0.0006847042422322843162, 0.001027056363348427667, 0.001198232423906498258, 0.001283820454185534638, 0.001369408484464571018 ),
 .UNSPECIFIED. ) ;
#19827=EDGE_LOOP ( 'NONE', ( #17547, #2650, #21502, #6910, #9015, #8739 ) ) ;
#19828=DIRECTION ( 'NONE',  ( 0.000000000000000000, 1.000000000000000000, 0.000000000000000000 ) ) ;
#19830=UNCERTAINTY_MEASURE_WITH_UNIT (LENGTH_MEASURE( 1.000000000000000082E-05 ), #5293, 'distance_accuracy_value', 'NONE');
#19831=ORIENTED_EDGE ( 'NONE', *, *, #517, .F. ) ;
#19833=ORIENTED_EDGE ( 'NONE', *, *, #4260, .T. ) ;
#19834=CIRCLE ( 'NONE', #7684, 5.000000000000000888 ) ;
#19835=AXIS2_PLACEMENT_3D ( 'NONE', #21573, #19878, #19768 ) ;
#19836=ORIENTED_EDGE ( 'NONE', *, *, #6134, .F. ) ;
#19838=FACE_OUTER_BOUND ( 'NONE', #7592, .T. ) ;
#19841=ORIENTED_EDGE ( 'NONE', *, *, #18803, .F. ) ;
#19842=DIRECTION ( 'NONE',  ( 1.000000000000000000, 0.000000000000000000, 0.000000000000000000 ) ) ;
#19843=FACE_OUTER_BOUND ( 'NONE', #12591, .T. ) ;
#19845=CARTESIAN_POINT ( 'NONE',  ( -23.02398829872513986, 2.157133568460765094, 13.26806292639400908 ) ) ;
#19846=ORIENTED_EDGE ( 'NONE', *, *, #6956, .F. ) ;
#19847=DIRECTION ( 'NONE',  ( 0.000000000000000000, 0.000000000000000000, 1.000000000000000000 ) ) ;
#19850=ORIENTED_EDGE ( 'NONE', *, *, #1162, .T. ) ;
#19851=CIRCLE ( 'NONE', #4118, 0.5000000000000004441 ) ;
#19854=FACE_OUTER_BOUND ( 'NONE', #10128, .T. ) ;
#19855=VERTEX_POINT ( 'NONE', #7252 ) ;
#19858=ORIENTED_EDGE ( 'NONE', *, *, #10121, .T. ) ;
#19859=CARTESIAN_POINT ( 'NONE',  ( -27.67540678000428400, -36.74634676501047181, 13.50000000000000000 ) ) ;
#19860=VECTOR ( 'NONE', #9965, 1000.000000000000000 ) ;
#19863=EDGE_CURVE ( 'NONE', #7977, #14982, #834, .T. ) ;
#19867=DIRECTION ( 'NONE',  ( 0.000000000000000000, 0.000000000000000000, 1.000000000000000000 ) ) ;
#19868=VECTOR ( 'NONE', #5441, 1000.000000000000000 ) ;
#19869=FACE_OUTER_BOUND ( 'NONE', #17067, .T. ) ;
#19870=CIRCLE ( 'NONE', #553, 0.2999999999999999334 ) ;
#19873=DIRECTION ( 'NONE',  ( 0.9823853469773031755, -0.1868663427273193067, 0.000000000000000000 ) ) ;
#19875=FACE_OUTER_BOUND ( 'NONE', #2215, .T. ) ;
#19878=DIRECTION ( 'NONE',  ( 0.000000000000000000, 1.000000000000000000, -0.000000000000000000 ) ) ;
#19885=VECTOR ( 'NONE', #19705, 1000.000000000000000 ) ;
#19886=CIRCLE ( 'NONE', #8097, 0.5000000000000000000 ) ;
#19887=ORIENTED_EDGE ( 'NONE', *, *, #8509, .F. ) ;
#19889=ORIENTED_EDGE ( 'NONE', *, *, #12686, .F. ) ;
#19890=CARTESIAN_POINT ( 'NONE',  ( -29.50000000000002132, 69.00000000000000000, 0.2999999999999947153 ) ) ;
#19891=DIRECTION ( 'NONE',  ( -0.000000000000000000, -0.000000000000000000, -1.000000000000000000 ) ) ;
#19892=ADVANCED_FACE ( 'NONE', ( #4322 ), #2526, .T. ) ;
#19893=DIRECTION ( 'NONE',  ( 0.000000000000000000, 0.000000000000000000, 1.000000000000000000 ) ) ;
#19895=AXIS2_PLACEMENT_3D ( 'NONE', #4869, #8571, #6670 ) ;
#19897=CARTESIAN_POINT ( 'NONE',  ( 31.50000000000002132, 71.00000000000001421, 3.200000000000000178 ) ) ;
#19898=EDGE_CURVE ( 'NONE', #5647, #1165, #16666, .T. ) ;
#19899=FACE_OUTER_BOUND ( 'NONE', #11831, .T. ) ;
#19900=CARTESIAN_POINT ( 'NONE',  ( -29.17540678000427690, 0.000000000000000000, 7.500000000000000000 ) ) ;
#19901=EDGE_CURVE ( 'NONE', #7269, #8930, #17412, .T. ) ;
#19902=CARTESIAN_POINT ( 'NONE',  ( -25.37540678000429395, -38.74634676501045760, 13.79999999999999893 ) ) ;
#19905=CARTESIAN_POINT ( 'NONE',  ( -17.95292532278785913, -50.11873716947361856, 68.00000000000000000 ) ) ;
#19908=ORIENTED_EDGE ( 'NONE', *, *, #11258, .T. ) ;
#19909=CARTESIAN_POINT ( 'NONE',  ( 3.627054932750481964, 32.61873716947361856, 7.321391277662001151 ) ) ;
#19910=CARTESIAN_POINT ( 'NONE',  ( -14.96174975910705207, -51.76873716947361714, 13.79999999999999716 ) ) ;
#19911=LINE ( 'NONE', #4573, #1019 ) ;
#19913=CARTESIAN_POINT ( 'NONE',  ( 9.141460742840918030, -32.93424481021354921, 13.50000000000000000 ) ) ;
#19916=FACE_OUTER_BOUND ( 'NONE', #11840, .T. ) ;
#19917=ORIENTED_EDGE ( 'NONE', *, *, #12284, .F. ) ;
#19918=FACE_OUTER_BOUND ( 'NONE', #21029, .T. ) ;
#19921=ORIENTED_EDGE ( 'NONE', *, *, #9098, .T. ) ;
#19922=AXIS2_PLACEMENT_3D ( 'NONE', #21641, #2602, #12880 ) ;
#19931=FACE_OUTER_BOUND ( 'NONE', #8749, .T. ) ;
#19932=ORIENTED_EDGE ( 'NONE', *, *, #8479, .F. ) ;
#19934=EDGE_CURVE ( 'NONE', #8611, #1327, #17369, .T. ) ;
#19937=DIRECTION ( 'NONE',  ( 0.000000000000000000, 0.000000000000000000, 1.000000000000000000 ) ) ;
#19939=TOROIDAL_SURFACE ( 'NONE', #9204, 6.800000000000001599, 0.2999999999999999889 ) ;
#19945=DIRECTION ( 'NONE',  ( 0.000000000000000000, 0.000000000000000000, -1.000000000000000000 ) ) ;
#19946=TOROIDAL_SURFACE ( 'NONE', #10297, 1.500000000000000000, 0.5000000000000000000 ) ;
#19950=DIRECTION ( 'NONE',  ( 0.000000000000000000, 0.000000000000000000, 1.000000000000000000 ) ) ;
#19951=EDGE_LOOP ( 'NONE', ( #15655, #9169, #8504, #9761 ) ) ;
#19952=ORIENTED_EDGE ( 'NONE', *, *, #9949, .T. ) ;
#19953=LINE ( 'NONE', #4618, #18887 ) ;
#19955=CIRCLE ( 'NONE', #15991, 0.2500000000000002220 ) ;
#19959=ORIENTED_EDGE ( 'NONE', *, *, #5487, .F. ) ;
#19960=AXIS2_PLACEMENT_3D ( 'NONE', #10181, #2289, #5269 ) ;
#19964=CARTESIAN_POINT ( 'NONE',  ( -32.50000000000002132, 71.00000000000001421, 3.500000000000000000 ) ) ;
#19969=DIRECTION ( 'NONE',  ( 1.000000000000000000, 3.552713678800501718E-15, 0.000000000000000000 ) ) ;
#19970=AXIS2_PLACEMENT_3D ( 'NONE', #5072, #6049, #7090 ) ;
#19971=DIRECTION ( 'NONE',  ( -1.000000000000000000, 0.000000000000000000, 0.000000000000000000 ) ) ;
#19973=DIRECTION ( 'NONE',  ( 1.000000000000000000, 0.000000000000000000, 0.000000000000000000 ) ) ;
#19976=AXIS2_PLACEMENT_3D ( 'NONE', #17366, #13679, #10348 ) ;
#19977=ORIENTED_EDGE ( 'NONE', *, *, #12903, .F. ) ;
#19982=CARTESIAN_POINT ( 'NONE',  ( -29.44760963940965226, -2.533475775848048617, 0.1250376690123979340 ) ) ;
#19983=ADVANCED_FACE ( 'NONE', ( #6461 ), #6570, .F. ) ;
#19985=ADVANCED_FACE ( 'NONE', ( #13361 ), #14602, .T. ) ;
#19987=ORIENTED_EDGE ( 'NONE', *, *, #16398, .F. ) ;
#19989=AXIS2_PLACEMENT_3D ( 'NONE', #14278, #21130, #12684 ) ;
#19991=CARTESIAN_POINT ( 'NONE',  ( 23.02398829872513630, -2.502141052783102726, 13.57900107139873214 ) ) ;
#19992=CIRCLE ( 'NONE', #11397, 0.2999999999999999334 ) ;
#19997=VECTOR ( 'NONE', #866, 1000.000000000000000 ) ;
#19998=DIRECTION ( 'NONE',  ( 0.000000000000000000, 0.000000000000000000, 1.000000000000000000 ) ) ;
#20001=EDGE_CURVE ( 'NONE', #18889, #6249, #20100, .T. ) ;
#20004=ORIENTED_EDGE ( 'NONE', *, *, #11069, .T. ) ;
#20005=DIRECTION ( 'NONE',  ( 0.000000000000000000, 0.000000000000000000, 1.000000000000000000 ) ) ;
#20008=ORIENTED_EDGE ( 'NONE', *, *, #16104, .T. ) ;
#20014=ORIENTED_EDGE ( 'NONE', *, *, #13599, .T. ) ;
#20015=VERTEX_POINT ( 'NONE', #946 ) ;
#20018=DIRECTION ( 'NONE',  ( 0.000000000000000000, 0.000000000000000000, -1.000000000000000000 ) ) ;
#20020=DIRECTION ( 'NONE',  ( 0.000000000000000000, 0.000000000000000000, 1.000000000000000000 ) ) ;
#20021=ORIENTED_EDGE ( 'NONE', *, *, #1756, .T. ) ;
#20022=LINE ( 'NONE', #4689, #19250 ) ;
#20023=EDGE_CURVE ( 'NONE', #9735, #4947, #11646, .T. ) ;
#20024=AXIS2_PLACEMENT_3D ( 'NONE', #12708, #11388, #21485 ) ;
#20025=VECTOR ( 'NONE', #8468, 1000.000000000000000 ) ;
#20026=SPHERICAL_SURFACE ( 'NONE', #7415, 0.5000000000000000000 ) ;
#20028=DIRECTION ( 'NONE',  ( -0.000000000000000000, -0.000000000000000000, -1.000000000000000000 ) ) ;
#20029=EDGE_LOOP ( 'NONE', ( #5907, #16378, #7670, #13432 ) ) ;
#20031=DIRECTION ( 'NONE',  ( 0.000000000000000000, 0.000000000000000000, -1.000000000000000000 ) ) ;
#20033=FACE_OUTER_BOUND ( 'NONE', #12371, .T. ) ;
#20034=ADVANCED_FACE ( 'NONE', ( #6231 ), #14814, .F. ) ;
#20038=VERTEX_POINT ( 'NONE', #21456 ) ;
#20039=CARTESIAN_POINT ( 'NONE',  ( 17.95292532278785913, -34.11873716947361856, 13.49999999999999822 ) ) ;
#20040=AXIS2_PLACEMENT_3D ( 'NONE', #13585, #5200, #1724 ) ;
#20042=ORIENTED_EDGE ( 'NONE', *, *, #20598, .F. ) ;
#20045=LINE ( 'NONE', #7631, #10585 ) ;
#20048=CARTESIAN_POINT ( 'NONE',  ( 23.07454441928563682, 2.431172533959870208, 13.33570496075367906 ) ) ;
#20050=VECTOR ( 'NONE', #2361, 1000.000000000000000 ) ;
#20051=AXIS2_PLACEMENT_3D ( 'NONE', #7301, #21183, #4153 ) ;
#20052=DIRECTION ( 'NONE',  ( 1.000000000000000000, 0.000000000000000000, 0.000000000000000000 ) ) ;
#20055=ADVANCED_FACE ( 'NONE', ( #4536 ), #932, .F. ) ;
#20056=LINE ( 'NONE', #14358, #3478 ) ;
#20058=CARTESIAN_POINT ( 'NONE',  ( -15.21174975910705207, 51.61873716947361856, 68.00000000000000000 ) ) ;
#20061=ORIENTED_EDGE ( 'NONE', *, *, #6466, .T. ) ;
#20062=LINE ( 'NONE', #6197, #3874 ) ;
#20063=EDGE_CURVE ( 'NONE', #17966, #12755, #11358, .T. ) ;
#20064=CARTESIAN_POINT ( 'NONE',  ( -15.21174975910705207, -52.10286008774954780, 13.87500000000000000 ) ) ;
#20065=ORIENTED_EDGE ( 'NONE', *, *, #17115, .F. ) ;
#20066=ORIENTED_EDGE ( 'NONE', *, *, #16798, .T. ) ;
#20067=AXIS2_PLACEMENT_3D ( 'NONE', #11923, #9932, #11708 ) ;
#20068=EDGE_LOOP ( 'NONE', ( #18121, #20141, #4200, #15117 ) ) ;
#20069=EDGE_CURVE ( 'NONE', #16873, #18705, #8816, .T. ) ;
#20070=CARTESIAN_POINT ( 'NONE',  ( -3.127054932750481964, 32.93424481021354921, 68.50000000000000000 ) ) ;
#20073=LINE ( 'NONE', #8545, #17105 ) ;
#20074=ORIENTED_EDGE ( 'NONE', *, *, #21821, .T. ) ;
#20076=VECTOR ( 'NONE', #7892, 1000.000000000000000 ) ;
#20078=AXIS2_PLACEMENT_3D ( 'NONE', #64, #5108, #20031 ) ;
#20080=CARTESIAN_POINT ( 'NONE',  ( -28.90789898151107451, 6.496209923375007911, 7.643284004395015430 ) ) ;
#20081=CARTESIAN_POINT ( 'NONE',  ( -15.95292532278785913, -50.11873716947361856, 68.00000000000000000 ) ) ;
#20083=VERTEX_POINT ( 'NONE', #15580 ) ;
#20085=ORIENTED_EDGE ( 'NONE', *, *, #15798, .F. ) ;
#20086=CARTESIAN_POINT ( 'NONE',  ( -30.07540678000427548, 0.000000000000000000, 7.200000000000000178 ) ) ;
#20087=EDGE_CURVE ( 'NONE', #13533, #9687, #16289, .T. ) ;
#20088=CARTESIAN_POINT ( 'NONE',  ( 29.20000000000002061, -2.799282752659324025, 0.000000000000000000 ) ) ;
#20090=AXIS2_PLACEMENT_3D ( 'NONE', #9247, #2523, #19422 ) ;
#20091=CARTESIAN_POINT ( 'NONE',  ( 31.63662752439705272, 0.000000000000000000, 3.500000000000000000 ) ) ;
#20092=AXIS2_PLACEMENT_3D ( 'NONE', #11088, #11419, #18132 ) ;
#20093=VECTOR ( 'NONE', #17464, 1000.000000000000000 ) ;
#20094=TOROIDAL_SURFACE ( 'NONE', #11846, 0.7000000000000000666, 0.2999999999999999889 ) ;
#20095=ORIENTED_EDGE ( 'NONE', *, *, #9102, .T. ) ;
#20096=LINE ( 'NONE', #17050, #13940 ) ;
#20098=CARTESIAN_POINT ( 'NONE',  ( 0.000000000000000000, -69.04634676501045476, 3.500000000000000000 ) ) ;
#20099=ORIENTED_EDGE ( 'NONE', *, *, #9098, .F. ) ;
#20100=LINE ( 'NONE', #21567, #18090 ) ;
#20101=CARTESIAN_POINT ( 'NONE',  ( -15.95292532278785913, 50.11873716947361856, 109.6002446535588319 ) ) ;
#20102=ADVANCED_FACE ( 'NONE', ( #6904 ), #11789, .F. ) ;
#20104=DIRECTION ( 'NONE',  ( 1.000000000000000000, 0.000000000000000000, 0.000000000000000000 ) ) ;
#20106=ORIENTED_EDGE ( 'NONE', *, *, #17851, .F. ) ;
#20107=DIRECTION ( 'NONE',  ( 0.000000000000000000, 0.000000000000000000, -1.000000000000000000 ) ) ;
#20108=AXIS2_PLACEMENT_3D ( 'NONE', #15761, #3929, #5500 ) ;
#20109=EDGE_LOOP ( 'NONE', ( #1257, #11672, #3787, #19717 ) ) ;
#20110=FACE_OUTER_BOUND ( 'NONE', #2935, .T. ) ;
#20111=VECTOR ( 'NONE', #2448, 1000.000000000000000 ) ;
#20112=DIRECTION ( 'NONE',  ( 0.000000000000000000, -1.000000000000000000, 0.000000000000000000 ) ) ;
#20117=DIRECTION ( 'NONE',  ( -0.000000000000000000, 0.000000000000000000, 1.000000000000000000 ) ) ;
#20119=VECTOR ( 'NONE', #5854, 1000.000000000000000 ) ;
#20120=EDGE_LOOP ( 'NONE', ( #4011, #12663, #22016, #4189 ) ) ;
#20123=DIRECTION ( 'NONE',  ( -1.000000000000000000, -0.000000000000000000, 0.000000000000000000 ) ) ;
#20124=CARTESIAN_POINT ( 'NONE',  ( 30.07540678000427548, 0.000000000000000000, 7.200000000000000178 ) ) ;
#20128=ORIENTED_EDGE ( 'NONE', *, *, #11516, .F. ) ;
#20129=DIRECTION ( 'NONE',  ( 3.052134192567367925E-16, -1.000000000000000000, 0.000000000000000000 ) ) ;
#20130=LINE ( 'NONE', #4906, #22066 ) ;
#20132=EDGE_CURVE ( 'NONE', #1026, #11756, #5331, .T. ) ;
#20134=CARTESIAN_POINT ( 'NONE',  ( 0.000000000000000000, -68.44634676501046044, 7.200000000000000178 ) ) ;
#20135=ORIENTED_EDGE ( 'NONE', *, *, #9055, .T. ) ;
#20136=CYLINDRICAL_SURFACE ( 'NONE', #6762, 0.3000000000000016542 ) ;
#20140=DIRECTION ( 'NONE',  ( 0.000000000000000000, 0.000000000000000000, 1.000000000000000000 ) ) ;
#20141=ORIENTED_EDGE ( 'NONE', *, *, #10481, .T. ) ;
#20142=EDGE_CURVE ( 'NONE', #13909, #4856, #6673, .T. ) ;
#20143=CARTESIAN_POINT ( 'NONE',  ( -25.37540678000427263, -68.44634676501046044, 7.200000000000000178 ) ) ;
#20144=DIRECTION ( 'NONE',  ( 1.000000000000000000, 0.000000000000000000, 0.000000000000000000 ) ) ;
#20147=DIRECTION ( 'NONE',  ( -1.000000000000000000, -0.000000000000000000, 0.000000000000000000 ) ) ;
#20148=CARTESIAN_POINT ( 'NONE',  ( -27.67540678000428400, -36.74634676501047181, 13.79999999999999893 ) ) ;
#20149=DIRECTION ( 'NONE',  ( 1.000000000000000000, 0.000000000000000000, 0.000000000000000000 ) ) ;
#20150=DIRECTION ( 'NONE',  ( -0.1868663427273192512, -0.9823853469773029534, 0.000000000000000000 ) ) ;
#20151=CARTESIAN_POINT ( 'NONE',  ( 17.92752199202934094, 38.74634676501045760, 13.79999999999999893 ) ) ;
#20153=DIRECTION ( 'NONE',  ( 0.000000000000000000, 0.000000000000000000, -1.000000000000000000 ) ) ;
#20156=DIRECTION ( 'NONE',  ( 1.000000000000000000, 0.000000000000000000, 0.000000000000000000 ) ) ;
#20159=FACE_OUTER_BOUND ( 'NONE', #14615, .T. ) ;
#20160=ORIENTED_EDGE ( 'NONE', *, *, #18965, .F. ) ;
#20161=LINE ( 'NONE', #1573, #13171 ) ;
#20162=ADVANCED_FACE ( 'NONE', ( #13591 ), #18513, .T. ) ;
#20164=ORIENTED_EDGE ( 'NONE', *, *, #8002, .T. ) ;
#20166=ORIENTED_EDGE ( 'NONE', *, *, #2240, .F. ) ;
#20168=DIRECTION ( 'NONE',  ( 1.000000000000000000, 0.000000000000000000, 0.000000000000000000 ) ) ;
#20171=ORIENTED_EDGE ( 'NONE', *, *, #9918, .T. ) ;
#20174=CARTESIAN_POINT ( 'NONE',  ( -23.02398829872514341, 2.876860926786018791, 13.71498478227948503 ) ) ;
#20175=PLANE ( 'NONE',  #50 ) ;
#20176=DIRECTION ( 'NONE',  ( 1.000000000000000000, 0.000000000000000000, 0.000000000000000000 ) ) ;
#20178=EDGE_LOOP ( 'NONE', ( #16674, #7612, #17735, #16408 ) ) ;
#20181=DIRECTION ( 'NONE',  ( 1.000000000000000000, 0.000000000000000000, 0.000000000000000000 ) ) ;
#20182=CARTESIAN_POINT ( 'NONE',  ( -9.641460742840918030, 32.93424481021354921, 68.50000000000000000 ) ) ;
#20187=CIRCLE ( 'NONE', #9463, 0.2999999999999999334 ) ;
#20191=DIRECTION ( 'NONE',  ( 0.000000000000000000, 1.000000000000000000, -0.000000000000000000 ) ) ;
#20192=DIRECTION ( 'NONE',  ( 0.000000000000000000, 0.000000000000000000, 1.000000000000000000 ) ) ;
#20194=LINE ( 'NONE', #3637, #17363 ) ;
#20195=VERTEX_POINT ( 'NONE', #15481 ) ;
#20196=DIRECTION ( 'NONE',  ( 0.000000000000000000, -1.000000000000000000, 0.000000000000000000 ) ) ;
#20197=EDGE_CURVE ( 'NONE', #17364, #16494, #14646, .T. ) ;
#20198=DIRECTION ( 'NONE',  ( 0.000000000000000000, -0.000000000000000000, -1.000000000000000000 ) ) ;
#20202=ORIENTED_EDGE ( 'NONE', *, *, #12421, .T. ) ;
#20204=AXIS2_PLACEMENT_3D ( 'NONE', #7011, #13919, #9109 ) ;
#20207=DIRECTION ( 'NONE',  ( 0.000000000000000000, 0.000000000000000000, -1.000000000000000000 ) ) ;
#20208=CARTESIAN_POINT ( 'NONE',  ( 30.37540678000427619, -6.000000000000000000, 7.500000000000000000 ) ) ;
#20209=ORIENTED_EDGE ( 'NONE', *, *, #2205, .T. ) ;
#20211=VERTEX_POINT ( 'NONE', #54 ) ;
#20212=DIRECTION ( 'NONE',  ( 0.000000000000000000, 0.000000000000000000, 1.000000000000000000 ) ) ;
#20213=FACE_OUTER_BOUND ( 'NONE', #9947, .T. ) ;
#20214=EDGE_LOOP ( 'NONE', ( #1296, #18364, #2074, #20638 ) ) ;
#20216=ORIENTED_EDGE ( 'NONE', *, *, #20786, .T. ) ;
#20217=EDGE_CURVE ( 'NONE', #13749, #16971, #6452, .T. ) ;
#20218=VERTEX_POINT ( 'NONE', #4178 ) ;
#20219=CARTESIAN_POINT ( 'NONE',  ( -25.37540678000427263, -63.74634676501045050, 7.200000000000000178 ) ) ;
#20221=CIRCLE ( 'NONE', #3790, 0.2999999999999999334 ) ;
#20223=CARTESIAN_POINT ( 'NONE',  ( 3.127054932750481964, -32.61873716947361856, 68.00000000000000000 ) ) ;
#20224=CARTESIAN_POINT ( 'NONE',  ( -23.02398829872513986, -3.395978615688242996, 13.79999998357615532 ) ) ;
#20226=CARTESIAN_POINT ( 'NONE',  ( -15.95292532278785913, -34.11873716947361856, 68.00000000000000000 ) ) ;
#20228=EDGE_CURVE ( 'NONE', #19432, #4119, #5024, .T. ) ;
#20231=CYLINDRICAL_SURFACE ( 'NONE', #3885, 2.500000000000002220 ) ;
#20232=ORIENTED_EDGE ( 'NONE', *, *, #19757, .F. ) ;
#20233=VECTOR ( 'NONE', #788, 1000.000000000000000 ) ;
#20234=AXIS2_PLACEMENT_3D ( 'NONE', #21883, #4757, #13246 ) ;
#20236=VECTOR ( 'NONE', #8414, 1000.000000000000000 ) ;
#20237=ORIENTED_EDGE ( 'NONE', *, *, #16088, .T. ) ;
#20238=AXIS2_PLACEMENT_3D ( 'NONE', #17899, #1002, #13203 ) ;
#20240=DIRECTION ( 'NONE',  ( -0.000000000000000000, -1.000000000000000000, 0.000000000000000000 ) ) ;
#20243=ORIENTED_EDGE ( 'NONE', *, *, #17595, .T. ) ;
#20244=FACE_OUTER_BOUND ( 'NONE', #15774, .T. ) ;
#20245=EDGE_CURVE ( 'NONE', #3082, #12310, #472, .T. ) ;
#20246=EDGE_CURVE ( 'NONE', #9769, #706, #3585, .T. ) ;
#20248=VECTOR ( 'NONE', #6682, 1000.000000000000000 ) ;
#20249=AXIS2_PLACEMENT_3D ( 'NONE', #9301, #16105, #787 ) ;
#20252=DIRECTION ( 'NONE',  ( -0.000000000000000000, -0.000000000000000000, -1.000000000000000000 ) ) ;
#20253=VECTOR ( 'NONE', #8079, 1000.000000000000000 ) ;
#20255=DIRECTION ( 'NONE',  ( 0.000000000000000000, -1.000000000000000000, 0.000000000000000000 ) ) ;
#20256=DIRECTION ( 'NONE',  ( -0.000000000000000000, -1.000000000000000000, -0.000000000000000000 ) ) ;
#20257=DIRECTION ( 'NONE',  ( 1.000000000000000000, 0.000000000000000000, 0.000000000000000000 ) ) ;
#20258=DIRECTION ( 'NONE',  ( -1.000000000000000000, 0.000000000000000000, 0.000000000000000000 ) ) ;
#20261=DIRECTION ( 'NONE',  ( 1.000000000000000000, 0.000000000000000000, 0.000000000000000000 ) ) ;
#20262=EDGE_CURVE ( 'NONE', #12734, #21299, #1801, .T. ) ;
#20263=TOROIDAL_SURFACE ( 'NONE', #22064, 0.7000000000000000666, 0.2999999999999999889 ) ;
#20266=CARTESIAN_POINT ( 'NONE',  ( 4.127054932750481520, 33.93424481021354921, 68.00000000000000000 ) ) ;
#20267=ORIENTED_EDGE ( 'NONE', *, *, #12218, .F. ) ;
#20268=CARTESIAN_POINT ( 'NONE',  ( -15.95292532278785913, -50.11873716947361856, 13.99999999999999822 ) ) ;
#20269=VERTEX_POINT ( 'NONE', #15803 ) ;
#20270=AXIS2_PLACEMENT_3D ( 'NONE', #6361, #16278, #9470 ) ;
#20274=EDGE_CURVE ( 'NONE', #8409, #17039, #4668, .T. ) ;
#20275=ORIENTED_EDGE ( 'NONE', *, *, #3471, .T. ) ;
#20276=( NAMED_UNIT ( * ) PLANE_ANGLE_UNIT ( ) SI_UNIT ( $, .RADIAN. ) );
#20277=VERTEX_POINT ( 'NONE', #11000 ) ;
#20280=VERTEX_POINT ( 'NONE', #7221 ) ;
#20283=VECTOR ( 'NONE', #2698, 1000.000000000000000 ) ;
#20284=CYLINDRICAL_SURFACE ( 'NONE', #4951, 0.3000000000000016542 ) ;
#20290=PLANE ( 'NONE',  #8998 ) ;
#20291=DIRECTION ( 'NONE',  ( 0.000000000000000000, 0.000000000000000000, -1.000000000000000000 ) ) ;
#20293=VERTEX_POINT ( 'NONE', #19397 ) ;
#20295=CIRCLE ( 'NONE', #10647, 0.3000000000000016542 ) ;
#20296=ORIENTED_EDGE ( 'NONE', *, *, #19603, .T. ) ;
#20297=ORIENTED_EDGE ( 'NONE', *, *, #15335, .T. ) ;
#20302=EDGE_CURVE ( 'NONE', #17392, #7401, #4068, .T. ) ;
#20303=VECTOR ( 'NONE', #2556, 1000.000000000000000 ) ;
#20305=AXIS2_PLACEMENT_3D ( 'NONE', #6087, #11095, #11200 ) ;
#20307=ORIENTED_EDGE ( 'NONE', *, *, #20928, .T. ) ;
#20309=LINE ( 'NONE', #148, #14519 ) ;
#20311=CIRCLE ( 'NONE', #9539, 3.200000000000001510 ) ;
#20315=LINE ( 'NONE', #4767, #9969 ) ;
#20317=CARTESIAN_POINT ( 'NONE',  ( 0.000000000000000000, 51.61873716947361856, 68.00000000000000000 ) ) ;
#20318=VECTOR ( 'NONE', #1872, 1000.000000000000000 ) ;
#20320=CARTESIAN_POINT ( 'NONE',  ( 0.000000000000000000, -38.74634676501045760, 42.50000000000000000 ) ) ;
#20321=ORIENTED_EDGE ( 'NONE', *, *, #5988, .T. ) ;
#20322=FACE_OUTER_BOUND ( 'NONE', #21212, .T. ) ;
#20324=CIRCLE ( 'NONE', #19253, 0.5000000000000004441 ) ;
#20327=CARTESIAN_POINT ( 'NONE',  ( 23.32398829872514412, -5.683640910026986681, 13.79999999999999893 ) ) ;
#20328=DIRECTION ( 'NONE',  ( 0.000000000000000000, -0.000000000000000000, 1.000000000000000000 ) ) ;
#20329=EDGE_LOOP ( 'NONE', ( #20202, #13224, #8307, #20899 ) ) ;
#20332=LINE ( 'NONE', #15396, #18471 ) ;
#20333=ADVANCED_FACE ( 'NONE', ( #9323, #21203, #12320, #809 ), #10558, .T. ) ;
#20335=ADVANCED_FACE ( 'NONE', ( #17377 ), #20971, .T. ) ;
#20337=VERTEX_POINT ( 'NONE', #10789 ) ;
#20339=EDGE_CURVE ( 'NONE', #16591, #20218, #18947, .T. ) ;
#20343=LINE ( 'NONE', #6820, #17857 ) ;
#20345=VERTEX_POINT ( 'NONE', #20759 ) ;
#20346=DIRECTION ( 'NONE',  ( -1.000000000000000000, 0.000000000000000000, 0.000000000000000000 ) ) ;
#20350=ORIENTED_EDGE ( 'NONE', *, *, #21991, .F. ) ;
#20351=CARTESIAN_POINT ( 'NONE',  ( 0.000000000000000000, 69.04634676501045476, 3.799999999999999822 ) ) ;
#20352=CARTESIAN_POINT ( 'NONE',  ( -9.141460742840918030, -32.93424481021354921, 42.50000000000000000 ) ) ;
#20353=EDGE_CURVE ( 'NONE', #6383, #15755, #17517, .T. ) ;
#20357=EDGE_LOOP ( 'NONE', ( #3459, #9817, #18186, #21554 ) ) ;
#20359=EDGE_CURVE ( 'NONE', #15132, #1577, #12552, .T. ) ;
#20360=CIRCLE ( 'NONE', #16413, 1.000000000000000888 ) ;
#20362=ORIENTED_EDGE ( 'NONE', *, *, #2252, .F. ) ;
#20364=DIRECTION ( 'NONE',  ( 0.000000000000000000, -0.000000000000000000, -1.000000000000000000 ) ) ;
#20366=ORIENTED_EDGE ( 'NONE', *, *, #9180, .T. ) ;
#20367=DIRECTION ( 'NONE',  ( 0.000000000000000000, 0.000000000000000000, -1.000000000000000000 ) ) ;
#20369=ORIENTED_EDGE ( 'NONE', *, *, #12512, .T. ) ;
#20370=AXIS2_PLACEMENT_3D ( 'NONE', #373, #17607, #5439 ) ;
#20375=COLOUR_RGB ( '', 0.31764706, 0.68627451, 0.89019608) ;
#20376=VECTOR ( 'NONE', #15819, 1000.000000000000000 ) ;
#20379=CYLINDRICAL_SURFACE ( 'NONE', #1774, 0.5000000000000004441 ) ;
#20380=DIRECTION ( 'NONE',  ( 0.000000000000000000, 0.000000000000000000, -1.000000000000000000 ) ) ;
#20382=FACE_OUTER_BOUND ( 'NONE', #1185, .T. ) ;
#20383=EDGE_CURVE ( 'NONE', #1923, #9228, #21448, .T. ) ;
#20384=LINE ( 'NONE', #15441, #15781 ) ;
#20385=EDGE_CURVE ( 'NONE', #8021, #17208, #13583, .T. ) ;
#20388=ORIENTED_EDGE ( 'NONE', *, *, #1281, .T. ) ;
#20389=DIRECTION ( 'NONE',  ( -1.000000000000000000, 0.000000000000000000, -0.000000000000000000 ) ) ;
#20390=ORIENTED_EDGE ( 'NONE', *, *, #13104, .T. ) ;
#20391=DIRECTION ( 'NONE',  ( -1.000000000000000000, 0.000000000000000000, 0.000000000000000000 ) ) ;
#20393=VERTEX_POINT ( 'NONE', #4742 ) ;
#20394=ORIENTED_EDGE ( 'NONE', *, *, #16209, .F. ) ;
#20395=DIRECTION ( 'NONE',  ( 1.000000000000000000, 0.000000000000000000, 0.000000000000000000 ) ) ;
#20397=EDGE_LOOP ( 'NONE', ( #4390, #10958, #6655, #15474 ) ) ;
#20398=ORIENTED_EDGE ( 'NONE', *, *, #7203, .T. ) ;
#20399=ORIENTED_EDGE ( 'NONE', *, *, #18247, .F. ) ;
#20401=ORIENTED_EDGE ( 'NONE', *, *, #11112, .F. ) ;
#20402=AXIS2_PLACEMENT_3D ( 'NONE', #4201, #11022, #17842 ) ;
#20405=CARTESIAN_POINT ( 'NONE',  ( -1.836970198721029934E-16, -72.00000000000001421, 3.500000000000000000 ) ) ;
#20406=EDGE_LOOP ( 'NONE', ( #7848, #17218, #10822, #18768 ) ) ;
#20408=EDGE_CURVE ( 'NONE', #3983, #12670, #7532, .T. ) ;
#20409=DIRECTION ( 'NONE',  ( 1.000000000000000000, -3.052134192567374827E-16, 0.000000000000000000 ) ) ;
#20410=DIRECTION ( 'NONE',  ( 1.000000000000000000, 2.832483164223420229E-16, 0.000000000000000000 ) ) ;
#20411=EDGE_CURVE ( 'NONE', #16033, #19805, #21539, .T. ) ;
#20412=CARTESIAN_POINT ( 'NONE',  ( 29.37540678000427619, -6.000000000000000000, 3.799999999999999822 ) ) ;
#20413=CARTESIAN_POINT ( 'NONE',  ( 15.95292532278785913, 50.11873716947361856, 13.99999999999999822 ) ) ;
#20414=ORIENTED_EDGE ( 'NONE', *, *, #21721, .F. ) ;
#20417=ORIENTED_EDGE ( 'NONE', *, *, #14359, .T. ) ;
#20418=DIRECTION ( 'NONE',  ( 0.000000000000000000, 0.000000000000000000, 1.000000000000000000 ) ) ;
#20419=CARTESIAN_POINT ( 'NONE',  ( -29.33570773061603276, -2.657594995084290979, 0.02220324760240992637 ) ) ;
#20421=VECTOR ( 'NONE', #18575, 1000.000000000000000 ) ;
#20422=FACE_OUTER_BOUND ( 'NONE', #18378, .T. ) ;
#20425=VECTOR ( 'NONE', #8685, 1000.000000000000000 ) ;
#20427=VECTOR ( 'NONE', #592, 1000.000000000000000 ) ;
#20428=DIRECTION ( 'NONE',  ( 1.000000000000000000, 0.000000000000000000, 0.000000000000000000 ) ) ;
#20430=CARTESIAN_POINT ( 'NONE',  ( 0.000000000000000000, -32.61873716947361856, 68.00000000000000000 ) ) ;
#20432=ADVANCED_FACE ( 'NONE', ( #2713 ), #4631, .T. ) ;
#20433=CARTESIAN_POINT ( 'NONE',  ( 27.67540678000427690, 10.94079601157914539, 13.50000000000000000 ) ) ;
#20436=CARTESIAN_POINT ( 'NONE',  ( -29.13662752439705272, 5.000000000000000000, 7.500000000000000000 ) ) ;
#20437=VERTEX_POINT ( 'NONE', #3050 ) ;
#20438=CARTESIAN_POINT ( 'NONE',  ( -15.95292532278785913, -34.11873716947361856, 68.50000000000000000 ) ) ;
#20439=ORIENTED_EDGE ( 'NONE', *, *, #5541, .T. ) ;
#20440=CARTESIAN_POINT ( 'NONE',  ( 29.50000000000002132, 2.512390033608338236, -150.0833101980363722 ) ) ;
#20441=PLANE ( 'NONE',  #9478 ) ;
#20442=AXIS2_PLACEMENT_3D ( 'NONE', #12886, #9674, #14684 ) ;
#20443=CARTESIAN_POINT ( 'NONE',  ( 0.000000000000000000, 52.39333383871510108, 13.79999999999999893 ) ) ;
#20444=ORIENTED_EDGE ( 'NONE', *, *, #22050, .F. ) ;
#20446=EDGE_LOOP ( 'NONE', ( #2183, #4034, #6357, #1402 ) ) ;
#20448=DIRECTION ( 'NONE',  ( -1.000000000000000000, 0.000000000000000000, 0.000000000000000000 ) ) ;
#20452=ORIENTED_EDGE ( 'NONE', *, *, #7152, .F. ) ;
#20453=EDGE_CURVE ( 'NONE', #13600, #14227, #18372, .T. ) ;
#20454=ORIENTED_EDGE ( 'NONE', *, *, #1284, .F. ) ;
#20455=DIRECTION ( 'NONE',  ( 1.000000000000000000, 0.000000000000000000, 0.000000000000000000 ) ) ;
#20457=ORIENTED_EDGE ( 'NONE', *, *, #15782, .T. ) ;
#20458=DIRECTION ( 'NONE',  ( 0.000000000000000000, 0.000000000000000000, 1.000000000000000000 ) ) ;
#20461=DIRECTION ( 'NONE',  ( 3.052134192567367925E-16, 1.000000000000000000, 0.000000000000000000 ) ) ;
#20463=DIRECTION ( 'NONE',  ( 1.000000000000000000, -8.881784197001252323E-16, 0.000000000000000000 ) ) ;
#20466=AXIS2_PLACEMENT_3D ( 'NONE', #19251, #15653, #430 ) ;
#20470=DIRECTION ( 'NONE',  ( 1.000000000000000000, -0.000000000000000000, -0.000000000000000000 ) ) ;
#20471=DIRECTION ( 'NONE',  ( 1.000000000000000000, -1.334402673828314029E-15, 0.000000000000000000 ) ) ;
#20472=EDGE_LOOP ( 'NONE', ( #11606, #19932, #11551, #4335 ) ) ;
#20474=EDGE_CURVE ( 'NONE', #3329, #10953, #2159, .T. ) ;
#20477=DIRECTION ( 'NONE',  ( 1.000000000000000000, -2.832483164223420229E-16, 0.000000000000000000 ) ) ;
#20478=CARTESIAN_POINT ( 'NONE',  ( -0.000000000000000000, -69.00000000000000000, 1.500000000000000000 ) ) ;
#20482=EDGE_CURVE ( 'NONE', #19361, #19672, #12151, .T. ) ;
#20483=ORIENTED_EDGE ( 'NONE', *, *, #9474, .T. ) ;
#20486=DIRECTION ( 'NONE',  ( -1.000000000000000000, 2.832483164223434527E-16, 0.000000000000000000 ) ) ;
#20487=DIRECTION ( 'NONE',  ( -1.000000000000000000, 0.000000000000000000, 0.000000000000000000 ) ) ;
#20489=DIRECTION ( 'NONE',  ( 0.000000000000000000, 0.000000000000000000, -1.000000000000000000 ) ) ;
#20493=EDGE_CURVE ( 'NONE', #6037, #10046, #21483, .T. ) ;
#20495=CARTESIAN_POINT ( 'NONE',  ( 14.96174975910705918, 51.76873716947361714, 13.79999999999999716 ) ) ;
#20500=ORIENTED_EDGE ( 'NONE', *, *, #7728, .T. ) ;
#20501=DIRECTION ( 'NONE',  ( 0.000000000000000000, 0.000000000000000000, -1.000000000000000000 ) ) ;
#20504=FILL_AREA_STYLE ('',( #8648 ) ) ;
#20508=ORIENTED_EDGE ( 'NONE', *, *, #17304, .T. ) ;
#20509=CARTESIAN_POINT ( 'NONE',  ( -15.21174975910705207, -52.39333383871510108, 13.50000000000000000 ) ) ;
#20510=DIRECTION ( 'NONE',  ( 0.000000000000000000, 1.000000000000000000, 0.000000000000000000 ) ) ;
#20511=DIRECTION ( 'NONE',  ( -1.000000000000000000, 0.000000000000000000, 0.000000000000000000 ) ) ;
#20513=DIRECTION ( 'NONE',  ( 0.000000000000000000, 0.000000000000000000, 1.000000000000000000 ) ) ;
#20514=DIRECTION ( 'NONE',  ( 0.000000000000000000, 0.000000000000000000, 1.000000000000000000 ) ) ;
#20516=DIRECTION ( 'NONE',  ( 1.000000000000000000, 0.000000000000000000, 0.000000000000000000 ) ) ;
#20519=ORIENTED_EDGE ( 'NONE', *, *, #5382, .F. ) ;
#20521=EDGE_LOOP ( 'NONE', ( #21900, #22125, #19643, #2680 ) ) ;
#20524=CARTESIAN_POINT ( 'NONE',  ( -15.21174975910705207, 41.81054587065082728, 68.25000000000000000 ) ) ;
#20525=AXIS2_PLACEMENT_3D ( 'NONE', #2306, #5801, #17533 ) ;
#20528=EDGE_CURVE ( 'NONE', #4986, #4038, #6113, .T. ) ;
#20531=DIRECTION ( 'NONE',  ( 1.000000000000000000, 0.000000000000000000, 0.000000000000000000 ) ) ;
#20533=AXIS2_PLACEMENT_3D ( 'NONE', #57, #19998, #11470 ) ;
#20535=CARTESIAN_POINT ( 'NONE',  ( -8.641460742840918030, 33.43424481021354921, 68.00000000000000000 ) ) ;
#20536=ORIENTED_EDGE ( 'NONE', *, *, #8938, .F. ) ;
#20540=DIRECTION ( 'NONE',  ( 0.000000000000000000, 0.000000000000000000, 1.000000000000000000 ) ) ;
#20542=DIRECTION ( 'NONE',  ( 0.000000000000000000, 1.000000000000000000, 0.000000000000000000 ) ) ;
#20544=EDGE_LOOP ( 'NONE', ( #6306, #5390, #9531, #7294 ) ) ;
#20547=FACE_OUTER_BOUND ( 'NONE', #1933, .T. ) ;
#20549=EDGE_LOOP ( 'NONE', ( #21578, #13001, #4411, #19095 ) ) ;
#20550=ORIENTED_EDGE ( 'NONE', *, *, #3173, .T. ) ;
#20553=CARTESIAN_POINT ( 'NONE',  ( 23.32398829872514057, 7.118794219358020148E-15, 13.50000000000000000 ) ) ;
#20556=B_SPLINE_CURVE_WITH_KNOTS ( 'NONE', 3,
 ( #9165, #21157, #2453, #7385, #20919, #15756, #5829, #8841 ),
 .UNSPECIFIED., .F., .F.,
 ( 4, 2, 2, 4 ),
 ( 0.000000000000000000, 0.0002326155127978793088, 0.0004652310255957586176, 0.0009304620511915139827 ),
 .UNSPECIFIED. ) ;
#20558=CARTESIAN_POINT ( 'NONE',  ( 3.127054932750481964, 32.11873716947361856, 42.50000000000000711 ) ) ;
#20562=AXIS2_PLACEMENT_3D ( 'NONE', #17860, #18070, #844 ) ;
#20566=ORIENTED_EDGE ( 'NONE', *, *, #3683, .T. ) ;
#20567=DIRECTION ( 'NONE',  ( 0.000000000000000000, 0.000000000000000000, -1.000000000000000000 ) ) ;
#20568=DIRECTION ( 'NONE',  ( -0.000000000000000000, -0.000000000000000000, -1.000000000000000000 ) ) ;
#20573=CARTESIAN_POINT ( 'NONE',  ( 0.000000000000000000, 39.04634676501046187, 13.79999999999999893 ) ) ;
#20575=DIRECTION ( 'NONE',  ( 0.000000000000000000, 1.000000000000000000, 0.000000000000000000 ) ) ;
#20576=ORIENTED_EDGE ( 'NONE', *, *, #17467, .F. ) ;
#20578=FACE_OUTER_BOUND ( 'NONE', #15822, .T. ) ;
#20583=AXIS2_PLACEMENT_3D ( 'NONE', #18185, #7910, #14812 ) ;
#20588=DIRECTION ( 'NONE',  ( 0.000000000000000000, 0.000000000000000000, -1.000000000000000000 ) ) ;
#20589=ORIENTED_EDGE ( 'NONE', *, *, #9673, .T. ) ;
#20590=DIRECTION ( 'NONE',  ( 0.000000000000000000, 1.000000000000000000, 0.000000000000000000 ) ) ;
#20593=DIRECTION ( 'NONE',  ( 0.000000000000000000, 0.000000000000000000, -1.000000000000000000 ) ) ;
#20595=CARTESIAN_POINT ( 'NONE',  ( -15.95292532278785913, 50.11873716947361856, 68.00000000000000000 ) ) ;
#20596=AXIS2_PLACEMENT_3D ( 'NONE', #21726, #9300, #884 ) ;
#20598=EDGE_CURVE ( 'NONE', #17139, #17752, #19474, .T. ) ;
#20599=DIRECTION ( 'NONE',  ( 0.000000000000000000, -0.000000000000000000, -1.000000000000000000 ) ) ;
#20600=CARTESIAN_POINT ( 'NONE',  ( -14.96174975910705207, -51.76873716947361714, 13.79999999999999893 ) ) ;
#20602=PLANE ( 'NONE',  #12037 ) ;
#20612=EDGE_CURVE ( 'NONE', #20854, #11511, #16078, .T. ) ;
#20616=ADVANCED_FACE ( 'NONE', ( #15779 ), #9191, .T. ) ;
#20617=EDGE_LOOP ( 'NONE', ( #14153, #10587, #20910, #13551 ) ) ;
#20620=DIRECTION ( 'NONE',  ( 1.000000000000000000, 3.052134192567374827E-16, 0.000000000000000000 ) ) ;
#20622=AXIS2_PLACEMENT_3D ( 'NONE', #19434, #5905, #16407 ) ;
#20626=FACE_OUTER_BOUND ( 'NONE', #7585, .T. ) ;
#20627=DIRECTION ( 'NONE',  ( -1.000000000000000000, 0.000000000000000000, 0.000000000000000000 ) ) ;
#20629=DIRECTION ( 'NONE',  ( 0.000000000000000000, 0.000000000000000000, 1.000000000000000000 ) ) ;
#20632=DIRECTION ( 'NONE',  ( 0.000000000000000000, 0.000000000000000000, 1.000000000000000000 ) ) ;
#20634=ORIENTED_EDGE ( 'NONE', *, *, #12616, .T. ) ;
#20638=ORIENTED_EDGE ( 'NONE', *, *, #14084, .T. ) ;
#20639=VECTOR ( 'NONE', #15260, 1000.000000000000000 ) ;
#20641=CIRCLE ( 'NONE', #13463, 6.800000000000000711 ) ;
#20645=CARTESIAN_POINT ( 'NONE',  ( -15.21174975910705207, -52.11873716947361856, 68.00000000000000000 ) ) ;
#20646=AXIS2_PLACEMENT_3D ( 'NONE', #5190, #8330, #13777 ) ;
#20647=FACE_OUTER_BOUND ( 'NONE', #2902, .T. ) ;
#20650=DIRECTION ( 'NONE',  ( -0.000000000000000000, 0.000000000000000000, 1.000000000000000000 ) ) ;
#20653=FACE_OUTER_BOUND ( 'NONE', #11967, .T. ) ;
#20657=CARTESIAN_POINT ( 'NONE',  ( 29.17540678000427690, 63.74634676501045050, 7.500000000000000000 ) ) ;
#20660=DIRECTION ( 'NONE',  ( -0.000000000000000000, -0.000000000000000000, 1.000000000000000000 ) ) ;
#20661=CIRCLE ( 'NONE', #9919, 2.000000000000001776 ) ;
#20662=DIRECTION ( 'NONE',  ( 0.000000000000000000, 0.000000000000000000, -1.000000000000000000 ) ) ;
#20663=EDGE_CURVE ( 'NONE', #5533, #15579, #365, .T. ) ;
#20666=AXIS2_PLACEMENT_3D ( 'NONE', #7312, #13896, #12643 ) ;
#20668=DIRECTION ( 'NONE',  ( -1.000000000000000000, 0.000000000000000000, 0.000000000000000000 ) ) ;
#20669=CARTESIAN_POINT ( 'NONE',  ( 31.50000000000002132, -72.00000000000001421, 3.500000000000000000 ) ) ;
#20670=VECTOR ( 'NONE', #9017, 1000.000000000000000 ) ;
#20672=EDGE_LOOP ( 'NONE', ( #945, #3034, #16008, #68, #3484, #3774, #8824, #3941 ) ) ;
#20673=DIRECTION ( 'NONE',  ( 0.000000000000000000, 0.000000000000000000, 1.000000000000000000 ) ) ;
#20675=VECTOR ( 'NONE', #5586, 1000.000000000000000 ) ;
#20676=ORIENTED_EDGE ( 'NONE', *, *, #8247, .F. ) ;
#20677=CARTESIAN_POINT ( 'NONE',  ( -25.37540678000427263, -63.74634676501045050, 3.500000000000000000 ) ) ;
#20682=VECTOR ( 'NONE', #3844, 1000.000000000000000 ) ;
#20685=CARTESIAN_POINT ( 'NONE',  ( 23.02398829872490182, 2.928742984578568631, 13.54178985689097736 ) ) ;
#20687=CARTESIAN_POINT ( 'NONE',  ( 14.96174975910707161, 51.61873716947361856, 68.00000000000000000 ) ) ;
#20688=CARTESIAN_POINT ( 'NONE',  ( -3.127054932750481964, -32.61873716947361856, 68.00000000000000000 ) ) ;
#20690=ORIENTED_EDGE ( 'NONE', *, *, #17702, .T. ) ;
#20695=VECTOR ( 'NONE', #18601, 1000.000000000000000 ) ;
#20696=ORIENTED_EDGE ( 'NONE', *, *, #12072, .T. ) ;
#20699=VERTEX_POINT ( 'NONE', #21620 ) ;
#20701=ORIENTED_EDGE ( 'NONE', *, *, #3909, .F. ) ;
#20703=EDGE_LOOP ( 'NONE', ( #4133, #2644, #5355, #21471 ) ) ;
#20704=CARTESIAN_POINT ( 'NONE',  ( 18.22752199202934520, 38.74634676501045760, 13.79999999999999893 ) ) ;
#20705=DIRECTION ( 'NONE',  ( -0.000000000000000000, -0.000000000000000000, -1.000000000000000000 ) ) ;
#20708=CARTESIAN_POINT ( 'NONE',  ( 29.48703555828264911, 2.527994776753299533, 0.2022843821483596705 ) ) ;
#20709=EDGE_CURVE ( 'NONE', #20437, #8649, #4481, .T. ) ;
#20711=FACE_OUTER_BOUND ( 'NONE', #16586, .T. ) ;
#20713=LINE ( 'NONE', #5389, #11156 ) ;
#20714=EDGE_LOOP ( 'NONE', ( #1811, #19610, #21532 ) ) ;
#20716=FACE_OUTER_BOUND ( 'NONE', #12208, .T. ) ;
#20718=VERTEX_POINT ( 'NONE', #16108 ) ;
#20722=ORIENTED_EDGE ( 'NONE', *, *, #4496, .F. ) ;
#20726=CARTESIAN_POINT ( 'NONE',  ( 23.02398829872514341, -2.211005166398812616, 13.19999999999999041 ) ) ;
#20727=VERTEX_POINT ( 'NONE', #9303 ) ;
#20730=LINE ( 'NONE', #12294, #1990 ) ;
#20731=DIRECTION ( 'NONE',  ( -1.000000000000000000, 0.000000000000000000, 0.000000000000000000 ) ) ;
#20732=CARTESIAN_POINT ( 'NONE',  ( 23.02398829872514341, 2.333099608346429044, 13.47123417368288223 ) ) ;
#20736=AXIS2_PLACEMENT_3D ( 'NONE', #20781, #12242, #17728 ) ;
#20738=CARTESIAN_POINT ( 'NONE',  ( -23.02398829872513986, 2.211005166398795740, 13.19999999999999041 ) ) ;
#20739=EDGE_CURVE ( 'NONE', #7598, #6237, #6074, .T. ) ;
#20740=DIRECTION ( 'NONE',  ( 0.000000000000000000, 0.000000000000000000, 1.000000000000000000 ) ) ;
#20742=DIRECTION ( 'NONE',  ( 0.000000000000000000, 0.000000000000000000, 1.000000000000000000 ) ) ;
#20743=ADVANCED_FACE ( 'NONE', ( #7967 ), #19708, .F. ) ;
#20748=DIRECTION ( 'NONE',  ( 1.000000000000000000, 0.000000000000000000, 0.000000000000000000 ) ) ;
#20751=VERTEX_POINT ( 'NONE', #2923 ) ;
#20752=CARTESIAN_POINT ( 'NONE',  ( -14.96174975910705207, 32.10873716947361345, 13.05380965755523448 ) ) ;
#20753=AXIS2_PLACEMENT_3D ( 'NONE', #10969, #2583, #3632 ) ;
#20754=EDGE_CURVE ( 'NONE', #9603, #8176, #14769, .T. ) ;
#20757=CYLINDRICAL_SURFACE ( 'NONE', #21667, 1.999999999999991340 ) ;
#20758=EDGE_LOOP ( 'NONE', ( #3163, #8786, #1383, #8968 ) ) ;
#20759=CARTESIAN_POINT ( 'NONE',  ( -31.63662752439705272, 0.000000000000000000, 1.500000000000001332 ) ) ;
#20763=CARTESIAN_POINT ( 'NONE',  ( 0.000000000000000000, 50.00000000000000000, 0.000000000000000000 ) ) ;
#20767=PLANE ( 'NONE',  #20078 ) ;
#20768=AXIS2_PLACEMENT_3D ( 'NONE', #14426, #7738, #14539 ) ;
#20770=DIRECTION ( 'NONE',  ( 0.000000000000000000, 0.000000000000000000, 1.000000000000000000 ) ) ;
#20771=ORIENTED_EDGE ( 'NONE', *, *, #21612, .F. ) ;
#20772=EDGE_LOOP ( 'NONE', ( #1236, #9867, #11804, #14116 ) ) ;
#20773=ORIENTED_EDGE ( 'NONE', *, *, #14513, .T. ) ;
#20781=CARTESIAN_POINT ( 'NONE',  ( 25.37540678000429040, -36.74634676501047181, 42.50000000000000000 ) ) ;
#20783=VERTEX_POINT ( 'NONE', #17799 ) ;
#20784=CARTESIAN_POINT ( 'NONE',  ( -28.86382559268571057, -6.505889654322387194, 13.29319881794719294 ) ) ;
#20786=EDGE_CURVE ( 'NONE', #9883, #17139, #6855, .T. ) ;
#20789=CARTESIAN_POINT ( 'NONE',  ( 28.87540678000427619, -63.74634676501045050, 7.799999999999999822 ) ) ;
#20790=ORIENTED_EDGE ( 'NONE', *, *, #2679, .T. ) ;
#20791=CARTESIAN_POINT ( 'NONE',  ( 23.02398829872536368, 2.681050038336382446, 13.50121499737447728 ) ) ;
#20792=DIRECTION ( 'NONE',  ( -1.000000000000000000, -0.000000000000000000, 2.388292521039847891E-16 ) ) ;
#20793=VECTOR ( 'NONE', #19734, 1000.000000000000000 ) ;
#20796=ORIENTED_EDGE ( 'NONE', *, *, #586, .F. ) ;
#20799=AXIS2_PLACEMENT_3D ( 'NONE', #4508, #2953, #9886 ) ;
#20800=ORIENTED_EDGE ( 'NONE', *, *, #3831, .T. ) ;
#20804=VERTEX_POINT ( 'NONE', #6287 ) ;
#20805=ORIENTED_EDGE ( 'NONE', *, *, #19155, .T. ) ;
#20807=CARTESIAN_POINT ( 'NONE',  ( 29.13662752439705272, 0.000000000000000000, 7.500000000000000000 ) ) ;
#20808=ORIENTED_EDGE ( 'NONE', *, *, #12383, .T. ) ;
#20809=ORIENTED_EDGE ( 'NONE', *, *, #16724, .T. ) ;
#20810=VECTOR ( 'NONE', #17295, 1000.000000000000000 ) ;
#20811=CIRCLE ( 'NONE', #16865, 0.5000000000000004441 ) ;
#20812=EDGE_LOOP ( 'NONE', ( #2749, #1708, #9958, #2406 ) ) ;
#20813=CARTESIAN_POINT ( 'NONE',  ( -15.95292532278785913, 52.10286008774954780, 13.87499999999999822 ) ) ;
#20817=CYLINDRICAL_SURFACE ( 'NONE', #18501, 0.2999999999999999334 ) ;
#20822=DIRECTION ( 'NONE',  ( 1.000000000000000000, 0.000000000000000000, 0.000000000000000000 ) ) ;
#20827=VECTOR ( 'NONE', #6575, 1000.000000000000000 ) ;
#20829=ORIENTED_EDGE ( 'NONE', *, *, #765, .F. ) ;
#20831=DIRECTION ( 'NONE',  ( -1.000000000000000000, 0.000000000000000000, -0.000000000000000000 ) ) ;
#20835=ADVANCED_FACE ( 'NONE', ( #16330 ), #9643, .F. ) ;
#20841=CYLINDRICAL_SURFACE ( 'NONE', #15561, 0.2999999999999999334 ) ;
#20842=DIRECTION ( 'NONE',  ( 1.000000000000000000, 0.000000000000000000, 0.000000000000000000 ) ) ;
#20846=CARTESIAN_POINT ( 'NONE',  ( -29.37540678000427619, 6.000000000000000000, 7.200000000000000178 ) ) ;
#20847=DIRECTION ( 'NONE',  ( 0.000000000000000000, 0.000000000000000000, 1.000000000000000000 ) ) ;
#20849=CARTESIAN_POINT ( 'NONE',  ( -14.96174975910705207, -51.76873716947361714, 13.79999999999999716 ) ) ;
#20850=ORIENTED_EDGE ( 'NONE', *, *, #21069, .T. ) ;
#20852=DIRECTION ( 'NONE',  ( -0.000000000000000000, -0.000000000000000000, -1.000000000000000000 ) ) ;
#20854=VERTEX_POINT ( 'NONE', #13541 ) ;
#20855=EDGE_LOOP ( 'NONE', ( #21963, #282, #12404, #14312 ) ) ;
#20856=EDGE_CURVE ( 'NONE', #21585, #13976, #749, .T. ) ;
#20857=EDGE_CURVE ( 'NONE', #16560, #19513, #21497, .T. ) ;
#20858=ADVANCED_FACE ( 'NONE', ( #16781 ), #3026, .F. ) ;
#20864=DIRECTION ( 'NONE',  ( 0.000000000000000000, 0.000000000000000000, -1.000000000000000000 ) ) ;
#20865=CARTESIAN_POINT ( 'NONE',  ( -27.37540678000428684, -36.74634676501047181, 13.79999999999999893 ) ) ;
#20866=DIRECTION ( 'NONE',  ( -1.000000000000000000, 0.000000000000000000, 0.000000000000000000 ) ) ;
#20867=CARTESIAN_POINT ( 'NONE',  ( 25.37540678000427263, 63.74634676501045050, 13.19999999999999929 ) ) ;
#20869=FACE_OUTER_BOUND ( 'NONE', #10829, .T. ) ;
#20871=ORIENTED_EDGE ( 'NONE', *, *, #3663, .T. ) ;
#20873=FACE_OUTER_BOUND ( 'NONE', #3873, .T. ) ;
#20874=CARTESIAN_POINT ( 'NONE',  ( 29.50000000000001421, -69.00000000000000000, 0.1242640687119233311 ) ) ;
#20877=EDGE_LOOP ( 'NONE', ( #18720, #18140, #7662, #13218 ) ) ;
#20879=DIRECTION ( 'NONE',  ( 0.000000000000000000, 0.000000000000000000, 1.000000000000000000 ) ) ;
#20887=DIRECTION ( 'NONE',  ( 1.000000000000000000, 0.000000000000000000, 0.000000000000000000 ) ) ;
#20889=ORIENTED_EDGE ( 'NONE', *, *, #4591, .T. ) ;
#20890=DIRECTION ( 'NONE',  ( 0.000000000000000000, -1.000000000000000000, 0.000000000000000000 ) ) ;
#20891=DIRECTION ( 'NONE',  ( 1.000000000000000000, 0.000000000000000000, 0.000000000000000000 ) ) ;
#20892=FACE_OUTER_BOUND ( 'NONE', #9370, .T. ) ;
#20894=VERTEX_POINT ( 'NONE', #21841 ) ;
#20895=DIRECTION ( 'NONE',  ( -2.832483164223434527E-16, -1.000000000000000000, 0.000000000000000000 ) ) ;
#20897=CARTESIAN_POINT ( 'NONE',  ( 32.20000000000001705, -71.00000000000001421, 3.500000000000000000 ) ) ;
#20899=ORIENTED_EDGE ( 'NONE', *, *, #13247, .F. ) ;
#20902=DIRECTION ( 'NONE',  ( 1.000000000000000000, 0.000000000000000000, 0.000000000000000000 ) ) ;
#20904=ORIENTED_EDGE ( 'NONE', *, *, #13436, .T. ) ;
#20905=ORIENTED_EDGE ( 'NONE', *, *, #3727, .T. ) ;
#20906=DIRECTION ( 'NONE',  ( 0.000000000000000000, 0.000000000000000000, 1.000000000000000000 ) ) ;
#20907=EDGE_CURVE ( 'NONE', #19066, #12981, #9331, .T. ) ;
#20910=ORIENTED_EDGE ( 'NONE', *, *, #21199, .F. ) ;
#20911=AXIS2_PLACEMENT_3D ( 'NONE', #12592, #18690, #10926 ) ;
#20912=VECTOR ( 'NONE', #16004, 1000.000000000000000 ) ;
#20916=DIRECTION ( 'NONE',  ( -0.000000000000000000, 0.000000000000000000, 1.000000000000000000 ) ) ;
#20917=CARTESIAN_POINT ( 'NONE',  ( -27.67540678000427690, 10.94079601157914539, 13.79999999999999893 ) ) ;
#20919=CARTESIAN_POINT ( 'NONE',  ( 14.75227361591076836, 52.14371094704549847, 13.50000000000000000 ) ) ;
#20921=CARTESIAN_POINT ( 'NONE',  ( -3.127054932750481964, -32.11873716947361856, 109.6002446535588319 ) ) ;
#20925=EDGE_CURVE ( 'NONE', #1152, #21509, #8516, .T. ) ;
#20927=ORIENTED_EDGE ( 'NONE', *, *, #9038, .T. ) ;
#20928=EDGE_CURVE ( 'NONE', #5745, #18705, #6128, .T. ) ;
#20929=ORIENTED_EDGE ( 'NONE', *, *, #4515, .T. ) ;
#20931=LINE ( 'NONE', #12517, #3893 ) ;
#20933=VERTEX_POINT ( 'NONE', #15206 ) ;
#20934=ORIENTED_EDGE ( 'NONE', *, *, #14305, .T. ) ;
#20936=CARTESIAN_POINT ( 'NONE',  ( 23.02398829872513986, -2.624711895713193410, 13.63074282194498821 ) ) ;
#20938=AXIS2_PLACEMENT_3D ( 'NONE', #21394, #1214, #11184 ) ;
#20939=AXIS2_PLACEMENT_3D ( 'NONE', #9804, #10248, #2977 ) ;
#20941=VERTEX_POINT ( 'NONE', #15330 ) ;
#20943=FACE_OUTER_BOUND ( 'NONE', #9542, .T. ) ;
#20944=CARTESIAN_POINT ( 'NONE',  ( -17.95292532278785913, 34.11873716947361856, 68.00000000000000000 ) ) ;
#20945=EDGE_CURVE ( 'NONE', #18066, #8501, #3255, .T. ) ;
#20947=CARTESIAN_POINT ( 'NONE',  ( 28.57540678000427548, 6.776800961815481195, 13.50000000000000000 ) ) ;
#20950=VECTOR ( 'NONE', #17736, 1000.000000000000000 ) ;
#20951=AXIS2_PLACEMENT_3D ( 'NONE', #20752, #21086, #19065 ) ;
#20953=EDGE_CURVE ( 'NONE', #11867, #8198, #11852, .T. ) ;
#20954=CARTESIAN_POINT ( 'NONE',  ( -15.13056916446893396, -52.10286008774955491, 13.87500000000000178 ) ) ;
#20956=AXIS2_PLACEMENT_3D ( 'NONE', #3527, #10358, #17166 ) ;
#20957=CARTESIAN_POINT ( 'NONE',  ( 9.141460742840918030, 33.43424481021354921, 68.00000000000000000 ) ) ;
#20959=CARTESIAN_POINT ( 'NONE',  ( 29.50000000000002132, 0.000000000000000000, 1.500000000000000000 ) ) ;
#20961=ORIENTED_EDGE ( 'NONE', *, *, #5844, .T. ) ;
#20964=AXIS2_PLACEMENT_3D ( 'NONE', #4551, #9467, #7923 ) ;
#20967=CARTESIAN_POINT ( 'NONE',  ( -29.13662752439705272, 0.000000000000000000, 7.500000000000000000 ) ) ;
#20968=CARTESIAN_POINT ( 'NONE',  ( 29.50000000000002132, -69.00000000000000000, -150.0833101980363722 ) ) ;
#20969=CIRCLE ( 'NONE', #5255, 6.800000000000000711 ) ;
#20970=ORIENTED_EDGE ( 'NONE', *, *, #17595, .F. ) ;
#20971=CYLINDRICAL_SURFACE ( 'NONE', #16060, 2.000000000000000000 ) ;
#20974=LINE ( 'NONE', #10562, #2123 ) ;
#20976=CARTESIAN_POINT ( 'NONE',  ( -27.37540678000427619, 5.683640910026986681, 13.50000000000000000 ) ) ;
#20977=EDGE_CURVE ( 'NONE', #19696, #9561, #2993, .T. ) ;
#20980=CARTESIAN_POINT ( 'NONE',  ( -14.66174975910705136, 42.11054587065083155, 13.50000000000000000 ) ) ;
#20983=FACE_OUTER_BOUND ( 'NONE', #664, .T. ) ;
#20985=AXIS2_PLACEMENT_3D ( 'NONE', #21717, #1544, #13408 ) ;
#20986=CIRCLE ( 'NONE', #11317, 0.5000000000000004441 ) ;
#20990=DIRECTION ( 'NONE',  ( 0.000000000000000000, -1.000000000000000000, 0.000000000000000000 ) ) ;
#20991=AXIS2_PLACEMENT_3D ( 'NONE', #20917, #9730, #14509 ) ;
#20993=TOROIDAL_SURFACE ( 'NONE', #19976, 2.800000000000002043, 0.2999999999999999889 ) ;
#20995=ORIENTED_EDGE ( 'NONE', *, *, #8049, .F. ) ;
#20998=EDGE_CURVE ( 'NONE', #9803, #620, #18614, .T. ) ;
#21002=CIRCLE ( 'NONE', #14558, 0.5000000000000004441 ) ;
#21007=EDGE_LOOP ( 'NONE', ( #9819, #8623, #7976, #8995 ) ) ;
#21009=DIRECTION ( 'NONE',  ( 1.000000000000000000, 0.000000000000000000, 0.000000000000000000 ) ) ;
#21011=DIRECTION ( 'NONE',  ( 1.000000000000000000, 0.000000000000000000, 0.000000000000000000 ) ) ;
#21012=CARTESIAN_POINT ( 'NONE',  ( 25.37540678000429040, -36.74634676501047181, 42.50000000000000000 ) ) ;
#21016=VECTOR ( 'NONE', #11197, 1000.000000000000000 ) ;
#21017=EDGE_CURVE ( 'NONE', #16490, #9069, #4709, .T. ) ;
#21018=ORIENTED_EDGE ( 'NONE', *, *, #654, .F. ) ;
#21021=CARTESIAN_POINT ( 'NONE',  ( 0.000000000000000000, -39.04634676501046187, 13.79999999999999893 ) ) ;
#21029=EDGE_LOOP ( 'NONE', ( #19484, #15115, #5114, #4403 ) ) ;
#21030=AXIS2_PLACEMENT_3D ( 'NONE', #15967, #14400, #7609 ) ;
#21033=AXIS2_PLACEMENT_3D ( 'NONE', #2412, #830, #17845 ) ;
#21036=DIRECTION ( 'NONE',  ( -0.000000000000000000, 1.000000000000000000, -0.000000000000000000 ) ) ;
#21037=CARTESIAN_POINT ( 'NONE',  ( -15.21174975910705207, -32.10873716947361345, 68.25000000000000000 ) ) ;
#21038=CYLINDRICAL_SURFACE ( 'NONE', #11862, 0.2500000000000002220 ) ;
#21040=EDGE_CURVE ( 'NONE', #706, #8846, #6503, .T. ) ;
#21041=DIRECTION ( 'NONE',  ( -1.000000000000000000, 0.000000000000000000, 0.000000000000000000 ) ) ;
#21042=ORIENTED_EDGE ( 'NONE', *, *, #15370, .T. ) ;
#21043=AXIS2_PLACEMENT_3D ( 'NONE', #20967, #2046, #5766 ) ;
#21044=CIRCLE ( 'NONE', #5328, 1.000000000000000888 ) ;
#21046=FACE_BOUND ( 'NONE', #2342, .T. ) ;
#21047=CIRCLE ( 'NONE', #9604, 1.000000000000000000 ) ;
#21050=AXIS2_PLACEMENT_3D ( 'NONE', #7956, #11282, #4588 ) ;
#21053=ORIENTED_EDGE ( 'NONE', *, *, #18237, .F. ) ;
#21054=DIRECTION ( 'NONE',  ( -0.000000000000000000, -0.000000000000000000, -1.000000000000000000 ) ) ;
#21055=VERTEX_POINT ( 'NONE', #16522 ) ;
#21057=ORIENTED_EDGE ( 'NONE', *, *, #13941, .F. ) ;
#21058=DIRECTION ( 'NONE',  ( -1.000000000000000000, 0.000000000000000000, -0.000000000000000000 ) ) ;
#21061=AXIS2_PLACEMENT_3D ( 'NONE', #6265, #8046, #13052 ) ;
#21062=CARTESIAN_POINT ( 'NONE',  ( 23.02398829872513986, -3.528912754968634768, 13.50000000000000000 ) ) ;
#21063=VERTEX_POINT ( 'NONE', #4346 ) ;
#21064=LINE ( 'NONE', #17791, #6470 ) ;
#21067=AXIS2_PLACEMENT_3D ( 'NONE', #19249, #10519, #8842 ) ;
#21069=EDGE_CURVE ( 'NONE', #17577, #19547, #14835, .T. ) ;
#21070=DIRECTION ( 'NONE',  ( 1.000000000000000000, 0.000000000000000000, 0.000000000000000000 ) ) ;
#21073=EDGE_CURVE ( 'NONE', #21768, #14801, #2172, .T. ) ;
#21075=CARTESIAN_POINT ( 'NONE',  ( 28.86382559268571057, 6.505889654322387194, 13.29319881794719294 ) ) ;
#21076=CARTESIAN_POINT ( 'NONE',  ( 0.000000000000000000, 69.00000000000000000, 0.2999999999999947153 ) ) ;
#21077=CARTESIAN_POINT ( 'NONE',  ( -27.37540678000427619, 10.94079601157914539, 13.79999999999999893 ) ) ;
#21078=PLANE ( 'NONE',  #17173 ) ;
#21079=CIRCLE ( 'NONE', #7156, 3.800000000000004707 ) ;
#21080=EDGE_LOOP ( 'NONE', ( #5834, #12307, #6112, #3958 ) ) ;
#21084=ORIENTED_EDGE ( 'NONE', *, *, #12589, .T. ) ;
#21086=DIRECTION ( 'NONE',  ( -1.000000000000000000, 0.000000000000000000, 0.000000000000000000 ) ) ;
#21089=CIRCLE ( 'NONE', #1786, 0.5000000000000004441 ) ;
#21090=PLANE ( 'NONE',  #6700 ) ;
#21091=AXIS2_PLACEMENT_3D ( 'NONE', #5186, #13769, #20742 ) ;
#21096=DIRECTION ( 'NONE',  ( -0.000000000000000000, -0.000000000000000000, 1.000000000000000000 ) ) ;
#21097=CARTESIAN_POINT ( 'NONE',  ( 23.04692967985606700, 2.284552260428339032, 13.25236378595242392 ) ) ;
#21098=FACE_OUTER_BOUND ( 'NONE', #19511, .T. ) ;
#21099=DIRECTION ( 'NONE',  ( -0.000000000000000000, -1.000000000000000000, -0.000000000000000000 ) ) ;
#21100=LINE ( 'NONE', #18037, #11992 ) ;
#21105=EDGE_LOOP ( 'NONE', ( #2611, #18933, #4850, #327 ) ) ;
#21106=ORIENTED_EDGE ( 'NONE', *, *, #17161, .F. ) ;
#21108=DIRECTION ( 'NONE',  ( 1.000000000000000000, 0.000000000000000000, -0.000000000000000000 ) ) ;
#21109=AXIS2_PLACEMENT_3D ( 'NONE', #18506, #21989, #3404 ) ;
#21110=CARTESIAN_POINT ( 'NONE',  ( 9.641460742840918030, 32.61873716947361856, 68.00000000000000000 ) ) ;
#21113=EDGE_CURVE ( 'NONE', #6391, #9883, #13613, .T. ) ;
#21118=ADVANCED_FACE ( 'NONE', ( #8704 ), #12140, .T. ) ;
#21119=ORIENTED_EDGE ( 'NONE', *, *, #20754, .T. ) ;
#21120=CARTESIAN_POINT ( 'NONE',  ( -28.64417692495746692, -6.713479613976641502, 13.50000000000000000 ) ) ;
#21122=CYLINDRICAL_SURFACE ( 'NONE', #20090, 4.351418481279137218 ) ;
#21123=DIRECTION ( 'NONE',  ( 0.000000000000000000, 0.000000000000000000, 1.000000000000000000 ) ) ;
#21126=DIRECTION ( 'NONE',  ( -1.000000000000000000, 0.000000000000000000, 0.000000000000000000 ) ) ;
#21127=AXIS2_PLACEMENT_3D ( 'NONE', #4546, #18302, #8019 ) ;
#21130=DIRECTION ( 'NONE',  ( -0.000000000000000000, -0.000000000000000000, -1.000000000000000000 ) ) ;
#21131=ORIENTED_EDGE ( 'NONE', *, *, #9815, .T. ) ;
#21133=ORIENTED_EDGE ( 'NONE', *, *, #14958, .F. ) ;
#21136=ORIENTED_EDGE ( 'NONE', *, *, #5256, .F. ) ;
#21139=EDGE_CURVE ( 'NONE', #8815, #6391, #5050, .T. ) ;
#21141=ORIENTED_EDGE ( 'NONE', *, *, #16280, .T. ) ;
#21143=VERTEX_POINT ( 'NONE', #20558 ) ;
#21148=CIRCLE ( 'NONE', #8283, 0.5000000000000004441 ) ;
#21149=EDGE_CURVE ( 'NONE', #1748, #2230, #17192, .T. ) ;
#21151=EDGE_CURVE ( 'NONE', #13818, #18447, #3554, .T. ) ;
#21152=CARTESIAN_POINT ( 'NONE',  ( 25.37540678000427263, 63.74634676501045050, 7.500000000000000000 ) ) ;
#21153=AXIS2_PLACEMENT_3D ( 'NONE', #19183, #11003, #2275 ) ;
#21155=DIRECTION ( 'NONE',  ( 1.000000000000000000, 0.000000000000000000, 0.000000000000000000 ) ) ;
#21156=ORIENTED_EDGE ( 'NONE', *, *, #16663, .T. ) ;
#21157=CARTESIAN_POINT ( 'NONE',  ( 14.66174975910705847, 51.84675762924570108, 13.50000000000000355 ) ) ;
#21160=VERTEX_POINT ( 'NONE', #1526 ) ;
#21161=ADVANCED_FACE ( 'NONE', ( #22145 ), #14644, .T. ) ;
#21164=CIRCLE ( 'NONE', #17215, 0.5000000000000004441 ) ;
#21165=EDGE_LOOP ( 'NONE', ( #20074, #8792, #17640, #15055 ) ) ;
#21166=EDGE_LOOP ( 'NONE', ( #2850, #16354, #16844, #13039 ) ) ;
#21167=CARTESIAN_POINT ( 'NONE',  ( -3.127054932750481964, 32.61873716947361856, 109.6002446535588319 ) ) ;
#21171=AXIS2_PLACEMENT_3D ( 'NONE', #20317, #1609, #1506 ) ;
#21173=AXIS2_PLACEMENT_3D ( 'NONE', #19587, #17789, #2676 ) ;
#21175=EDGE_LOOP ( 'NONE', ( #16175, #10847, #4396, #18371 ) ) ;
#21176=LINE ( 'NONE', #10458, #3594 ) ;
#21177=EDGE_CURVE ( 'NONE', #18812, #2320, #394, .T. ) ;
#21178=EDGE_LOOP ( 'NONE', ( #1758, #1376, #11922, #8964 ) ) ;
#21181=DIRECTION ( 'NONE',  ( -0.000000000000000000, 0.000000000000000000, 1.000000000000000000 ) ) ;
#21183=DIRECTION ( 'NONE',  ( 1.000000000000000000, 0.000000000000000000, -0.000000000000000000 ) ) ;
#21184=TOROIDAL_SURFACE ( 'NONE', #11513, 1.000000000000000000, 0.5000000000000000000 ) ;
#21185=PLANE ( 'NONE',  #442 ) ;
#21187=PLANE ( 'NONE',  #9363 ) ;
#21188=CARTESIAN_POINT ( 'NONE',  ( -1.836970198721029934E-16, 72.00000000000001421, 3.500000000000000000 ) ) ;
#21191=VERTEX_POINT ( 'NONE', #8258 ) ;
#21193=CARTESIAN_POINT ( 'NONE',  ( 29.17540678000427690, 0.000000000000000000, 7.500000000000000000 ) ) ;
#21196=EDGE_CURVE ( 'NONE', #15364, #4630, #18760, .T. ) ;
#21197=ORIENTED_EDGE ( 'NONE', *, *, #11279, .F. ) ;
#21198=ORIENTED_EDGE ( 'NONE', *, *, #4055, .F. ) ;
#21199=EDGE_CURVE ( 'NONE', #421, #8448, #18627, .T. ) ;
#21200=DIRECTION ( 'NONE',  ( 0.000000000000000000, 1.000000000000000000, 0.000000000000000000 ) ) ;
#21201=DIRECTION ( 'NONE',  ( -0.000000000000000000, -0.000000000000000000, -1.000000000000000000 ) ) ;
#21202=ORIENTED_EDGE ( 'NONE', *, *, #66, .F. ) ;
#21203=FACE_OUTER_BOUND ( 'NONE', #6500, .T. ) ;
#21204=DIRECTION ( 'NONE',  ( 0.000000000000000000, -1.000000000000000000, -0.000000000000000000 ) ) ;
#21205=CARTESIAN_POINT ( 'NONE',  ( 28.87540678000427619, 63.74634676501045050, 13.19999999999999929 ) ) ;
#21206=CARTESIAN_POINT ( 'NONE',  ( -15.21174975910705207, -51.61873716947361856, 68.00000000000000000 ) ) ;
#21207=FACE_OUTER_BOUND ( 'NONE', #19671, .T. ) ;
#21208=ORIENTED_EDGE ( 'NONE', *, *, #20228, .T. ) ;
#21209=LINE ( 'NONE', #9010, #20427 ) ;
#21212=EDGE_LOOP ( 'NONE', ( #13931, #613, #3320, #5097 ) ) ;
#21213=ORIENTED_EDGE ( 'NONE', *, *, #12114, .T. ) ;
#21216=CARTESIAN_POINT ( 'NONE',  ( 18.05178606074127501, 38.87061083372239523, 13.49999999999999822 ) ) ;
#21217=EDGE_CURVE ( 'NONE', #9468, #12543, #20343, .T. ) ;
#21219=EDGE_CURVE ( 'NONE', #21351, #16066, #10014, .T. ) ;
#21224=FACE_OUTER_BOUND ( 'NONE', #19137, .T. ) ;
#21230=CARTESIAN_POINT ( 'NONE',  ( -14.96244602927845335, 51.84405746083547228, 13.82646097708239274 ) ) ;
#21232=EDGE_LOOP ( 'NONE', ( #2016, #2619, #20701, #5092 ) ) ;
#21234=DIRECTION ( 'NONE',  ( 0.000000000000000000, 0.000000000000000000, -1.000000000000000000 ) ) ;
#21238=CARTESIAN_POINT ( 'NONE',  ( -23.02398829872514341, -2.333099608346434373, 13.47123417368287868 ) ) ;
#21239=EDGE_CURVE ( 'NONE', #2536, #5528, #18475, .T. ) ;
#21241=EDGE_LOOP ( 'NONE', ( #4391, #7345, #18260, #16163 ) ) ;
#21242=DIRECTION ( 'NONE',  ( 1.000000000000000000, 0.000000000000000000, 0.000000000000000000 ) ) ;
#21244=ADVANCED_FACE ( 'NONE', ( #1864 ), #15722, .T. ) ;
#21247=ORIENTED_EDGE ( 'NONE', *, *, #18957, .F. ) ;
#21248=ORIENTED_EDGE ( 'NONE', *, *, #1563, .T. ) ;
#21250=CARTESIAN_POINT ( 'NONE',  ( 0.000000000000000000, 52.11873716947361856, 109.6002446535588319 ) ) ;
#21251=CARTESIAN_POINT ( 'NONE',  ( -9.641460742840918030, 33.43424481021354921, 68.50000000000000000 ) ) ;
#21252=DIRECTION ( 'NONE',  ( -0.000000000000000000, -0.000000000000000000, -1.000000000000000000 ) ) ;
#21253=EDGE_CURVE ( 'NONE', #20038, #2381, #6146, .T. ) ;
#21254=DIRECTION ( 'NONE',  ( 0.000000000000000000, 0.000000000000000000, 1.000000000000000000 ) ) ;
#21259=CARTESIAN_POINT ( 'NONE',  ( 23.32398829872514057, -2.157133568460768647, 7.500000000000000000 ) ) ;
#21260=EDGE_CURVE ( 'NONE', #1813, #7349, #19706, .T. ) ;
#21261=ADVANCED_FACE ( 'NONE', ( #19417 ), #391, .T. ) ;
#21265=AXIS2_PLACEMENT_3D ( 'NONE', #15840, #5581, #14057 ) ;
#21267=VECTOR ( 'NONE', #8760, 1000.000000000000000 ) ;
#21268=DIRECTION ( 'NONE',  ( -1.000000000000000000, 0.000000000000000000, 0.000000000000000000 ) ) ;
#21269=ORIENTED_EDGE ( 'NONE', *, *, #1147, .T. ) ;
#21270=EDGE_LOOP ( 'NONE', ( #2098, #6139, #15595, #14752 ) ) ;
#21279=AXIS2_PLACEMENT_3D ( 'NONE', #6522, #11299, #20153 ) ;
#21281=DIRECTION ( 'NONE',  ( -0.000000000000000000, 1.000000000000000000, 0.000000000000000000 ) ) ;
#21284=CARTESIAN_POINT ( 'NONE',  ( -3.627054932750481964, 33.43424481021354921, 7.321391277662001151 ) ) ;
#21286=CARTESIAN_POINT ( 'NONE',  ( 29.13662752439705272, 0.000000000000000000, 13.50000000000000000 ) ) ;
#21288=CARTESIAN_POINT ( 'NONE',  ( -25.37540678000427263, 66.94634676501046044, 13.50000000000000000 ) ) ;
#21292=CARTESIAN_POINT ( 'NONE',  ( 17.45292532278785913, -34.11873716947361856, 68.00000000000000000 ) ) ;
#21297=VECTOR ( 'NONE', #6354, 1000.000000000000000 ) ;
#21298=AXIS2_PLACEMENT_3D ( 'NONE', #14152, #9130, #21123 ) ;
#21299=VERTEX_POINT ( 'NONE', #10705 ) ;
#21301=CARTESIAN_POINT ( 'NONE',  ( -14.66174975910704958, -51.84664399969962290, 13.50000000000000178 ) ) ;
#21302=AXIS2_PLACEMENT_3D ( 'NONE', #7633, #2921, #13079 ) ;
#21308=FACE_OUTER_BOUND ( 'NONE', #13701, .T. ) ;
#21309=CARTESIAN_POINT ( 'NONE',  ( 15.00289696508457915, 51.98500081155935248, 13.86091301037357226 ) ) ;
#21310=CARTESIAN_POINT ( 'NONE',  ( 14.66174975910705847, 51.76873716947361714, 13.50000000000000000 ) ) ;
#21313=CIRCLE ( 'NONE', #14146, 3.200000000000001510 ) ;
#21319=VERTEX_POINT ( 'NONE', #15928 ) ;
#21320=CARTESIAN_POINT ( 'NONE',  ( 14.98852729675275164, 51.95836184682381287, 13.85634242029625973 ) ) ;
#21321=EDGE_CURVE ( 'NONE', #8649, #20699, #13581, .T. ) ;
#21325=AXIS2_PLACEMENT_3D ( 'NONE', #21021, #12049, #5708 ) ;
#21326=CARTESIAN_POINT ( 'NONE',  ( 15.95292532278785913, 52.39333383871510108, 13.50000000000000000 ) ) ;
#21327=VECTOR ( 'NONE', #885, 1000.000000000000000 ) ;
#21328=VERTEX_POINT ( 'NONE', #14265 ) ;
#21329=DIRECTION ( 'NONE',  ( 1.000000000000000000, 0.000000000000000000, 0.000000000000000000 ) ) ;
#21333=CARTESIAN_POINT ( 'NONE',  ( -23.02398829872513986, 7.027230193580998154E-15, 42.50000000000000000 ) ) ;
#21334=CARTESIAN_POINT ( 'NONE',  ( 23.02398829872513986, -3.528912754968634768, 13.79999999999999893 ) ) ;
#21335=DIRECTION ( 'NONE',  ( -0.000000000000000000, 1.000000000000000000, 0.000000000000000000 ) ) ;
#21336=VERTEX_POINT ( 'NONE', #8801 ) ;
#21337=DIRECTION ( 'NONE',  ( 0.000000000000000000, 0.000000000000000000, 1.000000000000000000 ) ) ;
#21338=DIRECTION ( 'NONE',  ( 0.000000000000000000, 0.000000000000000000, 1.000000000000000000 ) ) ;
#21340=DIRECTION ( 'NONE',  ( 0.000000000000000000, 0.000000000000000000, 1.000000000000000000 ) ) ;
#21341=CARTESIAN_POINT ( 'NONE',  ( 25.37540678000427263, -68.74634676501045760, 3.799999999999999822 ) ) ;
#21345=AXIS2_PLACEMENT_3D ( 'NONE', #18251, #13211, #14456 ) ;
#21347=CARTESIAN_POINT ( 'NONE',  ( 0.000000000000000000, 68.74634676501045760, 7.200000000000000178 ) ) ;
#21348=VECTOR ( 'NONE', #4354, 1000.000000000000000 ) ;
#21351=VERTEX_POINT ( 'NONE', #18992 ) ;
#21353=VERTEX_POINT ( 'NONE', #1956 ) ;
#21355=DIRECTION ( 'NONE',  ( -0.000000000000000000, 0.000000000000000000, -1.000000000000000000 ) ) ;
#21360=TOROIDAL_SURFACE ( 'NONE', #1322, 6.800000000000001599, 0.2999999999999999889 ) ;
#21362=ORIENTED_EDGE ( 'NONE', *, *, #21624, .F. ) ;
#21366=CIRCLE ( 'NONE', #10980, 2.000000000000000000 ) ;
#21367=DIRECTION ( 'NONE',  ( 0.000000000000000000, -1.000000000000000000, 0.000000000000000000 ) ) ;
#21368=CIRCLE ( 'NONE', #17078, 1.000000000000000888 ) ;
#21369=LINE ( 'NONE', #17768, #20303 ) ;
#21373=DIRECTION ( 'NONE',  ( -1.000000000000000000, -0.000000000000000000, -0.000000000000000000 ) ) ;
#21374=LINE ( 'NONE', #7615, #18189 ) ;
#21375=CARTESIAN_POINT ( 'NONE',  ( 25.37540678000426908, 39.04634676501046187, 13.50000000000000000 ) ) ;
#21377=CIRCLE ( 'NONE', #9577, 2.274596669241485181 ) ;
#21378=CARTESIAN_POINT ( 'NONE',  ( 30.07540678000427548, 6.000000000000000000, 7.500000000000000000 ) ) ;
#21380=CIRCLE ( 'NONE', #1718, 0.5000000000000000000 ) ;
#21381=VERTEX_POINT ( 'NONE', #18178 ) ;
#21387=ORIENTED_EDGE ( 'NONE', *, *, #20001, .F. ) ;
#21389=CARTESIAN_POINT ( 'NONE',  ( -29.13662752439705272, 5.299999999999999822, 7.500000000000000000 ) ) ;
#21392=VECTOR ( 'NONE', #18370, 1000.000000000000000 ) ;
#21393=EDGE_CURVE ( 'NONE', #15847, #5647, #21559, .T. ) ;
#21394=CARTESIAN_POINT ( 'NONE',  ( -25.37540678000427263, -63.74634676501045050, 13.19999999999999929 ) ) ;
#21395=DIRECTION ( 'NONE',  ( -1.000000000000000000, 0.000000000000000000, -0.000000000000000000 ) ) ;
#21396=CARTESIAN_POINT ( 'NONE',  ( -9.641460742840918030, -32.93424481021354921, 68.00000000000000000 ) ) ;
#21404=FACE_OUTER_BOUND ( 'NONE', #3846, .T. ) ;
#21407=ORIENTED_EDGE ( 'NONE', *, *, #18245, .F. ) ;
#21408=DIRECTION ( 'NONE',  ( -0.000000000000000000, -0.000000000000000000, -1.000000000000000000 ) ) ;
#21409=CIRCLE ( 'NONE', #10339, 1.999999999999991340 ) ;
#21412=ORIENTED_EDGE ( 'NONE', *, *, #11585, .T. ) ;
#21416=CIRCLE ( 'NONE', #16391, 0.2999999999999999334 ) ;
#21417=ORIENTED_EDGE ( 'NONE', *, *, #18273, .F. ) ;
#21418=CIRCLE ( 'NONE', #2104, 1.299999999999999156 ) ;
#21420=DIRECTION ( 'NONE',  ( 1.000000000000000000, 0.000000000000000000, 0.000000000000000000 ) ) ;
#21421=ADVANCED_FACE ( 'NONE', ( #2861 ), #17951, .T. ) ;
#21422=DIRECTION ( 'NONE',  ( 1.000000000000000000, 0.000000000000000000, 0.000000000000000000 ) ) ;
#21423=ORIENTED_EDGE ( 'NONE', *, *, #15529, .T. ) ;
#21424=EDGE_CURVE ( 'NONE', #11393, #10096, #5425, .T. ) ;
#21425=FACE_OUTER_BOUND ( 'NONE', #5237, .T. ) ;
#21427=CARTESIAN_POINT ( 'NONE',  ( 14.96174975910705918, 51.83053110199097091, 13.82013245744073160 ) ) ;
#21428=CARTESIAN_POINT ( 'NONE',  ( -29.13662752439705272, 0.000000000000000000, 13.50000000000000000 ) ) ;
#21429=CARTESIAN_POINT ( 'NONE',  ( -23.02398829872513630, 2.333754220862760409, 13.47170153661532943 ) ) ;
#21432=DIRECTION ( 'NONE',  ( -0.000000000000000000, -0.000000000000000000, -1.000000000000000000 ) ) ;
#21433=CARTESIAN_POINT ( 'NONE',  ( 17.45292532278785913, 0.000000000000000000, 68.50000000000000000 ) ) ;
#21435=VERTEX_POINT ( 'NONE', #8006 ) ;
#21437=CYLINDRICAL_SURFACE ( 'NONE', #9568, 0.2999999999999999334 ) ;
#21438=CARTESIAN_POINT ( 'NONE',  ( -32.50000000000002132, 71.00000000000001421, 3.200000000000000178 ) ) ;
#21439=EDGE_CURVE ( 'NONE', #13135, #19461, #15284, .T. ) ;
#21440=EDGE_LOOP ( 'NONE', ( #4637, #9422, #5711, #7697 ) ) ;
#21441=CIRCLE ( 'NONE', #11766, 0.5000000000000004441 ) ;
#21443=CIRCLE ( 'NONE', #4276, 4.351418481279133665 ) ;
#21445=AXIS2_PLACEMENT_3D ( 'NONE', #3656, #9115, #14036 ) ;
#21446=ORIENTED_EDGE ( 'NONE', *, *, #20612, .F. ) ;
#21448=( BOUNDED_CURVE ( )  B_SPLINE_CURVE ( 3, ( #6205, #12773, #18033, #14570 ),
 .UNSPECIFIED., .F., .T. ) 
 B_SPLINE_CURVE_WITH_KNOTS ( ( 4, 4 ),
 ( 3.141592653589793116, 4.712388980384689674 ),
 .UNSPECIFIED. ) 
 CURVE ( )  GEOMETRIC_REPRESENTATION_ITEM ( )  RATIONAL_B_SPLINE_CURVE ( ( 1.000000000000000000, 0.8047378541243649375, 0.8047378541243649375, 1.000000000000000000 ) ) 
 REPRESENTATION_ITEM ( '' )  );
#21449=DIRECTION ( 'NONE',  ( 0.000000000000000000, 0.000000000000000000, 1.000000000000000000 ) ) ;
#21453=FACE_OUTER_BOUND ( 'NONE', #10990, .T. ) ;
#21455=VERTEX_POINT ( 'NONE', #19859 ) ;
#21456=CARTESIAN_POINT ( 'NONE',  ( -25.37540678000427263, -66.94634676501046044, 13.50000000000000000 ) ) ;
#21457=ADVANCED_FACE ( 'NONE', ( #19522 ), #15716, .F. ) ;
#21458=CARTESIAN_POINT ( 'NONE',  ( 29.13662752439705272, 4.700000000000000178, 3.500000000000000000 ) ) ;
#21461=ORIENTED_EDGE ( 'NONE', *, *, #1690, .F. ) ;
#21462=CYLINDRICAL_SURFACE ( 'NONE', #15204, 0.5000000000000004441 ) ;
#21466=ORIENTED_EDGE ( 'NONE', *, *, #6310, .T. ) ;
#21470=CARTESIAN_POINT ( 'NONE',  ( 3.627054932750481964, -32.61873716947361856, 68.50000000000000000 ) ) ;
#21471=ORIENTED_EDGE ( 'NONE', *, *, #18932, .F. ) ;
#21473=CARTESIAN_POINT ( 'NONE',  ( -15.16859876043988464, 52.00603549157913363, 13.50000000000000000 ) ) ;
#21474=DIRECTION ( 'NONE',  ( -1.000000000000000000, -0.000000000000000000, -0.000000000000000000 ) ) ;
#21475=ORIENTED_EDGE ( 'NONE', *, *, #8618, .T. ) ;
#21477=EDGE_CURVE ( 'NONE', #5864, #4912, #3950, .T. ) ;
#21478=EDGE_LOOP ( 'NONE', ( #6195, #15041, #6064, #15245 ) ) ;
#21481=CARTESIAN_POINT ( 'NONE',  ( 29.13662752439705272, 0.000000000000000000, 13.50000000000000000 ) ) ;
#21483=CIRCLE ( 'NONE', #12513, 0.2999999999999999334 ) ;
#21484=LINE ( 'NONE', #3645, #1306 ) ;
#21485=DIRECTION ( 'NONE',  ( 0.000000000000000000, 0.000000000000000000, -1.000000000000000000 ) ) ;
#21489=CARTESIAN_POINT ( 'NONE',  ( -32.20000000000001705, -71.00000000000001421, 1.500000000000000000 ) ) ;
#21490=CARTESIAN_POINT ( 'NONE',  ( 29.13662752439705272, 0.000000000000000000, -18.50000000000000000 ) ) ;
#21497=CIRCLE ( 'NONE', #43, 1.984122918275925462 ) ;
#21498=ORIENTED_EDGE ( 'NONE', *, *, #16397, .T. ) ;
#21499=ORIENTED_EDGE ( 'NONE', *, *, #16470, .T. ) ;
#21500=CARTESIAN_POINT ( 'NONE',  ( 29.13662752439705272, 0.000000000000000000, 13.19999999999999929 ) ) ;
#21502=ORIENTED_EDGE ( 'NONE', *, *, #18245, .T. ) ;
#21504=AXIS2_PLACEMENT_3D ( 'NONE', #10563, #19076, #19502 ) ;
#21509=VERTEX_POINT ( 'NONE', #6006 ) ;
#21511=CARTESIAN_POINT ( 'NONE',  ( 18.22752199202934520, -50.11873716947361856, 13.50000000000000000 ) ) ;
#21514=LINE ( 'NONE', #4712, #15669 ) ;
#21515=DIRECTION ( 'NONE',  ( -1.000000000000000000, 0.000000000000000000, 0.000000000000000000 ) ) ;
#21518=CARTESIAN_POINT ( 'NONE',  ( 3.127054932750481964, 32.61873716947361856, 68.00000000000000000 ) ) ;
#21519=LINE ( 'NONE', #21077, #11243 ) ;
#21520=ADVANCED_FACE ( 'NONE', ( #2623 ), #12671, .T. ) ;
#21522=ORIENTED_EDGE ( 'NONE', *, *, #6240, .F. ) ;
#21523=FACE_OUTER_BOUND ( 'NONE', #18999, .T. ) ;
#21525=DIRECTION ( 'NONE',  ( 1.000000000000000000, 0.000000000000000000, 0.000000000000000000 ) ) ;
#21526=VERTEX_POINT ( 'NONE', #3523 ) ;
#21527=ORIENTED_EDGE ( 'NONE', *, *, #2706, .F. ) ;
#21531=ADVANCED_FACE ( 'NONE', ( #15257 ), #2512, .T. ) ;
#21532=ORIENTED_EDGE ( 'NONE', *, *, #14926, .F. ) ;
#21535=CARTESIAN_POINT ( 'NONE',  ( 15.14085429618050682, -52.10286008412593617, 13.87499998596578976 ) ) ;
#21536=AXIS2_PLACEMENT_3D ( 'NONE', #13177, #16293, #7833 ) ;
#21538=ORIENTED_EDGE ( 'NONE', *, *, #13050, .F. ) ;
#21539=LINE ( 'NONE', #1144, #2880 ) ;
#21541=DIRECTION ( 'NONE',  ( 0.000000000000000000, 0.000000000000000000, -1.000000000000000000 ) ) ;
#21544=ORIENTED_EDGE ( 'NONE', *, *, #17486, .T. ) ;
#21545=FACE_OUTER_BOUND ( 'NONE', #12261, .T. ) ;
#21547=ORIENTED_EDGE ( 'NONE', *, *, #11157, .T. ) ;
#21549=ORIENTED_EDGE ( 'NONE', *, *, #586, .T. ) ;
#21550=CARTESIAN_POINT ( 'NONE',  ( 15.21174975910707161, 51.61873716947361856, 68.00000000000000000 ) ) ;
#21552=CARTESIAN_POINT ( 'NONE',  ( 25.37540678000426908, 39.04634676501046187, 13.50000000000000000 ) ) ;
#21553=ADVANCED_FACE ( 'NONE', ( #9901 ), #13354, .F. ) ;
#21554=ORIENTED_EDGE ( 'NONE', *, *, #9815, .F. ) ;
#21556=EDGE_CURVE ( 'NONE', #1513, #13945, #17871, .T. ) ;
#21558=ORIENTED_EDGE ( 'NONE', *, *, #15899, .T. ) ;
#21559=LINE ( 'NONE', #827, #18580 ) ;
#21564=LINE ( 'NONE', #11355, #4704 ) ;
#21567=CARTESIAN_POINT ( 'NONE',  ( -3.627054932750481964, -32.11873716947361856, 68.00000000000000000 ) ) ;
#21568=CARTESIAN_POINT ( 'NONE',  ( -14.96174975910705207, 41.81054587065082728, 13.79999999999999893 ) ) ;
#21572=ORIENTED_EDGE ( 'NONE', *, *, #21424, .F. ) ;
#21573=CARTESIAN_POINT ( 'NONE',  ( -30.67540678000428045, 0.000000000000000000, 3.799999999999999822 ) ) ;
#21574=EDGE_LOOP ( 'NONE', ( #18629, #5142, #17787, #21980 ) ) ;
#21576=CARTESIAN_POINT ( 'NONE',  ( -23.02398829872513986, -2.157133568460768647, 13.19999999999999929 ) ) ;
#21577=EDGE_LOOP ( 'NONE', ( #2349, #12816, #6821, #5846 ) ) ;
#21578=ORIENTED_EDGE ( 'NONE', *, *, #10429, .T. ) ;
#21580=CARTESIAN_POINT ( 'NONE',  ( -15.07123959906592248, 52.06981400416638905, 13.87294810141926149 ) ) ;
#21582=CARTESIAN_POINT ( 'NONE',  ( -17.45292532278785913, -34.11873716947361856, 68.50000000000000000 ) ) ;
#21583=EDGE_CURVE ( 'NONE', #21328, #22135, #20096, .T. ) ;
#21584=( BOUNDED_CURVE ( )  B_SPLINE_CURVE ( 3, ( #18211, #4446, #11588, #21916 ),
 .UNSPECIFIED., .F., .T. ) 
 B_SPLINE_CURVE_WITH_KNOTS ( ( 4, 4 ),
 ( 0.000000000000000000, 1.570796326794896558 ),
 .UNSPECIFIED. ) 
 CURVE ( )  GEOMETRIC_REPRESENTATION_ITEM ( )  RATIONAL_B_SPLINE_CURVE ( ( 1.000000000000000000, 0.8047378541243649375, 0.8047378541243649375, 1.000000000000000000 ) ) 
 REPRESENTATION_ITEM ( '' )  );
#21585=VERTEX_POINT ( 'NONE', #16714 ) ;
#21587=ORIENTED_EDGE ( 'NONE', *, *, #4705, .F. ) ;
#21590=CARTESIAN_POINT ( 'NONE',  ( -23.02398829872514696, -2.388551872609015359, 13.39771463486667358 ) ) ;
#21592=DIRECTION ( 'NONE',  ( -1.000000000000000000, 0.000000000000000000, 0.000000000000000000 ) ) ;
#21597=DIRECTION ( 'NONE',  ( -0.000000000000000000, -0.000000000000000000, 1.000000000000000000 ) ) ;
#21602=LINE ( 'NONE', #9623, #15687 ) ;
#21603=DIRECTION ( 'NONE',  ( 0.000000000000000000, 1.000000000000000000, 0.000000000000000000 ) ) ;
#21604=ORIENTED_EDGE ( 'NONE', *, *, #20482, .F. ) ;
#21608=ORIENTED_EDGE ( 'NONE', *, *, #15515, .F. ) ;
#21609=ORIENTED_EDGE ( 'NONE', *, *, #2372, .F. ) ;
#21610=FACE_OUTER_BOUND ( 'NONE', #1754, .T. ) ;
#21612=EDGE_CURVE ( 'NONE', #2108, #13253, #12860, .T. ) ;
#21617=DIRECTION ( 'NONE',  ( -0.000000000000000000, 0.000000000000000000, 1.000000000000000000 ) ) ;
#21618=LINE ( 'NONE', #16548, #16274 ) ;
#21619=DIRECTION ( 'NONE',  ( 0.000000000000000000, 0.000000000000000000, -1.000000000000000000 ) ) ;
#21620=CARTESIAN_POINT ( 'NONE',  ( 9.141460742840918030, -32.93424481021354921, 68.00000000000000000 ) ) ;
#21622=DIRECTION ( 'NONE',  ( 0.000000000000000000, 0.000000000000000000, 1.000000000000000000 ) ) ;
#21624=EDGE_CURVE ( 'NONE', #7044, #9803, #13228, .T. ) ;
#21625=CARTESIAN_POINT ( 'NONE',  ( 25.37540678000427263, -63.74634676501045050, 3.500000000000000000 ) ) ;
#21626=AXIS2_PLACEMENT_3D ( 'NONE', #7992, #11549, #3387 ) ;
#21627=VERTEX_POINT ( 'NONE', #18389 ) ;
#21628=DIRECTION ( 'NONE',  ( 1.000000000000000000, 0.000000000000000000, 0.000000000000000000 ) ) ;
#21637=EDGE_CURVE ( 'NONE', #19513, #712, #13598, .T. ) ;
#21638=AXIS2_PLACEMENT_3D ( 'NONE', #1559, #21847, #9859 ) ;
#21641=CARTESIAN_POINT ( 'NONE',  ( 0.000000000000000000, 0.000000000000000000, 7.500000000000000000 ) ) ;
#21643=ORIENTED_EDGE ( 'NONE', *, *, #12737, .F. ) ;
#21645=EDGE_CURVE ( 'NONE', #2851, #5528, #18235, .T. ) ;
#21646=CARTESIAN_POINT ( 'NONE',  ( 9.641460742840918030, -32.61873716947361856, 68.00000000000000000 ) ) ;
#21647=CARTESIAN_POINT ( 'NONE',  ( 3.127054932750481964, 32.61873716947361856, 68.00000000000000000 ) ) ;
#21648=CYLINDRICAL_SURFACE ( 'NONE', #15911, 0.5000000000000000000 ) ;
#21649=ORIENTED_EDGE ( 'NONE', *, *, #8718, .F. ) ;
#21652=VERTEX_POINT ( 'NONE', #13469 ) ;
#21653=VECTOR ( 'NONE', #20542, 1000.000000000000000 ) ;
#21654=EDGE_LOOP ( 'NONE', ( #20589, #11997, #8094, #7490 ) ) ;
#21655=DIRECTION ( 'NONE',  ( 1.000000000000000000, 0.000000000000000000, -2.388292521039847891E-16 ) ) ;
#21658=CARTESIAN_POINT ( 'NONE',  ( -25.37540678000427263, 63.74634676501045050, 7.500000000000000000 ) ) ;
#21659=EDGE_CURVE ( 'NONE', #18309, #8904, #10392, .T. ) ;
#21660=ORIENTED_EDGE ( 'NONE', *, *, #15226, .F. ) ;
#21663=CARTESIAN_POINT ( 'NONE',  ( -30.37540678000427619, 6.000000000000000000, 3.499999999999999556 ) ) ;
#21667=AXIS2_PLACEMENT_3D ( 'NONE', #17601, #2379, #10679 ) ;
#21669=CARTESIAN_POINT ( 'NONE',  ( 15.21174975910707161, -51.61873716947361856, 68.00000000000000000 ) ) ;
#21671=EDGE_CURVE ( 'NONE', #16763, #6333, #8440, .T. ) ;
#21673=EDGE_CURVE ( 'NONE', #17663, #7349, #8956, .T. ) ;
#21677=LINE ( 'NONE', #16056, #4480 ) ;
#21679=VERTEX_POINT ( 'NONE', #4145 ) ;
#21681=CARTESIAN_POINT ( 'NONE',  ( 28.57540678000427548, 63.74634676501045050, 13.50000000000000000 ) ) ;
#21683=VECTOR ( 'NONE', #18959, 1000.000000000000000 ) ;
#21686=VERTEX_POINT ( 'NONE', #12523 ) ;
#21687=CARTESIAN_POINT ( 'NONE',  ( -15.05373532783226054, 52.39333378048836920, 13.50000000000000000 ) ) ;
#21690=VECTOR ( 'NONE', #20428, 1000.000000000000000 ) ;
#21691=EDGE_CURVE ( 'NONE', #3263, #12488, #21829, .T. ) ;
#21692=ORIENTED_EDGE ( 'NONE', *, *, #8127, .T. ) ;
#21693=CARTESIAN_POINT ( 'NONE',  ( 3.627054932750481964, 33.43424481021354921, 68.00000000000000000 ) ) ;
#21694=CARTESIAN_POINT ( 'NONE',  ( 0.000000000000000000, 51.61873716947361856, 14.00000000000000000 ) ) ;
#21695=LINE ( 'NONE', #7831, #16701 ) ;
#21696=VECTOR ( 'NONE', #8122, 1000.000000000000000 ) ;
#21701=PLANE ( 'NONE',  #270 ) ;
#21702=EDGE_CURVE ( 'NONE', #6237, #13366, #21176, .T. ) ;
#21704=CARTESIAN_POINT ( 'NONE',  ( -30.07540678000427548, 63.74634676501045050, 7.500000000000000000 ) ) ;
#21706=CARTESIAN_POINT ( 'NONE',  ( -15.95292532278785913, 52.11873716947361856, 14.00000000000000000 ) ) ;
#21709=CARTESIAN_POINT ( 'NONE',  ( -25.37540678000426908, 36.74634676501047181, 13.79999999999999893 ) ) ;
#21711=CARTESIAN_POINT ( 'NONE',  ( -15.95292532278785913, 34.11873716947361856, 109.6002446535588319 ) ) ;
#21713=ORIENTED_EDGE ( 'NONE', *, *, #16694, .T. ) ;
#21714=AXIS2_PLACEMENT_3D ( 'NONE', #3497, #20510, #6546 ) ;
#21715=AXIS2_PLACEMENT_3D ( 'NONE', #16888, #20486, #3584 ) ;
#21716=ORIENTED_EDGE ( 'NONE', *, *, #606, .T. ) ;
#21717=CARTESIAN_POINT ( 'NONE',  ( 0.000000000000000000, 32.61873716947361856, 68.00000000000000000 ) ) ;
#21718=EDGE_CURVE ( 'NONE', #12330, #7824, #21064, .T. ) ;
#21719=VECTOR ( 'NONE', #5192, 1000.000000000000000 ) ;
#21721=EDGE_CURVE ( 'NONE', #21652, #16241, #9299, .T. ) ;
#21722=AXIS2_PLACEMENT_3D ( 'NONE', #12180, #19035, #16067 ) ;
#21724=DIRECTION ( 'NONE',  ( 0.000000000000000000, 0.000000000000000000, 1.000000000000000000 ) ) ;
#21725=LINE ( 'NONE', #4809, #12380 ) ;
#21726=CARTESIAN_POINT ( 'NONE',  ( -30.67540678000428045, 63.74634676501045050, 3.799999999999999822 ) ) ;
#21727=DIRECTION ( 'NONE',  ( 0.000000000000000000, 0.000000000000000000, 1.000000000000000000 ) ) ;
#21730=VECTOR ( 'NONE', #17994, 1000.000000000000000 ) ;
#21732=CARTESIAN_POINT ( 'NONE',  ( 8.641460742840918030, -33.43424481021354921, 68.50000000000000000 ) ) ;
#21736=LINE ( 'NONE', #2925, #10440 ) ;
#21737=DIRECTION ( 'NONE',  ( 1.000000000000000000, 0.000000000000000000, 0.000000000000000000 ) ) ;
#21738=AXIS2_PLACEMENT_3D ( 'NONE', #7664, #1258, #13128 ) ;
#21739=AXIS2_PLACEMENT_3D ( 'NONE', #5347, #3877, #20879 ) ;
#21740=DIRECTION ( 'NONE',  ( 1.000000000000000000, 0.000000000000000000, 0.000000000000000000 ) ) ;
#21741=ORIENTED_EDGE ( 'NONE', *, *, #8597, .F. ) ;
#21742=DIRECTION ( 'NONE',  ( -0.000000000000000000, -0.000000000000000000, 1.000000000000000000 ) ) ;
#21753=VECTOR ( 'NONE', #7539, 1000.000000000000000 ) ;
#21756=CARTESIAN_POINT ( 'NONE',  ( -14.66174975910705136, -51.76873716947361714, 13.50000000000000000 ) ) ;
#21757=CARTESIAN_POINT ( 'NONE',  ( -32.20000000000001705, 71.00000000000001421, 1.500000000000000000 ) ) ;
#21759=DIRECTION ( 'NONE',  ( 0.000000000000000000, -1.000000000000000000, 0.000000000000000000 ) ) ;
#21762=CARTESIAN_POINT ( 'NONE',  ( -17.95292532278785913, 0.000000000000000000, 42.50000000000000711 ) ) ;
#21763=LINE ( 'NONE', #4404, #15753 ) ;
#21765=ORIENTED_EDGE ( 'NONE', *, *, #1563, .F. ) ;
#21766=VECTOR ( 'NONE', #3961, 1000.000000000000000 ) ;
#21767=ORIENTED_EDGE ( 'NONE', *, *, #16636, .F. ) ;
#21768=VERTEX_POINT ( 'NONE', #20645 ) ;
#21772=ORIENTED_EDGE ( 'NONE', *, *, #504, .T. ) ;
#21774=EDGE_CURVE ( 'NONE', #14314, #16813, #11085, .T. ) ;
#21775=VECTOR ( 'NONE', #10363, 1000.000000000000000 ) ;
#21778=EDGE_CURVE ( 'NONE', #17444, #11974, #12628, .T. ) ;
#21779=VECTOR ( 'NONE', #404, 1000.000000000000000 ) ;
#21782=AXIS2_PLACEMENT_3D ( 'NONE', #12120, #260, #20864 ) ;
#21789=CARTESIAN_POINT ( 'NONE',  ( 3.127054932750481964, -32.93424481021354921, 68.50000000000000000 ) ) ;
#21790=ORIENTED_EDGE ( 'NONE', *, *, #3092, .T. ) ;
#21794=ORIENTED_EDGE ( 'NONE', *, *, #6604, .T. ) ;
#21795=CARTESIAN_POINT ( 'NONE',  ( 0.000000000000000000, -38.74634676501045760, 42.50000000000000000 ) ) ;
#21800=ORIENTED_EDGE ( 'NONE', *, *, #18910, .F. ) ;
#21801=CARTESIAN_POINT ( 'NONE',  ( -18.22752199202934520, 39.04634676501046187, 13.50000000000000000 ) ) ;
#21802=CARTESIAN_POINT ( 'NONE',  ( 30.67540678000427690, 6.000000000000000000, 3.500000000000000000 ) ) ;
#21803=AXIS2_PLACEMENT_3D ( 'NONE', #1625, #9927, #10144 ) ;
#21808=DIRECTION ( 'NONE',  ( -1.000000000000000000, 0.000000000000000000, -0.000000000000000000 ) ) ;
#21809=CARTESIAN_POINT ( 'NONE',  ( 17.45292532278785913, 0.000000000000000000, 68.50000000000000000 ) ) ;
#21810=CARTESIAN_POINT ( 'NONE',  ( -23.04273156199908712, -2.261510999193106386, 13.20000000000004015 ) ) ;
#21812=CARTESIAN_POINT ( 'NONE',  ( 8.641460742840918030, 33.43424481021354921, 42.50000000000000000 ) ) ;
#21813=DIRECTION ( 'NONE',  ( 1.000000000000000000, 0.000000000000000000, 0.000000000000000000 ) ) ;
#21815=VECTOR ( 'NONE', #15697, 1000.000000000000000 ) ;
#21816=AXIS2_PLACEMENT_3D ( 'NONE', #2071, #5558, #279 ) ;
#21818=DIRECTION ( 'NONE',  ( 0.000000000000000000, 1.000000000000000000, 0.000000000000000000 ) ) ;
#21820=DIRECTION ( 'NONE',  ( -1.000000000000000000, -0.000000000000000000, -0.000000000000000000 ) ) ;
#21821=EDGE_CURVE ( 'NONE', #4141, #10497, #18595, .T. ) ;
#21824=DIRECTION ( 'NONE',  ( -2.832483164223434527E-16, -1.000000000000000000, 0.000000000000000000 ) ) ;
#21827=ORIENTED_EDGE ( 'NONE', *, *, #17758, .T. ) ;
#21829=CIRCLE ( 'NONE', #20753, 4.999999999999997335 ) ;
#21830=ADVANCED_FACE ( 'NONE', ( #2255 ), #14657, .F. ) ;
#21831=AXIS2_PLACEMENT_3D ( 'NONE', #3949, #19152, #2357 ) ;
#21833=EDGE_LOOP ( 'NONE', ( #20166, #9990, #8221, #7602 ) ) ;
#21836=ORIENTED_EDGE ( 'NONE', *, *, #19475, .F. ) ;
#21837=DIRECTION ( 'NONE',  ( -0.000000000000000000, -0.000000000000000000, -1.000000000000000000 ) ) ;
#21841=CARTESIAN_POINT ( 'NONE',  ( -29.37540678000427619, 4.700000000000000178, 3.500000000000000000 ) ) ;
#21844=AXIS2_PLACEMENT_3D ( 'NONE', #9719, #14956, #2769 ) ;
#21847=DIRECTION ( 'NONE',  ( -0.000000000000000000, -0.000000000000000000, -1.000000000000000000 ) ) ;
#21848=ORIENTED_EDGE ( 'NONE', *, *, #14831, .F. ) ;
#21852=DIRECTION ( 'NONE',  ( 0.000000000000000000, -0.000000000000000000, -1.000000000000000000 ) ) ;
#21853=ORIENTED_EDGE ( 'NONE', *, *, #17756, .F. ) ;
#21854=EDGE_LOOP ( 'NONE', ( #20454, #2942, #16794, #11138 ) ) ;
#21855=DIRECTION ( 'NONE',  ( 1.000000000000000000, 0.000000000000000000, 0.000000000000000000 ) ) ;
#21856=ORIENTED_EDGE ( 'NONE', *, *, #2791, .F. ) ;
#21858=EDGE_CURVE ( 'NONE', #1401, #17690, #19602, .T. ) ;
#21860=ADVANCED_FACE ( 'NONE', ( #5856 ), #21078, .F. ) ;
#21861=ORIENTED_EDGE ( 'NONE', *, *, #20245, .F. ) ;
#21862=ORIENTED_EDGE ( 'NONE', *, *, #14276, .T. ) ;
#21864=CIRCLE ( 'NONE', #14699, 0.5000000000000004441 ) ;
#21866=VERTEX_POINT ( 'NONE', #19713 ) ;
#21868=VECTOR ( 'NONE', #10444, 1000.000000000000000 ) ;
#21869=CARTESIAN_POINT ( 'NONE',  ( -23.02398829872513986, 3.528912754968630772, 13.79999999999999893 ) ) ;
#21870=VECTOR ( 'NONE', #4847, 1000.000000000000000 ) ;
#21872=DIRECTION ( 'NONE',  ( 0.000000000000000000, 1.000000000000000000, 0.000000000000000000 ) ) ;
#21873=EDGE_CURVE ( 'NONE', #3158, #15670, #5756, .T. ) ;
#21875=CARTESIAN_POINT ( 'NONE',  ( 17.93704824106378837, 0.000000000000000000, 13.87500000000000000 ) ) ;
#21878=VERTEX_POINT ( 'NONE', #7536 ) ;
#21882=CIRCLE ( 'NONE', #19727, 0.3000000000000003775 ) ;
#21883=CARTESIAN_POINT ( 'NONE',  ( -25.37540678000429040, -36.74634676501047181, 13.79999999999999893 ) ) ;
#21887=ORIENTED_EDGE ( 'NONE', *, *, #7683, .T. ) ;
#21890=CARTESIAN_POINT ( 'NONE',  ( 29.37540678000427619, -5.000000000000000000, 7.500000000000000000 ) ) ;
#21893=DIRECTION ( 'NONE',  ( 0.000000000000000000, 0.000000000000000000, -1.000000000000000000 ) ) ;
#21894=CARTESIAN_POINT ( 'NONE',  ( 32.20000000000001705, -71.00000000000001421, 1.500000000000000000 ) ) ;
#21896=DIRECTION ( 'NONE',  ( -0.000000000000000000, 1.000000000000000000, 0.000000000000000000 ) ) ;
#21898=CARTESIAN_POINT ( 'NONE',  ( 25.37540678000427263, -68.74634676501045760, 7.500000000000000000 ) ) ;
#21899=EDGE_CURVE ( 'NONE', #2296, #14801, #12636, .T. ) ;
#21900=ORIENTED_EDGE ( 'NONE', *, *, #5816, .F. ) ;
#21901=PLANE ( 'NONE',  #11619 ) ;
#21902=CIRCLE ( 'NONE', #2592, 0.5000000000000004441 ) ;
#21906=ORIENTED_EDGE ( 'NONE', *, *, #14383, .F. ) ;
#21907=ORIENTED_EDGE ( 'NONE', *, *, #17405, .F. ) ;
#21908=CARTESIAN_POINT ( 'NONE',  ( -14.75141515765153954, 52.14252004795846318, 13.50000000000000000 ) ) ;
#21909=FACE_OUTER_BOUND ( 'NONE', #6757, .T. ) ;
#21910=ORIENTED_EDGE ( 'NONE', *, *, #10143, .F. ) ;
#21913=ORIENTED_EDGE ( 'NONE', *, *, #11020, .T. ) ;
#21916=CARTESIAN_POINT ( 'NONE',  ( -14.66174975910705136, -42.11054587065083155, 13.50000000000000000 ) ) ;
#21918=CARTESIAN_POINT ( 'NONE',  ( -3.627054932750481964, 32.61873716947361856, 42.50000000000000711 ) ) ;
#21920=DIRECTION ( 'NONE',  ( 0.000000000000000000, -0.000000000000000000, 1.000000000000000000 ) ) ;
#21921=CARTESIAN_POINT ( 'NONE',  ( 9.641460742840918030, -32.11873716947361856, 68.50000000000000000 ) ) ;
#21923=CARTESIAN_POINT ( 'NONE',  ( -17.92752199202933738, -38.74634676501045760, 13.62426406871192874 ) ) ;
#21925=ORIENTED_EDGE ( 'NONE', *, *, #18910, .T. ) ;
#21930=CARTESIAN_POINT ( 'NONE',  ( 14.66174975910705847, -51.76873716947361714, 13.50000000000000000 ) ) ;
#21932=VERTEX_POINT ( 'NONE', #9805 ) ;
#21933=ORIENTED_EDGE ( 'NONE', *, *, #3683, .F. ) ;
#21934=CARTESIAN_POINT ( 'NONE',  ( 14.96174975910705918, 51.86873716947361856, 14.00000000000000000 ) ) ;
#21935=VERTEX_POINT ( 'NONE', #4664 ) ;
#21936=EDGE_CURVE ( 'NONE', #20218, #12188, #9317, .T. ) ;
#21938=EDGE_LOOP ( 'NONE', ( #5615, #20444, #10060, #12871 ) ) ;
#21939=DIRECTION ( 'NONE',  ( 1.000000000000000000, 0.000000000000000000, 0.000000000000000000 ) ) ;
#21941=DIRECTION ( 'NONE',  ( 0.000000000000000000, -0.000000000000000000, -1.000000000000000000 ) ) ;
#21943=CARTESIAN_POINT ( 'NONE',  ( -29.37540678000427619, 4.700000000000000178, 3.799999999999999822 ) ) ;
#21945=EDGE_CURVE ( 'NONE', #3260, #1513, #6485, .T. ) ;
#21948=LINE ( 'NONE', #16896, #11559 ) ;
#21949=EDGE_CURVE ( 'NONE', #2108, #19696, #13026, .T. ) ;
#21951=CARTESIAN_POINT ( 'NONE',  ( 0.000000000000000000, -5.000000000000000000, 7.500000000000000000 ) ) ;
#21953=CARTESIAN_POINT ( 'NONE',  ( 29.13662752439705272, 5.000000000000000000, 7.200000000000000178 ) ) ;
#21955=FACE_OUTER_BOUND ( 'NONE', #16414, .T. ) ;
#21956=AXIS2_PLACEMENT_3D ( 'NONE', #18458, #6856, #18800 ) ;
#21960=ORIENTED_EDGE ( 'NONE', *, *, #19394, .T. ) ;
#21963=ORIENTED_EDGE ( 'NONE', *, *, #4471, .F. ) ;
#21965=ORIENTED_EDGE ( 'NONE', *, *, #18507, .F. ) ;
#21966=ORIENTED_EDGE ( 'NONE', *, *, #15913, .F. ) ;
#21967=DIRECTION ( 'NONE',  ( 0.000000000000000000, -0.000000000000000000, -1.000000000000000000 ) ) ;
#21970=ORIENTED_EDGE ( 'NONE', *, *, #10874, .T. ) ;
#21972=EDGE_CURVE ( 'NONE', #13239, #18812, #11454, .T. ) ;
#21974=EDGE_CURVE ( 'NONE', #4912, #9883, #8932, .T. ) ;
#21975=LINE ( 'NONE', #15358, #9343 ) ;
#21976=CARTESIAN_POINT ( 'NONE',  ( 25.37540678000427263, -66.94634676501046044, 13.19999999999999929 ) ) ;
#21978=DIRECTION ( 'NONE',  ( 1.000000000000000000, 0.000000000000000000, 0.000000000000000000 ) ) ;
#21979=ORIENTED_EDGE ( 'NONE', *, *, #17949, .T. ) ;
#21980=ORIENTED_EDGE ( 'NONE', *, *, #6936, .F. ) ;
#21983=DIRECTION ( 'NONE',  ( 1.000000000000000000, 0.000000000000000000, 0.000000000000000000 ) ) ;
#21987=EDGE_CURVE ( 'NONE', #1657, #4141, #841, .T. ) ;
#21989=DIRECTION ( 'NONE',  ( -0.000000000000000000, -0.000000000000000000, -1.000000000000000000 ) ) ;
#21990=CARTESIAN_POINT ( 'NONE',  ( -15.95292532278785913, 52.11873716947361856, 68.00000000000000000 ) ) ;
#21991=EDGE_CURVE ( 'NONE', #21652, #1033, #12811, .T. ) ;
#21993=DIRECTION ( 'NONE',  ( 0.000000000000000000, 0.000000000000000000, 1.000000000000000000 ) ) ;
#21994=ORIENTED_EDGE ( 'NONE', *, *, #17890, .T. ) ;
#21996=PLANE ( 'NONE',  #18183 ) ;
#21997=CARTESIAN_POINT ( 'NONE',  ( -31.50000000000002132, 72.00000000000001421, 1.800000000000000044 ) ) ;
#22006=FACE_OUTER_BOUND ( 'NONE', #1137, .T. ) ;
#22007=DIRECTION ( 'NONE',  ( 0.000000000000000000, 1.000000000000000000, 0.000000000000000000 ) ) ;
#22008=VERTEX_POINT ( 'NONE', #18715 ) ;
#22010=ORIENTED_EDGE ( 'NONE', *, *, #19576, .T. ) ;
#22012=DIRECTION ( 'NONE',  ( 1.000000000000000000, 0.000000000000000000, 0.000000000000000000 ) ) ;
#22013=ORIENTED_EDGE ( 'NONE', *, *, #12106, .T. ) ;
#22016=ORIENTED_EDGE ( 'NONE', *, *, #13604, .F. ) ;
#22017=CARTESIAN_POINT ( 'NONE',  ( 31.50000000000002132, 71.00000000000001421, 1.500000000000000000 ) ) ;
#22019=AXIS2_PLACEMENT_3D ( 'NONE', #1278, #8346, #20107 ) ;
#22020=TOROIDAL_SURFACE ( 'NONE', #1256, 5.300000000000004263, 0.2999999999999999889 ) ;
#22021=EDGE_CURVE ( 'NONE', #4383, #8471, #10378, .T. ) ;
#22022=ORIENTED_EDGE ( 'NONE', *, *, #12375, .T. ) ;
#22023=CARTESIAN_POINT ( 'NONE',  ( -23.02398829872513986, -3.419159475692170158, 13.52813170334705184 ) ) ;
#22024=ADVANCED_FACE ( 'NONE', ( #12105 ), #7154, .T. ) ;
#22025=CARTESIAN_POINT ( 'NONE',  ( -15.21174975910705207, 52.11873716947361856, 68.00000000000000000 ) ) ;
#22026=EDGE_CURVE ( 'NONE', #852, #483, #2485, .T. ) ;
#22034=AXIS2_PLACEMENT_3D ( 'NONE', #15674, #17676, #557 ) ;
#22036=LINE ( 'NONE', #1431, #6993 ) ;
#22037=AXIS2_PLACEMENT_3D ( 'NONE', #14091, #13762, #15459 ) ;
#22038=DIRECTION ( 'NONE',  ( -1.000000000000000000, 0.000000000000000000, 0.000000000000000000 ) ) ;
#22039=VERTEX_POINT ( 'NONE', #5523 ) ;
#22040=CIRCLE ( 'NONE', #919, 0.2999999999999999334 ) ;
#22046=CARTESIAN_POINT ( 'NONE',  ( -15.21174975910705207, 41.81054587065082728, 13.79999999999999893 ) ) ;
#22047=ORIENTED_EDGE ( 'NONE', *, *, #11432, .T. ) ;
#22048=CIRCLE ( 'NONE', #6683, 0.5000000000000004441 ) ;
#22049=AXIS2_PLACEMENT_3D ( 'NONE', #16830, #3529, #11679 ) ;
#22050=EDGE_CURVE ( 'NONE', #11165, #3327, #135, .T. ) ;
#22051=DIRECTION ( 'NONE',  ( 0.000000000000000000, -1.000000000000000000, 0.000000000000000000 ) ) ;
#22052=ORIENTED_EDGE ( 'NONE', *, *, #11911, .T. ) ;
#22053=CARTESIAN_POINT ( 'NONE',  ( -29.42156627136959557, 2.562835948873662506, 0.09431749384236855216 ) ) ;
#22059=DIRECTION ( 'NONE',  ( 0.000000000000000000, 0.000000000000000000, 1.000000000000000000 ) ) ;
#22060=DIRECTION ( 'NONE',  ( 0.9823853469773031755, 0.1868663427273193067, 0.000000000000000000 ) ) ;
#22061=AXIS2_PLACEMENT_3D ( 'NONE', #13472, #13358, #5202 ) ;
#22063=DIRECTION ( 'NONE',  ( 1.000000000000000000, 0.000000000000000000, 0.000000000000000000 ) ) ;
#22064=AXIS2_PLACEMENT_3D ( 'NONE', #3249, #16545, #6401 ) ;
#22066=VECTOR ( 'NONE', #20470, 1000.000000000000000 ) ;
#22067=CARTESIAN_POINT ( 'NONE',  ( 31.50000000000002132, 72.00000000000001421, 3.500000000000000000 ) ) ;
#22069=CARTESIAN_POINT ( 'NONE',  ( 27.37540678000427974, -5.683640910026986681, 42.50000000000000000 ) ) ;
#22070=ORIENTED_EDGE ( 'NONE', *, *, #10992, .T. ) ;
#22073=CYLINDRICAL_SURFACE ( 'NONE', #9589, 0.2999999999999999334 ) ;
#22075=EDGE_LOOP ( 'NONE', ( #14500, #13574, #18984, #21933 ) ) ;
#22076=EDGE_LOOP ( 'NONE', ( #15294, #7784, #15246, #19636 ) ) ;
#22079=EDGE_CURVE ( 'NONE', #16679, #3824, #580, .T. ) ;
#22080=CIRCLE ( 'NONE', #13843, 2.299999999999993161 ) ;
#22084=CYLINDRICAL_SURFACE ( 'NONE', #651, 0.2999999999999999334 ) ;
#22085=AXIS2_PLACEMENT_3D ( 'NONE', #5786, #8911, #10902 ) ;
#22086=FACE_OUTER_BOUND ( 'NONE', #6090, .T. ) ;
#22087=CARTESIAN_POINT ( 'NONE',  ( -17.45292532278785913, 38.74634676501045760, 13.99999999999999822 ) ) ;
#22088=AXIS2_PLACEMENT_3D ( 'NONE', #17511, #11014, #19194 ) ;
#22091=AXIS2_PLACEMENT_3D ( 'NONE', #5556, #11092, #17913 ) ;
#22092=CARTESIAN_POINT ( 'NONE',  ( 23.32398829872514057, 3.528912754968628551, 13.79999999999999893 ) ) ;
#22093=CARTESIAN_POINT ( 'NONE',  ( 0.000000000000000000, 0.000000000000000000, 42.50000000000000000 ) ) ;
#22094=LINE ( 'NONE', #21762, #17709 ) ;
#22095=ADVANCED_FACE ( 'NONE', ( #457 ), #11986, .T. ) ;
#22096=DIRECTION ( 'NONE',  ( 0.000000000000000000, 1.000000000000000000, 0.000000000000000000 ) ) ;
#22097=CIRCLE ( 'NONE', #2054, 0.2999999999999999334 ) ;
#22099=TOROIDAL_SURFACE ( 'NONE', #7822, 2.800000000000002043, 0.2999999999999999889 ) ;
#22100=AXIS2_PLACEMENT_3D ( 'NONE', #7493, #2436, #7047 ) ;
#22102=VERTEX_POINT ( 'NONE', #6986 ) ;
#22103=CYLINDRICAL_SURFACE ( 'NONE', #20646, 5.000000000000004441 ) ;
#22104=FACE_OUTER_BOUND ( 'NONE', #913, .T. ) ;
#22105=TOROIDAL_SURFACE ( 'NONE', #4235, 3.800000000000002931, 0.2999999999999999889 ) ;
#22106=CARTESIAN_POINT ( 'NONE',  ( 15.21174975910705918, -52.10286008774954780, 13.87500000000000000 ) ) ;
#22107=CIRCLE ( 'NONE', #11365, 0.5000000000000000000 ) ;
#22108=TOROIDAL_SURFACE ( 'NONE', #8179, 1.500000000000000000, 0.5000000000000000000 ) ;
#22109=ADVANCED_FACE ( 'NONE', ( #6886 ), #10543, .F. ) ;
#22110=EDGE_CURVE ( 'NONE', #20083, #6358, #14283, .T. ) ;
#22111=EDGE_CURVE ( 'NONE', #7135, #712, #13906, .T. ) ;
#22114=ADVANCED_FACE ( 'NONE', ( #5311 ), #3508, .F. ) ;
#22115=FACE_OUTER_BOUND ( 'NONE', #19456, .T. ) ;
#22117=DIRECTION ( 'NONE',  ( 0.000000000000000000, 0.000000000000000000, -1.000000000000000000 ) ) ;
#22118=ORIENTED_EDGE ( 'NONE', *, *, #18340, .T. ) ;
#22123=DIRECTION ( 'NONE',  ( 1.000000000000000000, 0.000000000000000000, -2.388292521039847891E-16 ) ) ;
#22125=ORIENTED_EDGE ( 'NONE', *, *, #18676, .T. ) ;
#22129=AXIS2_PLACEMENT_3D ( 'NONE', #15742, #20906, #9146 ) ;
#22131=VERTEX_POINT ( 'NONE', #10341 ) ;
#22133=DIRECTION ( 'NONE',  ( 0.000000000000000000, 0.000000000000000000, 1.000000000000000000 ) ) ;
#22135=VERTEX_POINT ( 'NONE', #13890 ) ;
#22137=VERTEX_POINT ( 'NONE', #20064 ) ;
#22138=CARTESIAN_POINT ( 'NONE',  ( 9.141460742840918030, 32.61873716947361856, 42.50000000000000711 ) ) ;
#22143=EDGE_CURVE ( 'NONE', #13733, #18637, #4830, .T. ) ;
#22144=ORIENTED_EDGE ( 'NONE', *, *, #15913, .T. ) ;
#22145=FACE_OUTER_BOUND ( 'NONE', #12481, .T. ) ;
#22147=AXIS2_PLACEMENT_3D ( 'NONE', #3592, #3695, #12508 ) ;
#22149=CARTESIAN_POINT ( 'NONE',  ( -23.02398829872513986, -3.264788445950693507, 13.78841001078610873 ) ) ;
#22152=LINE ( 'NONE', #12146, #18307 ) ;
#22155=CARTESIAN_POINT ( 'NONE',  ( -25.37540678000427263, 67.54634676501045476, 7.500000000000000000 ) ) ;
#22156=CARTESIAN_POINT ( 'NONE',  ( -18.05178606074127501, -38.87061083372239523, 13.49999999999999822 ) ) ;
#22157=DIRECTION ( 'NONE',  ( 0.000000000000000000, 1.000000000000000000, 0.000000000000000000 ) ) ;
#22158=ORIENTED_EDGE ( 'NONE', *, *, #17564, .T. ) ;
#22160=VECTOR ( 'NONE', #4031, 1000.000000000000000 ) ;
#22162=CARTESIAN_POINT ( 'NONE',  ( -15.21174975910705207, -51.86873716947361856, 14.00000000000000000 ) ) ;
ENDSEC;
END-ISO-10303-21;
